ISO-10303-21;
HEADER;
/* Generated by software containing ST-Developer
 * from STEP Tools, Inc. (www.steptools.com) 
 */

FILE_DESCRIPTION(
/* description */ ('Independent30mm screw-fed quill/spindle unit with16mm straight tool s
ocket, radial set screw, native reusable open ball bearings, retained 
inner/outer race stacks, keyed quill guide and M12x1.75 fine feed. Ext
ernal moving drive and tool not included. Ideal cage orbital links; in
dividual ball spin, force and preload not simulated. No drilling capac
ity, runout, speed, torque, load, life or machine safety rating.'),
/* implementation_level */ '2;1');

FILE_NAME(
/* name */ 'Set screw M6x18.step',
/* time_stamp */ '2026-11-08T18:59:42-08:00',
/* author */ (''),
/* organization */ (''),
/* preprocessor_version */ 'ST-DEVELOPER v20.2',
/* originating_system */ 'Autodesk Translation Framework v15.17.0.0',
/* authorisation */ '');

FILE_SCHEMA (('AUTOMOTIVE_DESIGN { 1 0 10303 214 3 1 1 }'));
ENDSEC;

DATA;
#10=MECHANICAL_DESIGN_GEOMETRIC_PRESENTATION_REPRESENTATION('',(#1602),#63898);
#262=B_SPLINE_SURFACE_WITH_KNOTS('',3,3,((#58934,#58935,#58936,#58937,#58938,
#58939,#58940,#58941,#58942,#58943,#58944,#58945,#58946,#58947,#58948,#58949,
#58950,#58951,#58952,#58953,#58954,#58955,#58956,#58957,#58958,#58959,#58960,
#58961,#58962,#58963,#58964,#58965,#58966,#58967,#58968,#58969,#58970,#58971,
#58972,#58973,#58974,#58975,#58976,#58977,#58978,#58979,#58980,#58981,#58982,
#58983,#58984,#58985,#58986,#58987,#58988,#58989,#58990,#58991,#58992,#58993,
#58994,#58995,#58996,#58997,#58998,#58999,#59000,#59001,#59002,#59003,#59004,
#59005,#59006,#59007,#59008,#59009,#59010,#59011,#59012,#59013,#59014,#59015,
#59016,#59017,#59018,#59019,#59020,#59021,#59022,#59023,#59024,#59025,#59026,
#59027,#59028,#59029,#59030,#59031,#59032,#59033,#59034,#59035,#59036,#59037,
#59038,#59039,#59040,#59041,#59042,#59043,#59044,#59045,#59046,#59047,#59048,
#59049,#59050,#59051,#59052),(#59053,#59054,#59055,#59056,#59057,#59058,
#59059,#59060,#59061,#59062,#59063,#59064,#59065,#59066,#59067,#59068,#59069,
#59070,#59071,#59072,#59073,#59074,#59075,#59076,#59077,#59078,#59079,#59080,
#59081,#59082,#59083,#59084,#59085,#59086,#59087,#59088,#59089,#59090,#59091,
#59092,#59093,#59094,#59095,#59096,#59097,#59098,#59099,#59100,#59101,#59102,
#59103,#59104,#59105,#59106,#59107,#59108,#59109,#59110,#59111,#59112,#59113,
#59114,#59115,#59116,#59117,#59118,#59119,#59120,#59121,#59122,#59123,#59124,
#59125,#59126,#59127,#59128,#59129,#59130,#59131,#59132,#59133,#59134,#59135,
#59136,#59137,#59138,#59139,#59140,#59141,#59142,#59143,#59144,#59145,#59146,
#59147,#59148,#59149,#59150,#59151,#59152,#59153,#59154,#59155,#59156,#59157,
#59158,#59159,#59160,#59161,#59162,#59163,#59164,#59165,#59166,#59167,#59168,
#59169,#59170,#59171),(#59172,#59173,#59174,#59175,#59176,#59177,#59178,
#59179,#59180,#59181,#59182,#59183,#59184,#59185,#59186,#59187,#59188,#59189,
#59190,#59191,#59192,#59193,#59194,#59195,#59196,#59197,#59198,#59199,#59200,
#59201,#59202,#59203,#59204,#59205,#59206,#59207,#59208,#59209,#59210,#59211,
#59212,#59213,#59214,#59215,#59216,#59217,#59218,#59219,#59220,#59221,#59222,
#59223,#59224,#59225,#59226,#59227,#59228,#59229,#59230,#59231,#59232,#59233,
#59234,#59235,#59236,#59237,#59238,#59239,#59240,#59241,#59242,#59243,#59244,
#59245,#59246,#59247,#59248,#59249,#59250,#59251,#59252,#59253,#59254,#59255,
#59256,#59257,#59258,#59259,#59260,#59261,#59262,#59263,#59264,#59265,#59266,
#59267,#59268,#59269,#59270,#59271,#59272,#59273,#59274,#59275,#59276,#59277,
#59278,#59279,#59280,#59281,#59282,#59283,#59284,#59285,#59286,#59287,#59288,
#59289,#59290),(#59291,#59292,#59293,#59294,#59295,#59296,#59297,#59298,
#59299,#59300,#59301,#59302,#59303,#59304,#59305,#59306,#59307,#59308,#59309,
#59310,#59311,#59312,#59313,#59314,#59315,#59316,#59317,#59318,#59319,#59320,
#59321,#59322,#59323,#59324,#59325,#59326,#59327,#59328,#59329,#59330,#59331,
#59332,#59333,#59334,#59335,#59336,#59337,#59338,#59339,#59340,#59341,#59342,
#59343,#59344,#59345,#59346,#59347,#59348,#59349,#59350,#59351,#59352,#59353,
#59354,#59355,#59356,#59357,#59358,#59359,#59360,#59361,#59362,#59363,#59364,
#59365,#59366,#59367,#59368,#59369,#59370,#59371,#59372,#59373,#59374,#59375,
#59376,#59377,#59378,#59379,#59380,#59381,#59382,#59383,#59384,#59385,#59386,
#59387,#59388,#59389,#59390,#59391,#59392,#59393,#59394,#59395,#59396,#59397,
#59398,#59399,#59400,#59401,#59402,#59403,#59404,#59405,#59406,#59407,#59408,
#59409)),.UNSPECIFIED.,.F.,.F.,.F.,(4,4),(4,1,1,1,1,1,1,1,1,1,1,1,1,1,1,
1,1,1,1,1,1,1,1,1,1,1,1,1,1,1,1,1,1,1,1,1,1,1,1,1,1,1,1,1,1,1,1,1,1,1,1,
1,1,1,1,1,1,1,1,1,1,1,1,1,1,1,1,1,1,1,1,1,1,1,1,1,1,1,1,1,1,1,1,1,1,1,1,
1,1,1,1,1,1,1,1,1,1,1,1,1,1,1,1,1,1,1,1,1,1,1,1,1,1,1,1,1,4),(0.,0.0658467982010768),
(8.30747755240098,9.30028767054014,10.2930977886793,11.2859079068184,12.2787180249576,
13.2715281430967,14.2643382612359,15.2571483793751,16.2499584975142,17.2427686156534,
18.2355787337925,19.2283888519317,20.2211989700708,21.21400908821,22.2068192063491,
23.1996293244883,24.1924394426274,25.1852495607666,26.1780596789057,27.1708697970449,
28.163679915184,29.1564900333232,30.1493001514623,31.1421102696015,32.1349203877406,
33.1277305058798,34.120540624019,35.1133507421581,36.1061608602973,37.0989709784364,
38.0917810965756,39.0845912147147,40.0774013328539,41.070211450993,42.0630215691322,
43.0558316872713,44.0486418054105,45.0414519235496,46.0342620416888,47.0270721598279,
48.0198822779671,49.0126923961063,50.0055025142454,50.9983126323846,51.9911227505237,
52.9839328686629,53.976742986802,54.9695531049412,55.9623632230803,56.9551733412195,
57.9479834593586,58.9407935774978,59.9336036956369,60.9264138137761,61.9192239319152,
62.9120340500544,63.9048441681935,64.8976542863327,65.8904644044719,66.883274522611,
67.8760846407502,68.8688947588893,69.8617048770285,70.8545149951676,71.8473251133068,
72.8401352314459,73.8329453495851,74.8257554677242,75.8185655858634,76.8113757040025,
77.8041858221417,78.7969959402808,79.78980605842,80.7826161765591,81.7754262946983,
82.7682364128375,83.7610465309766,84.7538566491157,85.7466667672549,86.7394768853941,
87.7322870035332,88.7250971216724,89.7179072398115,90.7107173579507,91.7035274760898,
92.696337594229,93.6891477123681,94.6819578305073,95.6747679486464,96.6675780667856,
97.6603881849247,98.6531983030639,99.646008421203,100.638818539342,101.631628657481,
102.624438775621,103.61724889376,104.610059011899,105.602869130038,106.595679248177,
107.588489366316,108.581299484455,109.574109602595,110.566919720734,111.559729838873,
112.552539957012,113.545350075151,114.53816019329,115.530970311429,116.523780429569,
117.516590547708,118.509400665847,119.502210783986,120.495020902125,121.487831020264,
122.480641138404,123.473451256543),.UNSPECIFIED.);
#263=B_SPLINE_SURFACE_WITH_KNOTS('',3,3,((#59633,#59634,#59635,#59636,#59637,
#59638,#59639,#59640,#59641,#59642,#59643,#59644,#59645,#59646,#59647,#59648,
#59649,#59650,#59651,#59652,#59653,#59654,#59655,#59656,#59657,#59658,#59659,
#59660,#59661,#59662,#59663,#59664,#59665,#59666,#59667,#59668,#59669,#59670,
#59671,#59672,#59673,#59674,#59675,#59676,#59677,#59678,#59679,#59680,#59681,
#59682,#59683,#59684,#59685,#59686,#59687,#59688,#59689,#59690,#59691,#59692,
#59693,#59694,#59695,#59696,#59697,#59698,#59699,#59700,#59701,#59702,#59703,
#59704,#59705,#59706,#59707,#59708,#59709,#59710,#59711,#59712,#59713,#59714,
#59715,#59716,#59717,#59718,#59719,#59720,#59721,#59722,#59723,#59724,#59725,
#59726,#59727,#59728,#59729,#59730,#59731,#59732,#59733,#59734,#59735,#59736,
#59737,#59738,#59739,#59740,#59741,#59742,#59743,#59744,#59745,#59746,#59747,
#59748,#59749,#59750,#59751),(#59752,#59753,#59754,#59755,#59756,#59757,
#59758,#59759,#59760,#59761,#59762,#59763,#59764,#59765,#59766,#59767,#59768,
#59769,#59770,#59771,#59772,#59773,#59774,#59775,#59776,#59777,#59778,#59779,
#59780,#59781,#59782,#59783,#59784,#59785,#59786,#59787,#59788,#59789,#59790,
#59791,#59792,#59793,#59794,#59795,#59796,#59797,#59798,#59799,#59800,#59801,
#59802,#59803,#59804,#59805,#59806,#59807,#59808,#59809,#59810,#59811,#59812,
#59813,#59814,#59815,#59816,#59817,#59818,#59819,#59820,#59821,#59822,#59823,
#59824,#59825,#59826,#59827,#59828,#59829,#59830,#59831,#59832,#59833,#59834,
#59835,#59836,#59837,#59838,#59839,#59840,#59841,#59842,#59843,#59844,#59845,
#59846,#59847,#59848,#59849,#59850,#59851,#59852,#59853,#59854,#59855,#59856,
#59857,#59858,#59859,#59860,#59861,#59862,#59863,#59864,#59865,#59866,#59867,
#59868,#59869,#59870),(#59871,#59872,#59873,#59874,#59875,#59876,#59877,
#59878,#59879,#59880,#59881,#59882,#59883,#59884,#59885,#59886,#59887,#59888,
#59889,#59890,#59891,#59892,#59893,#59894,#59895,#59896,#59897,#59898,#59899,
#59900,#59901,#59902,#59903,#59904,#59905,#59906,#59907,#59908,#59909,#59910,
#59911,#59912,#59913,#59914,#59915,#59916,#59917,#59918,#59919,#59920,#59921,
#59922,#59923,#59924,#59925,#59926,#59927,#59928,#59929,#59930,#59931,#59932,
#59933,#59934,#59935,#59936,#59937,#59938,#59939,#59940,#59941,#59942,#59943,
#59944,#59945,#59946,#59947,#59948,#59949,#59950,#59951,#59952,#59953,#59954,
#59955,#59956,#59957,#59958,#59959,#59960,#59961,#59962,#59963,#59964,#59965,
#59966,#59967,#59968,#59969,#59970,#59971,#59972,#59973,#59974,#59975,#59976,
#59977,#59978,#59979,#59980,#59981,#59982,#59983,#59984,#59985,#59986,#59987,
#59988,#59989),(#59990,#59991,#59992,#59993,#59994,#59995,#59996,#59997,
#59998,#59999,#60000,#60001,#60002,#60003,#60004,#60005,#60006,#60007,#60008,
#60009,#60010,#60011,#60012,#60013,#60014,#60015,#60016,#60017,#60018,#60019,
#60020,#60021,#60022,#60023,#60024,#60025,#60026,#60027,#60028,#60029,#60030,
#60031,#60032,#60033,#60034,#60035,#60036,#60037,#60038,#60039,#60040,#60041,
#60042,#60043,#60044,#60045,#60046,#60047,#60048,#60049,#60050,#60051,#60052,
#60053,#60054,#60055,#60056,#60057,#60058,#60059,#60060,#60061,#60062,#60063,
#60064,#60065,#60066,#60067,#60068,#60069,#60070,#60071,#60072,#60073,#60074,
#60075,#60076,#60077,#60078,#60079,#60080,#60081,#60082,#60083,#60084,#60085,
#60086,#60087,#60088,#60089,#60090,#60091,#60092,#60093,#60094,#60095,#60096,
#60097,#60098,#60099,#60100,#60101,#60102,#60103,#60104,#60105,#60106,#60107,
#60108)),.UNSPECIFIED.,.F.,.F.,.F.,(4,4),(4,1,1,1,1,1,1,1,1,1,1,1,1,1,1,
1,1,1,1,1,1,1,1,1,1,1,1,1,1,1,1,1,1,1,1,1,1,1,1,1,1,1,1,1,1,1,1,1,1,1,1,
1,1,1,1,1,1,1,1,1,1,1,1,1,1,1,1,1,1,1,1,1,1,1,1,1,1,1,1,1,1,1,1,1,1,1,1,
1,1,1,1,1,1,1,1,1,1,1,1,1,1,1,1,1,1,1,1,1,1,1,1,1,1,1,1,1,4),(0.,0.0658467982010768),
(11.6150328478182,12.6078429659573,13.6006530840965,14.5934632022356,15.5862733203748,
16.5790834385139,17.5718935566531,18.5647036747922,19.5575137929314,20.5503239110706,
21.5431340292097,22.5359441473489,23.528754265488,24.5215643836272,25.5143745017663,
26.5071846199055,27.4999947380446,28.4928048561838,29.4856149743229,30.4784250924621,
31.4712352106012,32.4640453287404,33.4568554468795,34.4496655650187,35.4424756831578,
36.435285801297,37.4280959194362,38.4209060375753,39.4137161557145,40.4065262738536,
41.3993363919928,42.3921465101319,43.3849566282711,44.3777667464102,45.3705768645494,
46.3633869826885,47.3561971008277,48.3490072189668,49.341817337106,50.3346274552451,
51.3274375733843,52.3202476915234,53.3130578096626,54.3058679278017,55.2986780459409,
56.2914881640801,57.2842982822192,58.2771084003584,59.2699185184975,60.2627286366367,
61.2555387547758,62.248348872915,63.2411589910541,64.2339691091933,65.2267792273324,
66.2195893454716,67.2123994636107,68.2052095817499,69.198019699889,70.1908298180282,
71.1836399361674,72.1764500543065,73.1692601724456,74.1620702905848,75.154880408724,
76.1476905268631,77.1405006450023,78.1333107631414,79.1261208812806,80.1189309994197,
81.1117411175589,82.104551235698,83.0973613538372,84.0901714719763,85.0829815901155,
86.0757917082546,87.0686018263938,88.0614119445329,89.0542220626721,90.0470321808113,
91.0398422989504,92.0326524170896,93.0254625352287,94.0182726533679,95.011082771507,
96.0038928896462,96.9967030077853,97.9895131259245,98.9823232440636,99.9751333622028,
100.967943480342,101.960753598481,102.95356371662,103.946373834759,104.939183952899,
105.931994071038,106.924804189177,107.917614307316,108.910424425455,109.903234543594,
110.896044661733,111.888854779873,112.881664898012,113.874475016151,114.86728513429,
115.860095252429,116.852905370568,117.845715488708,118.838525606847,119.831335724986,
120.824145843125,121.816955961264,122.809766079403,123.802576197542,124.795386315682,
125.788196433821,126.78100655196),.UNSPECIFIED.);
#1368=B_SPLINE_CURVE_WITH_KNOTS('',3,(#57596,#57597,#57598,#57599,#57600,
#57601,#57602,#57603,#57604,#57605),.UNSPECIFIED.,.F.,.F.,(4,3,3,4),(-4.09293042013067,
-3.97124047255661,-2.97843035441746,-2.06863817490915),.UNSPECIFIED.);
#1369=B_SPLINE_CURVE_WITH_KNOTS('',3,(#57608,#57609,#57610,#57611,#57612,
#57613,#57614),.UNSPECIFIED.,.F.,.F.,(4,3,4),(0.,0.992810118139154,1.11730040836816),
 .UNSPECIFIED.);
#1370=B_SPLINE_CURVE_WITH_KNOTS('',3,(#57619,#57620,#57621,#57622,#57623,
#57624,#57625,#57626,#57627,#57628,#57629,#57630,#57631,#57632,#57633,#57634,
#57635,#57636,#57637,#57638,#57639,#57640),.UNSPECIFIED.,.F.,.F.,(4,3,3,
3,3,3,3,4),(-10.3761157273103,-9.92810118139153,-8.93529106325238,-7.94248094511322,
-6.94967082697407,-5.95686070883492,-4.96405059069577,-4.09293042013067),
 .UNSPECIFIED.);
#1371=B_SPLINE_CURVE_WITH_KNOTS('',3,(#57641,#57642,#57643,#57644,#57645,
#57646,#57647,#57648,#57649,#57650,#57651,#57652,#57653,#57654,#57655,#57656,
#57657,#57658,#57659,#57660,#57661,#57662),.UNSPECIFIED.,.F.,.F.,(4,3,3,
3,3,3,3,4),(1.11730040836816,1.98562023627831,2.97843035441746,3.97124047255661,
4.96405059069576,5.95686070883492,6.94967082697407,7.40048571554774),
 .UNSPECIFIED.);
#1372=B_SPLINE_CURVE_WITH_KNOTS('',3,(#57667,#57668,#57669,#57670,#57671,
#57672,#57673,#57674,#57675,#57676,#57677,#57678,#57679,#57680,#57681,#57682,
#57683,#57684,#57685,#57686,#57687,#57688),.UNSPECIFIED.,.F.,.F.,(4,3,3,
3,3,3,3,4),(-16.6593010344898,-15.8849618902264,-14.8921517720873,-13.8993416539481,
-12.906531535809,-11.9137214176698,-10.9209112995307,-10.3761157273103),
 .UNSPECIFIED.);
#1373=B_SPLINE_CURVE_WITH_KNOTS('',3,(#57689,#57690,#57691,#57692,#57693,
#57694,#57695,#57696,#57697,#57698,#57699,#57700,#57701,#57702,#57703,#57704,
#57705,#57706,#57707,#57708,#57709,#57710),.UNSPECIFIED.,.F.,.F.,(4,3,3,
3,3,3,3,4),(7.40048571554774,7.94248094511322,8.93529106325238,9.92810118139153,
10.9209112995307,11.9137214176698,12.906531535809,13.6836710227273),
 .UNSPECIFIED.);
#1374=B_SPLINE_CURVE_WITH_KNOTS('',3,(#57715,#57716,#57717,#57718,#57719,
#57720,#57721,#57722,#57723,#57724,#57725,#57726,#57727,#57728,#57729,#57730,
#57731,#57732,#57733,#57734,#57735,#57736,#57737,#57738,#57739),
 .UNSPECIFIED.,.F.,.F.,(4,3,3,3,3,3,3,3,4),(-22.9424863416694,-22.8346327172005,
-21.8418225990614,-20.8490124809222,-19.8562023627831,-18.8633922446439,
-17.8705821265048,-16.8777720083656,-16.6593010344898),.UNSPECIFIED.);
#1375=B_SPLINE_CURVE_WITH_KNOTS('',3,(#57740,#57741,#57742,#57743,#57744,
#57745,#57746,#57747,#57748,#57749,#57750,#57751,#57752,#57753,#57754,#57755,
#57756,#57757,#57758,#57759,#57760,#57761,#57762,#57763,#57764),
 .UNSPECIFIED.,.F.,.F.,(4,3,3,3,3,3,3,3,4),(13.6836710227273,13.8993416539481,
14.8921517720873,15.8849618902264,16.8777720083656,17.8705821265047,18.8633922446439,
19.856202362783,19.9668563299069),.UNSPECIFIED.);
#1376=B_SPLINE_CURVE_WITH_KNOTS('',3,(#57769,#57770,#57771,#57772,#57773,
#57774,#57775,#57776,#57777,#57778,#57779,#57780,#57781,#57782,#57783,#57784,
#57785,#57786,#57787,#57788,#57789,#57790),.UNSPECIFIED.,.F.,.F.,(4,3,3,
3,3,3,3,4),(-29.225671648849,-28.7914934260354,-27.7986833078963,-26.8058731897571,
-25.813063071618,-24.8202529534788,-23.8274428353397,-22.9424863416694),
 .UNSPECIFIED.);
#1377=B_SPLINE_CURVE_WITH_KNOTS('',3,(#57791,#57792,#57793,#57794,#57795,
#57796,#57797,#57798,#57799,#57800,#57801,#57802,#57803,#57804,#57805,#57806,
#57807,#57808,#57809,#57810,#57811,#57812),.UNSPECIFIED.,.F.,.F.,(4,3,3,
3,3,3,3,4),(19.9668563299069,20.8490124809222,21.8418225990614,22.8346327172005,
23.8274428353397,24.8202529534788,25.813063071618,26.2500416370865),
 .UNSPECIFIED.);
#1378=B_SPLINE_CURVE_WITH_KNOTS('',3,(#57817,#57818,#57819,#57820,#57821,
#57822,#57823,#57824,#57825,#57826,#57827,#57828,#57829,#57830,#57831,#57832,
#57833,#57834,#57835,#57836,#57837,#57838),.UNSPECIFIED.,.F.,.F.,(4,3,3,
3,3,3,3,4),(-35.5088569560286,-34.7483541348703,-33.7555440167312,-32.762733898592,
-31.7699237804529,-30.7771136623137,-29.7843035441746,-29.225671648849),
 .UNSPECIFIED.);
#1379=B_SPLINE_CURVE_WITH_KNOTS('',3,(#57839,#57840,#57841,#57842,#57843,
#57844,#57845,#57846,#57847,#57848,#57849,#57850,#57851,#57852,#57853,#57854,
#57855,#57856,#57857,#57858,#57859,#57860),.UNSPECIFIED.,.F.,.F.,(4,3,3,
3,3,3,3,4),(26.2500416370865,26.8058731897571,27.7986833078963,28.7914934260354,
29.7843035441746,30.7771136623137,31.7699237804529,32.5332269442661),
 .UNSPECIFIED.);
#1380=B_SPLINE_CURVE_WITH_KNOTS('',3,(#57865,#57866,#57867,#57868,#57869,
#57870,#57871,#57872,#57873,#57874,#57875,#57876,#57877,#57878,#57879,#57880,
#57881,#57882,#57883,#57884,#57885,#57886,#57887,#57888,#57889),
 .UNSPECIFIED.,.F.,.F.,(4,3,3,3,3,3,3,3,4),(-41.7920422632082,-41.6980249618444,
-40.7052148437053,-39.7124047255661,-38.719594607427,-37.7267844892878,
-36.7339743711486,-35.7411642530095,-35.5088569560286),.UNSPECIFIED.);
#1381=B_SPLINE_CURVE_WITH_KNOTS('',3,(#57890,#57891,#57892,#57893,#57894,
#57895,#57896,#57897,#57898,#57899,#57900,#57901,#57902,#57903,#57904,#57905,
#57906,#57907,#57908,#57909,#57910,#57911,#57912,#57913,#57914),
 .UNSPECIFIED.,.F.,.F.,(4,3,3,3,3,3,3,3,4),(32.5332269442661,32.762733898592,
33.7555440167312,34.7483541348703,35.7411642530095,36.7339743711486,37.7267844892878,
38.7195946074269,38.8164122514457),.UNSPECIFIED.);
#1382=B_SPLINE_CURVE_WITH_KNOTS('',3,(#57919,#57920,#57921,#57922,#57923,
#57924,#57925,#57926,#57927,#57928,#57929,#57930,#57931,#57932,#57933,#57934,
#57935,#57936,#57937,#57938,#57939,#57940),.UNSPECIFIED.,.F.,.F.,(4,3,3,
3,3,3,3,4),(-48.0752275703878,-47.6548856706793,-46.6620755525402,-45.669265434401,
-44.6764553162619,-43.6836451981227,-42.6908350799836,-41.7920422632082),
 .UNSPECIFIED.);
#1383=B_SPLINE_CURVE_WITH_KNOTS('',3,(#57941,#57942,#57943,#57944,#57945,
#57946,#57947,#57948,#57949,#57950,#57951,#57952,#57953,#57954,#57955,#57956,
#57957,#57958,#57959,#57960,#57961,#57962),.UNSPECIFIED.,.F.,.F.,(4,3,3,
3,3,3,3,4),(38.8164122514457,39.7124047255661,40.7052148437053,41.6980249618444,
42.6908350799836,43.6836451981227,44.6764553162619,45.0995975586253),
 .UNSPECIFIED.);
#1384=B_SPLINE_CURVE_WITH_KNOTS('',3,(#57967,#57968,#57969,#57970,#57971,
#57972,#57973,#57974,#57975,#57976,#57977,#57978,#57979,#57980,#57981,#57982,
#57983,#57984,#57985,#57986,#57987,#57988),.UNSPECIFIED.,.F.,.F.,(4,3,3,
3,3,3,3,4),(-54.3584128775674,-53.6117463795143,-52.6189362613751,-51.626126143236,
-50.6333160250968,-49.6405059069576,-48.6476957888185,-48.0752275703878),
 .UNSPECIFIED.);
#1385=B_SPLINE_CURVE_WITH_KNOTS('',3,(#57989,#57990,#57991,#57992,#57993,
#57994,#57995,#57996,#57997,#57998,#57999,#58000,#58001,#58002,#58003,#58004,
#58005,#58006,#58007,#58008,#58009,#58010),.UNSPECIFIED.,.F.,.F.,(4,3,3,
3,3,3,3,4),(45.0995975586253,45.669265434401,46.6620755525402,47.6548856706793,
48.6476957888185,49.6405059069576,50.6333160250968,51.3827828658049),
 .UNSPECIFIED.);
#1386=B_SPLINE_CURVE_WITH_KNOTS('',3,(#58015,#58016,#58017,#58018,#58019,
#58020,#58021,#58022,#58023,#58024,#58025,#58026,#58027,#58028,#58029,#58030,
#58031,#58032,#58033,#58034,#58035,#58036,#58037,#58038,#58039),
 .UNSPECIFIED.,.F.,.F.,(4,3,3,3,3,3,3,3,4),(-60.641598184747,-60.5614172064883,
-59.5686070883492,-58.57579697021,-57.5829868520709,-56.5901767339317,-55.5973666157926,
-54.6045564976534,-54.3584128775674),.UNSPECIFIED.);
#1387=B_SPLINE_CURVE_WITH_KNOTS('',3,(#58040,#58041,#58042,#58043,#58044,
#58045,#58046,#58047,#58048,#58049,#58050,#58051,#58052,#58053,#58054,#58055,
#58056,#58057,#58058,#58059,#58060,#58061,#58062,#58063,#58064),
 .UNSPECIFIED.,.F.,.F.,(4,3,3,3,3,3,3,3,4),(51.3827828658049,51.626126143236,
52.6189362613751,53.6117463795143,54.6045564976534,55.5973666157926,56.5901767339317,
57.5829868520709,57.6659681729845),.UNSPECIFIED.);
#1388=B_SPLINE_CURVE_WITH_KNOTS('',3,(#58069,#58070,#58071,#58072,#58073,
#58074,#58075,#58076,#58077,#58078,#58079,#58080,#58081,#58082,#58083,#58084,
#58085,#58086,#58087,#58088,#58089,#58090),.UNSPECIFIED.,.F.,.F.,(4,3,3,
3,3,3,3,4),(-66.9247834919266,-66.5182779153233,-65.5254677971841,-64.5326576790449,
-63.5398475609058,-62.5470374427666,-61.5542273246275,-60.641598184747),
 .UNSPECIFIED.);
#1389=B_SPLINE_CURVE_WITH_KNOTS('',3,(#58091,#58092,#58093,#58094,#58095,
#58096,#58097,#58098,#58099,#58100,#58101,#58102,#58103,#58104,#58105,#58106,
#58107,#58108,#58109,#58110,#58111,#58112),.UNSPECIFIED.,.F.,.F.,(4,3,3,
3,3,3,3,4),(57.6659681729845,58.57579697021,59.5686070883492,60.5614172064883,
61.5542273246275,62.5470374427666,63.5398475609058,63.949153480164),
 .UNSPECIFIED.);
#1390=B_SPLINE_CURVE_WITH_KNOTS('',3,(#58117,#58118,#58119,#58120,#58121,
#58122,#58123,#58124,#58125,#58126,#58127,#58128,#58129,#58130,#58131,#58132,
#58133,#58134,#58135,#58136,#58137,#58138),.UNSPECIFIED.,.F.,.F.,(4,3,3,
3,3,3,3,4),(-73.2079687991062,-72.4751386241581,-71.482328506019,-70.4895183878799,
-69.4967082697407,-68.5038981516016,-67.5110880334624,-66.9247834919266),
 .UNSPECIFIED.);
#1391=B_SPLINE_CURVE_WITH_KNOTS('',3,(#58139,#58140,#58141,#58142,#58143,
#58144,#58145,#58146,#58147,#58148,#58149,#58150,#58151,#58152,#58153,#58154,
#58155,#58156,#58157,#58158,#58159,#58160),.UNSPECIFIED.,.F.,.F.,(4,3,3,
3,3,3,3,4),(63.949153480164,64.5326576790449,65.5254677971841,66.5182779153232,
67.5110880334624,68.5038981516015,69.4967082697407,70.2323387873436),
 .UNSPECIFIED.);
#1392=B_SPLINE_CURVE_WITH_KNOTS('',3,(#58165,#58166,#58167,#58168,#58169,
#58170,#58171,#58172,#58173,#58174,#58175,#58176,#58177,#58178,#58179,#58180,
#58181,#58182,#58183,#58184,#58185,#58186,#58187,#58188,#58189),
 .UNSPECIFIED.,.F.,.F.,(4,3,3,3,3,3,3,3,4),(-79.4911541062858,-79.4248094511322,
-78.4319993329931,-77.4391892148539,-76.4463790967148,-75.4535689785756,
-74.4607588604365,-73.4679487422973,-73.2079687991062),.UNSPECIFIED.);
#1393=B_SPLINE_CURVE_WITH_KNOTS('',3,(#58190,#58191,#58192,#58193,#58194,
#58195,#58196,#58197,#58198,#58199,#58200,#58201,#58202,#58203,#58204,#58205,
#58206,#58207,#58208,#58209,#58210,#58211,#58212,#58213,#58214),
 .UNSPECIFIED.,.F.,.F.,(4,3,3,3,3,3,3,3,4),(70.2323387873436,70.4895183878799,
71.482328506019,72.4751386241582,73.4679487422973,74.4607588604365,75.4535689785756,
76.4463790967148,76.5155240945232),.UNSPECIFIED.);
#1394=B_SPLINE_CURVE_WITH_KNOTS('',3,(#58219,#58220,#58221,#58222,#58223,
#58224,#58225,#58226,#58227,#58228,#58229,#58230,#58231,#58232,#58233,#58234,
#58235,#58236,#58237,#58238,#58239,#58240),.UNSPECIFIED.,.F.,.F.,(4,3,3,
3,3,3,3,4),(-85.7743394134654,-85.3816701599672,-84.388860041828,-83.3960499236888,
-82.4032398055497,-81.4104296874105,-80.4176195692714,-79.4911541062858),
 .UNSPECIFIED.);
#1395=B_SPLINE_CURVE_WITH_KNOTS('',3,(#58241,#58242,#58243,#58244,#58245,
#58246,#58247,#58248,#58249,#58250,#58251,#58252,#58253,#58254,#58255,#58256,
#58257,#58258,#58259,#58260,#58261,#58262),.UNSPECIFIED.,.F.,.F.,(4,3,3,
3,3,3,3,4),(76.5155240945232,77.4391892148539,78.4319993329931,79.4248094511322,
80.4176195692714,81.4104296874105,82.4032398055497,82.7987094017028),
 .UNSPECIFIED.);
#1396=B_SPLINE_CURVE_WITH_KNOTS('',3,(#58267,#58268,#58269,#58270,#58271,
#58272,#58273,#58274,#58275,#58276,#58277,#58278,#58279,#58280,#58281,#58282,
#58283,#58284,#58285,#58286,#58287,#58288),.UNSPECIFIED.,.F.,.F.,(4,3,3,
3,3,3,3,4),(-92.0575247206449,-91.3385308688021,-90.3457207506629,-89.3529106325238,
-88.3601005143846,-87.3672903962455,-86.3744802781063,-85.7743394134654),
 .UNSPECIFIED.);
#1397=B_SPLINE_CURVE_WITH_KNOTS('',3,(#58289,#58290,#58291,#58292,#58293,
#58294,#58295,#58296,#58297,#58298,#58299,#58300,#58301,#58302,#58303,#58304,
#58305,#58306,#58307,#58308,#58309,#58310),.UNSPECIFIED.,.F.,.F.,(4,3,3,
3,3,3,3,4),(82.7987094017028,83.3960499236888,84.388860041828,85.3816701599672,
86.3744802781063,87.3672903962455,88.3601005143846,89.0818947088824),
 .UNSPECIFIED.);
#1398=B_SPLINE_CURVE_WITH_KNOTS('',3,(#58315,#58316,#58317,#58318,#58319,
#58320,#58321,#58322,#58323,#58324,#58325,#58326,#58327,#58328,#58329,#58330,
#58331,#58332,#58333,#58334,#58335,#58336,#58337,#58338,#58339),
 .UNSPECIFIED.,.F.,.F.,(4,3,3,3,3,3,3,3,4),(-98.3407100278245,-98.2882016957761,
-97.295391577637,-96.3025814594978,-95.3097713413587,-94.3169612232195,
-93.3241511050804,-92.3313409869412,-92.0575247206449),.UNSPECIFIED.);
#1399=B_SPLINE_CURVE_WITH_KNOTS('',3,(#58340,#58341,#58342,#58343,#58344,
#58345,#58346,#58347,#58348,#58349,#58350,#58351,#58352,#58353,#58354,#58355,
#58356,#58357,#58358,#58359,#58360,#58361,#58362,#58363,#58364),
 .UNSPECIFIED.,.F.,.F.,(4,3,3,3,3,3,3,3,4),(89.0818947088824,89.3529106325238,
90.3457207506629,91.3385308688021,92.3313409869412,93.3241511050804,94.3169612232195,
95.3097713413587,95.365080016062),.UNSPECIFIED.);
#1400=B_SPLINE_CURVE_WITH_KNOTS('',3,(#58369,#58370,#58371,#58372,#58373,
#58374,#58375,#58376,#58377,#58378,#58379,#58380,#58381,#58382,#58383,#58384,
#58385,#58386,#58387,#58388,#58389,#58390),.UNSPECIFIED.,.F.,.F.,(4,3,3,
3,3,3,3,4),(-104.623895335004,-104.245062404611,-103.252252286472,-102.259442168333,
-101.266632050194,-100.273821932054,-99.2810118139153,-98.3407100278245),
 .UNSPECIFIED.);
#1401=B_SPLINE_CURVE_WITH_KNOTS('',3,(#58391,#58392,#58393,#58394,#58395,
#58396,#58397,#58398,#58399,#58400,#58401,#58402,#58403,#58404,#58405,#58406,
#58407,#58408,#58409,#58410,#58411,#58412),.UNSPECIFIED.,.F.,.F.,(4,3,3,
3,3,3,3,4),(95.365080016062,96.3025814594978,97.295391577637,98.2882016957761,
99.2810118139153,100.273821932054,101.266632050194,101.648265323242),
 .UNSPECIFIED.);
#1402=B_SPLINE_CURVE_WITH_KNOTS('',3,(#58417,#58418,#58419,#58420,#58421,
#58422,#58423,#58424,#58425,#58426,#58427,#58428,#58429,#58430,#58431,#58432,
#58433,#58434,#58435,#58436,#58437,#58438),.UNSPECIFIED.,.F.,.F.,(4,3,3,
3,3,3,3,4),(-110.907080642184,-110.201923113446,-109.209112995307,-108.216302877168,
-107.223492759029,-106.230682640889,-105.23787252275,-104.623895335004),
 .UNSPECIFIED.);
#1403=B_SPLINE_CURVE_WITH_KNOTS('',3,(#58439,#58440,#58441,#58442,#58443,
#58444,#58445,#58446,#58447,#58448,#58449,#58450,#58451,#58452,#58453,#58454,
#58455,#58456,#58457,#58458,#58459,#58460),.UNSPECIFIED.,.F.,.F.,(4,3,3,
3,3,3,3,4),(101.648265323242,102.259442168333,103.252252286472,104.245062404611,
105.23787252275,106.230682640889,107.223492759029,107.931450630421),
 .UNSPECIFIED.);
#1404=B_SPLINE_CURVE_WITH_KNOTS('',3,(#58466,#58467,#58468,#58469,#58470,
#58471),.UNSPECIFIED.,.F.,.F.,(4,1,1,4),(122.522113490002,122.809766079403,
123.802576197542,124.712368377051),.UNSPECIFIED.);
#1405=B_SPLINE_CURVE_WITH_KNOTS('',3,(#58474,#58475,#58476,#58477),
 .UNSPECIFIED.,.F.,.F.,(4,4),(122.522113490002,123.473451256543),
 .UNSPECIFIED.);
#1406=B_SPLINE_CURVE_WITH_KNOTS('',3,(#58482,#58483,#58484,#58485,#58486,
#58487,#58488,#58489,#58490,#58491),.UNSPECIFIED.,.F.,.F.,(4,1,1,1,1,1,
1,4),(116.238928182822,116.852905370568,117.845715488708,118.838525606847,
119.831335724986,120.824145843125,121.816955961264,122.522113490002),
 .UNSPECIFIED.);
#1407=B_SPLINE_CURVE_WITH_KNOTS('',3,(#58492,#58493,#58494,#58495,#58496,
#58497,#58498,#58499,#58500,#58501,#58502),.UNSPECIFIED.,.F.,.F.,(4,1,1,
1,1,1,1,1,4),(116.238928182822,116.523780429569,117.516590547708,118.509400665847,
119.502210783986,120.495020902125,121.487831020264,122.480641138404,122.522113490002),
 .UNSPECIFIED.);
#1408=B_SPLINE_CURVE_WITH_KNOTS('',3,(#58507,#58508,#58509,#58510,#58511,
#58512,#58513,#58514,#58515,#58516),.UNSPECIFIED.,.F.,.F.,(4,1,1,1,1,1,
1,4),(109.955742875643,110.896044661733,111.888854779873,112.881664898012,
113.874475016151,114.86728513429,115.860095252429,116.238928182822),
 .UNSPECIFIED.);
#1409=B_SPLINE_CURVE_WITH_KNOTS('',3,(#58517,#58518,#58519,#58520,#58521,
#58522,#58523,#58524,#58525,#58526),.UNSPECIFIED.,.F.,.F.,(4,1,1,1,1,1,
1,4),(109.955742875643,110.566919720734,111.559729838873,112.552539957012,
113.545350075151,114.53816019329,115.530970311429,116.238928182822),
 .UNSPECIFIED.);
#1410=B_SPLINE_CURVE_WITH_KNOTS('',3,(#58531,#58532,#58533,#58534,#58535,
#58536,#58537,#58538,#58539,#58540,#58541),.UNSPECIFIED.,.F.,.F.,(4,1,1,
1,1,1,1,1,4),(103.672557568463,103.946373834759,104.939183952899,105.931994071038,
106.924804189177,107.917614307316,108.910424425455,109.903234543594,109.955742875643),
 .UNSPECIFIED.);
#1411=B_SPLINE_CURVE_WITH_KNOTS('',3,(#58542,#58543,#58544,#58545,#58546,
#58547,#58548,#58549,#58550,#58551),.UNSPECIFIED.,.F.,.F.,(4,1,1,1,1,1,
1,4),(103.672557568463,104.610059011899,105.602869130038,106.595679248177,
107.588489366316,108.581299484455,109.574109602595,109.955742875643),
 .UNSPECIFIED.);
#1412=B_SPLINE_CURVE_WITH_KNOTS('',3,(#58556,#58557,#58558,#58559,#58560,
#58561,#58562,#58563,#58564,#58565),.UNSPECIFIED.,.F.,.F.,(4,1,1,1,1,1,
1,4),(97.3893722612836,97.9895131259245,98.9823232440636,99.9751333622028,
100.967943480342,101.960753598481,102.95356371662,103.672557568463),
 .UNSPECIFIED.);
#1413=B_SPLINE_CURVE_WITH_KNOTS('',3,(#58566,#58567,#58568,#58569,#58570,
#58571,#58572,#58573,#58574,#58575,#58576),.UNSPECIFIED.,.F.,.F.,(4,1,1,
1,1,1,1,1,4),(97.3893722612835,97.6603881849247,98.6531983030639,99.646008421203,
100.638818539342,101.631628657481,102.624438775621,103.61724889376,103.672557568463),
 .UNSPECIFIED.);
#1414=B_SPLINE_CURVE_WITH_KNOTS('',3,(#58581,#58582,#58583,#58584,#58585,
#58586,#58587,#58588,#58589,#58590),.UNSPECIFIED.,.F.,.F.,(4,1,1,1,1,1,
1,4),(91.106186954104,92.0326524170896,93.0254625352287,94.0182726533679,
95.011082771507,96.0038928896462,96.9967030077853,97.3893722612836),
 .UNSPECIFIED.);
#1415=B_SPLINE_CURVE_WITH_KNOTS('',3,(#58591,#58592,#58593,#58594,#58595,
#58596,#58597,#58598,#58599,#58600),.UNSPECIFIED.,.F.,.F.,(4,1,1,1,1,1,
1,4),(91.106186954104,91.7035274760898,92.696337594229,93.6891477123681,
94.6819578305073,95.6747679486464,96.6675780667856,97.3893722612835),
 .UNSPECIFIED.);
#1416=B_SPLINE_CURVE_WITH_KNOTS('',3,(#58605,#58606,#58607,#58608,#58609,
#58610,#58611,#58612,#58613,#58614,#58615),.UNSPECIFIED.,.F.,.F.,(4,1,1,
1,1,1,1,1,4),(84.8230016469244,85.0829815901155,86.0757917082546,87.0686018263938,
88.0614119445329,89.0542220626721,90.0470321808113,91.0398422989504,91.106186954104),
 .UNSPECIFIED.);
#1417=B_SPLINE_CURVE_WITH_KNOTS('',3,(#58616,#58617,#58618,#58619,#58620,
#58621,#58622,#58623,#58624,#58625),.UNSPECIFIED.,.F.,.F.,(4,1,1,1,1,1,
1,4),(84.8230016469244,85.7466667672549,86.7394768853941,87.7322870035332,
88.7250971216724,89.7179072398115,90.7107173579507,91.106186954104),
 .UNSPECIFIED.);
#1418=B_SPLINE_CURVE_WITH_KNOTS('',3,(#58630,#58631,#58632,#58633,#58634,
#58635,#58636,#58637,#58638,#58639),.UNSPECIFIED.,.F.,.F.,(4,1,1,1,1,1,
1,4),(78.5398163397448,79.1261208812806,80.1189309994197,81.1117411175589,
82.104551235698,83.0973613538372,84.0901714719763,84.8230016469244),
 .UNSPECIFIED.);
#1419=B_SPLINE_CURVE_WITH_KNOTS('',3,(#58640,#58641,#58642,#58643,#58644,
#58645,#58646,#58647,#58648,#58649,#58650),.UNSPECIFIED.,.F.,.F.,(4,1,1,
1,1,1,1,1,4),(78.5398163397448,78.7969959402808,79.78980605842,80.7826161765591,
81.7754262946983,82.7682364128375,83.7610465309766,84.7538566491157,84.8230016469244),
 .UNSPECIFIED.);
#1420=B_SPLINE_CURVE_WITH_KNOTS('',3,(#58655,#58656,#58657,#58658,#58659,
#58660,#58661,#58662,#58663,#58664),.UNSPECIFIED.,.F.,.F.,(4,1,1,1,1,1,
1,4),(72.2566310325652,73.1692601724456,74.1620702905848,75.154880408724,
76.1476905268631,77.1405006450023,78.1333107631414,78.5398163397448),
 .UNSPECIFIED.);
#1421=B_SPLINE_CURVE_WITH_KNOTS('',3,(#58665,#58666,#58667,#58668,#58669,
#58670,#58671,#58672,#58673,#58674),.UNSPECIFIED.,.F.,.F.,(4,1,1,1,1,1,
1,4),(72.2566310325652,72.8401352314459,73.8329453495851,74.8257554677242,
75.8185655858634,76.8113757040025,77.8041858221417,78.5398163397448),
 .UNSPECIFIED.);
#1422=B_SPLINE_CURVE_WITH_KNOTS('',3,(#58679,#58680,#58681,#58682,#58683,
#58684,#58685,#58686,#58687,#58688,#58689),.UNSPECIFIED.,.F.,.F.,(4,1,1,
1,1,1,1,1,4),(65.9734457253856,66.2195893454716,67.2123994636107,68.2052095817499,
69.198019699889,70.1908298180282,71.1836399361674,72.1764500543065,72.2566310325652),
 .UNSPECIFIED.);
#1423=B_SPLINE_CURVE_WITH_KNOTS('',3,(#58690,#58691,#58692,#58693,#58694,
#58695,#58696,#58697,#58698,#58699),.UNSPECIFIED.,.F.,.F.,(4,1,1,1,1,1,
1,4),(65.9734457253856,66.883274522611,67.8760846407502,68.8688947588893,
69.8617048770285,70.8545149951676,71.8473251133068,72.2566310325652),
 .UNSPECIFIED.);
#1424=B_SPLINE_CURVE_WITH_KNOTS('',3,(#58704,#58705,#58706,#58707,#58708,
#58709,#58710,#58711,#58712,#58713),.UNSPECIFIED.,.F.,.F.,(4,1,1,1,1,1,
1,4),(59.690260418206,60.2627286366367,61.2555387547758,62.248348872915,
63.2411589910541,64.2339691091933,65.2267792273324,65.9734457253856),
 .UNSPECIFIED.);
#1425=B_SPLINE_CURVE_WITH_KNOTS('',3,(#58714,#58715,#58716,#58717,#58718,
#58719,#58720,#58721,#58722,#58723,#58724),.UNSPECIFIED.,.F.,.F.,(4,1,1,
1,1,1,1,1,4),(59.690260418206,59.9336036956369,60.9264138137761,61.9192239319152,
62.9120340500544,63.9048441681935,64.8976542863327,65.8904644044719,65.9734457253856),
 .UNSPECIFIED.);
#1426=B_SPLINE_CURVE_WITH_KNOTS('',3,(#58729,#58730,#58731,#58732,#58733,
#58734,#58735,#58736,#58737,#58738),.UNSPECIFIED.,.F.,.F.,(4,1,1,1,1,1,
1,4),(53.4070751110264,54.3058679278017,55.2986780459409,56.2914881640801,
57.2842982822192,58.2771084003584,59.2699185184975,59.690260418206),
 .UNSPECIFIED.);
#1427=B_SPLINE_CURVE_WITH_KNOTS('',3,(#58739,#58740,#58741,#58742,#58743,
#58744,#58745,#58746,#58747,#58748),.UNSPECIFIED.,.F.,.F.,(4,1,1,1,1,1,
1,4),(53.4070751110264,53.976742986802,54.9695531049412,55.9623632230803,
56.9551733412195,57.9479834593586,58.9407935774978,59.690260418206),
 .UNSPECIFIED.);
#1428=B_SPLINE_CURVE_WITH_KNOTS('',3,(#58753,#58754,#58755,#58756,#58757,
#58758,#58759,#58760,#58761,#58762,#58763),.UNSPECIFIED.,.F.,.F.,(4,1,1,
1,1,1,1,1,4),(47.1238898038468,47.3561971008277,48.3490072189668,49.341817337106,
50.3346274552451,51.3274375733843,52.3202476915234,53.3130578096626,53.4070751110264),
 .UNSPECIFIED.);
#1429=B_SPLINE_CURVE_WITH_KNOTS('',3,(#58764,#58765,#58766,#58767,#58768,
#58769,#58770,#58771,#58772,#58773),.UNSPECIFIED.,.F.,.F.,(4,1,1,1,1,1,
1,4),(47.1238898038468,48.0198822779671,49.0126923961063,50.0055025142454,
50.9983126323846,51.9911227505237,52.9839328686629,53.4070751110264),
 .UNSPECIFIED.);
#1430=B_SPLINE_CURVE_WITH_KNOTS('',3,(#58778,#58779,#58780,#58781,#58782,
#58783,#58784,#58785,#58786,#58787),.UNSPECIFIED.,.F.,.F.,(4,1,1,1,1,1,
1,4),(40.8407044966672,41.3993363919928,42.3921465101319,43.3849566282711,
44.3777667464102,45.3705768645494,46.3633869826885,47.1238898038468),
 .UNSPECIFIED.);
#1431=B_SPLINE_CURVE_WITH_KNOTS('',3,(#58788,#58789,#58790,#58791,#58792,
#58793,#58794,#58795,#58796,#58797,#58798),.UNSPECIFIED.,.F.,.F.,(4,1,1,
1,1,1,1,1,4),(40.8407044966672,41.070211450993,42.0630215691322,43.0558316872713,
44.0486418054105,45.0414519235496,46.0342620416888,47.0270721598279,47.1238898038468),
 .UNSPECIFIED.);
#1432=B_SPLINE_CURVE_WITH_KNOTS('',3,(#58803,#58804,#58805,#58806,#58807,
#58808,#58809,#58810,#58811,#58812),.UNSPECIFIED.,.F.,.F.,(4,1,1,1,1,1,
1,4),(34.5575191894876,35.4424756831578,36.435285801297,37.4280959194362,
38.4209060375753,39.4137161557145,40.4065262738536,40.8407044966672),
 .UNSPECIFIED.);
#1433=B_SPLINE_CURVE_WITH_KNOTS('',3,(#58813,#58814,#58815,#58816,#58817,
#58818,#58819,#58820,#58821,#58822),.UNSPECIFIED.,.F.,.F.,(4,1,1,1,1,1,
1,4),(34.5575191894876,35.1133507421581,36.1061608602973,37.0989709784364,
38.0917810965756,39.0845912147147,40.0774013328539,40.8407044966672),
 .UNSPECIFIED.);
#1434=B_SPLINE_CURVE_WITH_KNOTS('',3,(#58827,#58828,#58829,#58830,#58831,
#58832,#58833,#58834,#58835,#58836,#58837),.UNSPECIFIED.,.F.,.F.,(4,1,1,
1,1,1,1,1,4),(28.2743338823081,28.4928048561838,29.4856149743229,30.4784250924621,
31.4712352106012,32.4640453287404,33.4568554468795,34.4496655650187,34.5575191894876),
 .UNSPECIFIED.);
#1435=B_SPLINE_CURVE_WITH_KNOTS('',3,(#58838,#58839,#58840,#58841,#58842,
#58843,#58844,#58845,#58846,#58847),.UNSPECIFIED.,.F.,.F.,(4,1,1,1,1,1,
1,4),(28.274333882308,29.1564900333232,30.1493001514623,31.1421102696015,
32.1349203877406,33.1277305058798,34.120540624019,34.5575191894876),
 .UNSPECIFIED.);
#1436=B_SPLINE_CURVE_WITH_KNOTS('',3,(#58852,#58853,#58854,#58855,#58856,
#58857,#58858,#58859,#58860,#58861),.UNSPECIFIED.,.F.,.F.,(4,1,1,1,1,1,
1,4),(21.9911485751285,22.5359441473489,23.528754265488,24.5215643836272,
25.5143745017663,26.5071846199055,27.4999947380446,28.2743338823081),
 .UNSPECIFIED.);
#1437=B_SPLINE_CURVE_WITH_KNOTS('',3,(#58862,#58863,#58864,#58865,#58866,
#58867,#58868,#58869,#58870,#58871,#58872),.UNSPECIFIED.,.F.,.F.,(4,1,1,
1,1,1,1,1,4),(21.9911485751284,22.2068192063491,23.1996293244883,24.1924394426274,
25.1852495607666,26.1780596789057,27.1708697970449,28.163679915184,28.274333882308),
 .UNSPECIFIED.);
#1438=B_SPLINE_CURVE_WITH_KNOTS('',3,(#58877,#58878,#58879,#58880,#58881,
#58882,#58883,#58884,#58885,#58886),.UNSPECIFIED.,.F.,.F.,(4,1,1,1,1,1,
1,4),(15.7079632679489,16.5790834385139,17.5718935566531,18.5647036747922,
19.5575137929314,20.5503239110706,21.5431340292097,21.9911485751285),
 .UNSPECIFIED.);
#1439=B_SPLINE_CURVE_WITH_KNOTS('',3,(#58887,#58888,#58889,#58890,#58891,
#58892,#58893,#58894,#58895,#58896),.UNSPECIFIED.,.F.,.F.,(4,1,1,1,1,1,
1,4),(15.7079632679489,16.2499584975142,17.2427686156534,18.2355787337925,
19.2283888519317,20.2211989700708,21.21400908821,21.9911485751284),
 .UNSPECIFIED.);
#1440=B_SPLINE_CURVE_WITH_KNOTS('',3,(#59411,#59412,#59413,#59414,#59415,
#59416,#59417,#59418,#59419,#59420,#59421,#59422,#59423,#59424,#59425,#59426,
#59427,#59428,#59429,#59430,#59431,#59432,#59433,#59434,#59435,#59436,#59437,
#59438,#59439,#59440,#59441,#59442,#59443,#59444,#59445,#59446,#59447,#59448,
#59449,#59450,#59451,#59452,#59453,#59454,#59455,#59456,#59457,#59458,#59459,
#59460,#59461,#59462,#59463,#59464,#59465,#59466,#59467,#59468,#59469,#59470,
#59471,#59472,#59473,#59474,#59475,#59476,#59477,#59478,#59479,#59480,#59481,
#59482,#59483,#59484,#59485,#59486,#59487,#59488,#59489,#59490,#59491,#59492,
#59493,#59494,#59495,#59496,#59497,#59498,#59499,#59500,#59501),
 .UNSPECIFIED.,.F.,.F.,(4,3,3,3,3,3,3,3,3,3,3,3,3,3,3,3,3,3,3,3,3,3,3,3,
3,3,3,3,3,3,4),(0.,0.0244828275480345,0.053633229323616,0.0831948315675068,
0.110714477628582,0.11526672716195,0.144013775177923,0.172670364792843,
0.200834260795346,0.213648978202941,0.219194492985043,0.223573650231945,
0.251155465393894,0.277944800071433,0.303352000056106,0.319097049327563,
0.323930180875061,0.328014801185161,0.354666699599173,0.38176869329296,
0.408582656634786,0.419018395384968,0.42428937677764,0.428315007817544,
0.454631255061835,0.479791638396231,0.488289756370224,0.494557171122132,
0.519833104861304,0.544394958619519,0.555272788399418),.UNSPECIFIED.);
#1441=B_SPLINE_CURVE_WITH_KNOTS('',3,(#59502,#59503,#59504,#59505,#59506,
#59507,#59508,#59509,#59510,#59511,#59512,#59513,#59514,#59515,#59516,#59517,
#59518,#59519,#59520),.UNSPECIFIED.,.F.,.F.,(4,3,3,3,3,3,4),(107.931450630421,
108.216302877168,109.209112995307,110.201923113446,111.194733231585,112.187543349724,
113.097335529233),.UNSPECIFIED.);
#1442=B_SPLINE_CURVE_WITH_KNOTS('',3,(#59522,#59523,#59524,#59525,#59526,
#59527,#59528,#59529,#59530,#59531,#59532,#59533,#59534,#59535,#59536,#59537,
#59538,#59539,#59540,#59541,#59542,#59543,#59544,#59545,#59546,#59547,#59548,
#59549,#59550,#59551,#59552,#59553,#59554,#59555,#59556,#59557,#59558,#59559,
#59560,#59561,#59562,#59563,#59564,#59565,#59566,#59567,#59568,#59569,#59570,
#59571,#59572,#59573,#59574,#59575,#59576,#59577,#59578,#59579,#59580,#59581,
#59582,#59583,#59584,#59585,#59586,#59587,#59588,#59589,#59590,#59591,#59592,
#59593,#59594,#59595,#59596,#59597,#59598,#59599,#59600,#59601,#59602,#59603,
#59604,#59605,#59606,#59607,#59608,#59609,#59610,#59611,#59612),
 .UNSPECIFIED.,.F.,.F.,(4,3,3,3,3,3,3,3,3,3,3,3,3,3,3,3,3,3,3,3,3,3,3,3,
3,3,3,3,3,3,4),(0.,0.0199484555424935,0.0444472219322248,0.0695704352965358,
0.0823017670372087,0.0889067669075885,0.0939032261859449,0.0978868073317507,
0.123848521149104,0.150333670415753,0.177012130518808,0.190045367541077,
0.195034003771074,0.222448330986507,0.249798458203261,0.273271743147302,
0.290738845349037,0.295003687011922,0.321757479861748,0.350630967175911,
0.377214736980723,0.389091550177083,0.398269541876197,0.403901739635534,
0.432677759684221,0.462694664356929,0.472448461766916,0.479349706952298,
0.508919877152419,0.538123179131352,0.552745378375053),.UNSPECIFIED.);
#1443=B_SPLINE_CURVE_WITH_KNOTS('',3,(#59613,#59614,#59615,#59616,#59617,
#59618,#59619,#59620,#59621),.UNSPECIFIED.,.F.,.F.,(4,1,1,1,1,1,4),(10.3761157273101,
11.2859079068184,12.2787180249576,13.2715281430967,14.2643382612359,15.2571483793751,
15.7079632679489),.UNSPECIFIED.);
#1444=B_SPLINE_CURVE_WITH_KNOTS('',3,(#59625,#59626,#59627,#59628,#59629,
#59630,#59631,#59632),.UNSPECIFIED.,.F.,.F.,(4,1,1,1,1,4),(11.6150328478182,
12.6078429659573,13.6006530840965,14.5934632022356,15.5862733203748,15.7079632679489),
 .UNSPECIFIED.);
#1445=B_SPLINE_CURVE_WITH_KNOTS('',3,(#60110,#60111,#60112,#60113,#60114,
#60115,#60116,#60117,#60118,#60119,#60120,#60121,#60122,#60123,#60124,#60125,
#60126,#60127,#60128,#60129,#60130,#60131,#60132,#60133,#60134,#60135,#60136,
#60137,#60138,#60139,#60140,#60141,#60142,#60143,#60144,#60145,#60146,#60147,
#60148,#60149,#60150,#60151,#60152,#60153,#60154,#60155,#60156,#60157,#60158,
#60159,#60160,#60161,#60162,#60163,#60164,#60165,#60166,#60167,#60168,#60169,
#60170,#60171,#60172,#60173,#60174,#60175,#60176,#60177,#60178,#60179,#60180,
#60181,#60182,#60183,#60184,#60185,#60186,#60187,#60188,#60189,#60190,#60191,
#60192,#60193,#60194,#60195,#60196,#60197,#60198,#60199,#60200),
 .UNSPECIFIED.,.F.,.F.,(4,3,3,3,3,3,3,3,3,3,3,3,3,3,3,3,3,3,3,3,3,3,3,3,
3,3,3,3,3,3,4),(0.,0.0199484555424956,0.0444472057453558,0.06957040842524,
0.082301741845369,0.0889067201937656,0.0939032092701117,0.0978868025698804,
0.123848506283839,0.150333651753478,0.177012112338214,0.190045334010802,
0.195033995567435,0.222448321497137,0.249798448556615,0.273271743147304,
0.290738845349038,0.295003687474005,0.321757477096169,0.35063096475603,
0.377214805322132,0.389091676062608,0.398269949867563,0.403901905426966,
0.432677921570632,0.462694785771738,0.472448780080044,0.479349722651653,
0.508919892898584,0.538123208459607,0.552745378375058),.UNSPECIFIED.);
#1446=B_SPLINE_CURVE_WITH_KNOTS('',3,(#60201,#60202,#60203,#60204,#60205,
#60206,#60207,#60208,#60209,#60210,#60211,#60212,#60213,#60214,#60215,#60216,
#60217,#60218,#60219,#60220,#60221,#60222,#60223,#60224,#60225,#60226,#60227,
#60228,#60229,#60230,#60231,#60232,#60233,#60234,#60235,#60236,#60237,#60238,
#60239,#60240,#60241,#60242,#60243,#60244,#60245,#60246,#60247,#60248,#60249,
#60250,#60251,#60252,#60253,#60254,#60255,#60256,#60257,#60258,#60259,#60260,
#60261,#60262,#60263,#60264,#60265,#60266,#60267,#60268,#60269,#60270,#60271,
#60272,#60273,#60274,#60275,#60276,#60277,#60278,#60279,#60280,#60281,#60282,
#60283,#60284,#60285,#60286,#60287,#60288,#60289,#60290,#60291),
 .UNSPECIFIED.,.F.,.F.,(4,3,3,3,3,3,3,3,3,3,3,3,3,3,3,3,3,3,3,3,3,3,3,3,
3,3,3,3,3,3,4),(0.,0.0244828275480203,0.0536332274622602,0.0831948298811238,
0.110714476152993,0.115266725820044,0.144013773894134,0.172670359523596,
0.20083424455867,0.213648963995846,0.219194447131387,0.223573639079567,
0.251155446612606,0.277944764436798,0.303352000056074,0.31909704932753,
0.323930181275963,0.328014801994789,0.354666688633115,0.381768683952949,
0.408582659874698,0.419018397971995,0.424289394077547,0.428315034389049,
0.454631289457757,0.479791664193159,0.488289819943521,0.494557177833865,
0.519833128909889,0.544395005481118,0.555272788399364),.UNSPECIFIED.);
#1447=B_SPLINE_CURVE_WITH_KNOTS('',3,(#60292,#60293,#60294,#60295,#60296,
#60297,#60298,#60299,#60300,#60301,#60302,#60303,#60304,#60305,#60306,#60307),
 .UNSPECIFIED.,.F.,.F.,(4,3,3,3,3,4),(-115.165973704142,-114.173163586003,
-113.180353467863,-112.187543349724,-111.194733231585,-110.907080642184),
 .UNSPECIFIED.);
#1566=SHAPE_REPRESENTATION_RELATIONSHIP('SRR','None',#64005,#1584);
#1584=ADVANCED_BREP_SHAPE_REPRESENTATION('',(#1620),#63890);
#1602=STYLED_ITEM('',(#64100),#1620);
#1620=MANIFOLD_SOLID_BREP('Body1',#15488);
#1691=FACE_BOUND('',#4291,.T.);
#2287=CYLINDRICAL_SURFACE('',#16532,2.942);
#2288=CYLINDRICAL_SURFACE('',#16534,2.942);
#2289=CYLINDRICAL_SURFACE('',#16535,2.942);
#2290=CYLINDRICAL_SURFACE('',#16536,2.942);
#2291=CYLINDRICAL_SURFACE('',#16537,2.942);
#2292=CYLINDRICAL_SURFACE('',#16538,2.942);
#2293=CYLINDRICAL_SURFACE('',#16539,2.942);
#2294=CYLINDRICAL_SURFACE('',#16540,2.942);
#2295=CYLINDRICAL_SURFACE('',#16541,2.942);
#2296=CYLINDRICAL_SURFACE('',#16542,2.942);
#2297=CYLINDRICAL_SURFACE('',#16543,2.942);
#2298=CYLINDRICAL_SURFACE('',#16544,2.942);
#2299=CYLINDRICAL_SURFACE('',#16545,2.942);
#2300=CYLINDRICAL_SURFACE('',#16546,2.942);
#2301=CYLINDRICAL_SURFACE('',#16547,2.942);
#2302=CYLINDRICAL_SURFACE('',#16548,2.942);
#2303=CYLINDRICAL_SURFACE('',#16549,2.942);
#2304=CYLINDRICAL_SURFACE('',#16550,2.942);
#2305=CYLINDRICAL_SURFACE('',#16551,2.37175);
#2306=CYLINDRICAL_SURFACE('',#16553,2.37175);
#2307=CYLINDRICAL_SURFACE('',#16554,2.37175);
#2308=CYLINDRICAL_SURFACE('',#16555,2.37175);
#2309=CYLINDRICAL_SURFACE('',#16556,2.37175);
#2310=CYLINDRICAL_SURFACE('',#16557,2.37175);
#2311=CYLINDRICAL_SURFACE('',#16558,2.37175);
#2312=CYLINDRICAL_SURFACE('',#16559,2.37175);
#2313=CYLINDRICAL_SURFACE('',#16560,2.37175);
#2314=CYLINDRICAL_SURFACE('',#16561,2.37175);
#2315=CYLINDRICAL_SURFACE('',#16562,2.37175);
#2316=CYLINDRICAL_SURFACE('',#16563,2.37175);
#2317=CYLINDRICAL_SURFACE('',#16564,2.37175);
#2318=CYLINDRICAL_SURFACE('',#16565,2.37175);
#2319=CYLINDRICAL_SURFACE('',#16566,2.37175);
#2320=CYLINDRICAL_SURFACE('',#16567,2.37175);
#2321=CYLINDRICAL_SURFACE('',#16568,2.37175);
#2322=CYLINDRICAL_SURFACE('',#16569,2.37175);
#2323=CYLINDRICAL_SURFACE('',#16577,2.37175);
#2324=CYLINDRICAL_SURFACE('',#16581,2.942);
#2546=CIRCLE('',#16533,2.942);
#2547=CIRCLE('',#16552,2.37175);
#2548=CIRCLE('',#16578,2.37175);
#2549=CIRCLE('',#16580,2.942);
#3341=FACE_OUTER_BOUND('',#4242,.T.);
#3342=FACE_OUTER_BOUND('',#4243,.T.);
#3343=FACE_OUTER_BOUND('',#4244,.T.);
#3344=FACE_OUTER_BOUND('',#4245,.T.);
#3345=FACE_OUTER_BOUND('',#4246,.T.);
#3346=FACE_OUTER_BOUND('',#4247,.T.);
#3347=FACE_OUTER_BOUND('',#4248,.T.);
#3348=FACE_OUTER_BOUND('',#4249,.T.);
#3349=FACE_OUTER_BOUND('',#4250,.T.);
#3350=FACE_OUTER_BOUND('',#4251,.T.);
#3351=FACE_OUTER_BOUND('',#4252,.T.);
#3352=FACE_OUTER_BOUND('',#4253,.T.);
#3353=FACE_OUTER_BOUND('',#4254,.T.);
#3354=FACE_OUTER_BOUND('',#4255,.T.);
#3355=FACE_OUTER_BOUND('',#4256,.T.);
#3356=FACE_OUTER_BOUND('',#4257,.T.);
#3357=FACE_OUTER_BOUND('',#4258,.T.);
#3358=FACE_OUTER_BOUND('',#4259,.T.);
#3359=FACE_OUTER_BOUND('',#4260,.T.);
#3360=FACE_OUTER_BOUND('',#4261,.T.);
#3361=FACE_OUTER_BOUND('',#4262,.T.);
#3362=FACE_OUTER_BOUND('',#4263,.T.);
#3363=FACE_OUTER_BOUND('',#4264,.T.);
#3364=FACE_OUTER_BOUND('',#4265,.T.);
#3365=FACE_OUTER_BOUND('',#4266,.T.);
#3366=FACE_OUTER_BOUND('',#4267,.T.);
#3367=FACE_OUTER_BOUND('',#4268,.T.);
#3368=FACE_OUTER_BOUND('',#4269,.T.);
#3369=FACE_OUTER_BOUND('',#4270,.T.);
#3370=FACE_OUTER_BOUND('',#4271,.T.);
#3371=FACE_OUTER_BOUND('',#4272,.T.);
#3372=FACE_OUTER_BOUND('',#4273,.T.);
#3373=FACE_OUTER_BOUND('',#4274,.T.);
#3374=FACE_OUTER_BOUND('',#4275,.T.);
#3375=FACE_OUTER_BOUND('',#4276,.T.);
#3376=FACE_OUTER_BOUND('',#4277,.T.);
#3377=FACE_OUTER_BOUND('',#4278,.T.);
#3378=FACE_OUTER_BOUND('',#4279,.T.);
#3379=FACE_OUTER_BOUND('',#4280,.T.);
#3380=FACE_OUTER_BOUND('',#4281,.T.);
#3381=FACE_OUTER_BOUND('',#4282,.T.);
#3382=FACE_OUTER_BOUND('',#4283,.T.);
#3383=FACE_OUTER_BOUND('',#4284,.T.);
#3384=FACE_OUTER_BOUND('',#4285,.T.);
#3385=FACE_OUTER_BOUND('',#4286,.T.);
#3386=FACE_OUTER_BOUND('',#4287,.T.);
#3387=FACE_OUTER_BOUND('',#4288,.T.);
#3388=FACE_OUTER_BOUND('',#4289,.T.);
#3389=FACE_OUTER_BOUND('',#4290,.T.);
#4242=EDGE_LOOP('',(#13654,#13655,#13656,#13657));
#4243=EDGE_LOOP('',(#13658,#13659,#13660,#13661));
#4244=EDGE_LOOP('',(#13662,#13663,#13664,#13665));
#4245=EDGE_LOOP('',(#13666,#13667,#13668,#13669));
#4246=EDGE_LOOP('',(#13670,#13671,#13672,#13673));
#4247=EDGE_LOOP('',(#13674,#13675,#13676,#13677));
#4248=EDGE_LOOP('',(#13678,#13679,#13680,#13681));
#4249=EDGE_LOOP('',(#13682,#13683,#13684,#13685));
#4250=EDGE_LOOP('',(#13686,#13687,#13688,#13689));
#4251=EDGE_LOOP('',(#13690,#13691,#13692,#13693));
#4252=EDGE_LOOP('',(#13694,#13695,#13696,#13697));
#4253=EDGE_LOOP('',(#13698,#13699,#13700,#13701));
#4254=EDGE_LOOP('',(#13702,#13703,#13704,#13705));
#4255=EDGE_LOOP('',(#13706,#13707,#13708,#13709));
#4256=EDGE_LOOP('',(#13710,#13711,#13712,#13713));
#4257=EDGE_LOOP('',(#13714,#13715,#13716,#13717));
#4258=EDGE_LOOP('',(#13718,#13719,#13720,#13721));
#4259=EDGE_LOOP('',(#13722,#13723,#13724,#13725));
#4260=EDGE_LOOP('',(#13726,#13727,#13728,#13729));
#4261=EDGE_LOOP('',(#13730,#13731,#13732,#13733));
#4262=EDGE_LOOP('',(#13734,#13735,#13736,#13737));
#4263=EDGE_LOOP('',(#13738,#13739,#13740,#13741));
#4264=EDGE_LOOP('',(#13742,#13743,#13744,#13745));
#4265=EDGE_LOOP('',(#13746,#13747,#13748,#13749));
#4266=EDGE_LOOP('',(#13750,#13751,#13752,#13753));
#4267=EDGE_LOOP('',(#13754,#13755,#13756,#13757));
#4268=EDGE_LOOP('',(#13758,#13759,#13760,#13761));
#4269=EDGE_LOOP('',(#13762,#13763,#13764,#13765));
#4270=EDGE_LOOP('',(#13766,#13767,#13768,#13769));
#4271=EDGE_LOOP('',(#13770,#13771,#13772,#13773));
#4272=EDGE_LOOP('',(#13774,#13775,#13776,#13777));
#4273=EDGE_LOOP('',(#13778,#13779,#13780,#13781));
#4274=EDGE_LOOP('',(#13782,#13783,#13784,#13785));
#4275=EDGE_LOOP('',(#13786,#13787,#13788,#13789));
#4276=EDGE_LOOP('',(#13790,#13791,#13792,#13793));
#4277=EDGE_LOOP('',(#13794,#13795,#13796,#13797));
#4278=EDGE_LOOP('',(#13798,#13799,#13800,#13801));
#4279=EDGE_LOOP('',(#13802,#13803,#13804,#13805));
#4280=EDGE_LOOP('',(#13806,#13807,#13808,#13809));
#4281=EDGE_LOOP('',(#13810,#13811,#13812,#13813));
#4282=EDGE_LOOP('',(#13814,#13815,#13816,#13817));
#4283=EDGE_LOOP('',(#13818,#13819,#13820,#13821));
#4284=EDGE_LOOP('',(#13822,#13823,#13824,#13825,#13826,#13827));
#4285=EDGE_LOOP('',(#13828,#13829,#13830,#13831,#13832,#13833,#13834,#13835,
#13836,#13837,#13838,#13839,#13840,#13841,#13842,#13843,#13844,#13845,#13846,
#13847,#13848,#13849,#13850,#13851,#13852,#13853,#13854,#13855,#13856,#13857,
#13858,#13859,#13860,#13861,#13862,#13863,#13864,#13865,#13866,#13867));
#4286=EDGE_LOOP('',(#13868,#13869,#13870,#13871));
#4287=EDGE_LOOP('',(#13872,#13873,#13874,#13875,#13876,#13877,#13878,#13879,
#13880,#13881,#13882,#13883,#13884,#13885,#13886,#13887,#13888,#13889,#13890,
#13891,#13892,#13893,#13894,#13895,#13896,#13897,#13898,#13899,#13900,#13901,
#13902,#13903,#13904,#13905,#13906,#13907,#13908,#13909,#13910,#13911));
#4288=EDGE_LOOP('',(#13912,#13913,#13914,#13915));
#4289=EDGE_LOOP('',(#13916,#13917,#13918,#13919));
#4290=EDGE_LOOP('',(#13920,#13921,#13922,#13923));
#4291=EDGE_LOOP('',(#13924,#13925,#13926,#13927,#13928,#13929));
#5060=LINE('',#57594,#5823);
#5061=LINE('',#57618,#5824);
#5062=LINE('',#57666,#5825);
#5063=LINE('',#57714,#5826);
#5064=LINE('',#57768,#5827);
#5065=LINE('',#57816,#5828);
#5066=LINE('',#57864,#5829);
#5067=LINE('',#57918,#5830);
#5068=LINE('',#57966,#5831);
#5069=LINE('',#58014,#5832);
#5070=LINE('',#58068,#5833);
#5071=LINE('',#58116,#5834);
#5072=LINE('',#58164,#5835);
#5073=LINE('',#58218,#5836);
#5074=LINE('',#58266,#5837);
#5075=LINE('',#58314,#5838);
#5076=LINE('',#58368,#5839);
#5077=LINE('',#58416,#5840);
#5078=LINE('',#58464,#5841);
#5079=LINE('',#58481,#5842);
#5080=LINE('',#58506,#5843);
#5081=LINE('',#58530,#5844);
#5082=LINE('',#58555,#5845);
#5083=LINE('',#58580,#5846);
#5084=LINE('',#58604,#5847);
#5085=LINE('',#58629,#5848);
#5086=LINE('',#58654,#5849);
#5087=LINE('',#58678,#5850);
#5088=LINE('',#58703,#5851);
#5089=LINE('',#58728,#5852);
#5090=LINE('',#58752,#5853);
#5091=LINE('',#58777,#5854);
#5092=LINE('',#58802,#5855);
#5093=LINE('',#58826,#5856);
#5094=LINE('',#58851,#5857);
#5095=LINE('',#58876,#5858);
#5096=LINE('',#58900,#5859);
#5097=LINE('',#58902,#5860);
#5098=LINE('',#58904,#5861);
#5099=LINE('',#58905,#5862);
#5100=LINE('',#58908,#5863);
#5101=LINE('',#58910,#5864);
#5102=LINE('',#58911,#5865);
#5103=LINE('',#58914,#5866);
#5104=LINE('',#58916,#5867);
#5105=LINE('',#58917,#5868);
#5106=LINE('',#58920,#5869);
#5107=LINE('',#58922,#5870);
#5108=LINE('',#58923,#5871);
#5109=LINE('',#58926,#5872);
#5110=LINE('',#58928,#5873);
#5111=LINE('',#58929,#5874);
#5112=LINE('',#58931,#5875);
#5113=LINE('',#58932,#5876);
#5823=VECTOR('',#19172,3.);
#5824=VECTOR('',#19177,3.);
#5825=VECTOR('',#19180,3.);
#5826=VECTOR('',#19183,3.);
#5827=VECTOR('',#19186,3.);
#5828=VECTOR('',#19189,3.);
#5829=VECTOR('',#19192,3.);
#5830=VECTOR('',#19195,3.);
#5831=VECTOR('',#19198,3.);
#5832=VECTOR('',#19201,3.);
#5833=VECTOR('',#19204,3.);
#5834=VECTOR('',#19207,3.);
#5835=VECTOR('',#19210,3.);
#5836=VECTOR('',#19213,3.);
#5837=VECTOR('',#19216,3.);
#5838=VECTOR('',#19219,3.);
#5839=VECTOR('',#19222,3.);
#5840=VECTOR('',#19225,3.);
#5841=VECTOR('',#19228,2.37175);
#5842=VECTOR('',#19233,2.37175);
#5843=VECTOR('',#19236,2.37175);
#5844=VECTOR('',#19239,2.37175);
#5845=VECTOR('',#19242,2.37175);
#5846=VECTOR('',#19245,2.37175);
#5847=VECTOR('',#19248,2.37175);
#5848=VECTOR('',#19251,2.37175);
#5849=VECTOR('',#19254,2.37175);
#5850=VECTOR('',#19257,2.37175);
#5851=VECTOR('',#19260,2.37175);
#5852=VECTOR('',#19263,2.37175);
#5853=VECTOR('',#19266,2.37175);
#5854=VECTOR('',#19269,2.37175);
#5855=VECTOR('',#19272,2.37175);
#5856=VECTOR('',#19275,2.37175);
#5857=VECTOR('',#19278,2.37175);
#5858=VECTOR('',#19281,2.37175);
#5859=VECTOR('',#19284,10.);
#5860=VECTOR('',#19285,10.);
#5861=VECTOR('',#19286,10.);
#5862=VECTOR('',#19287,10.);
#5863=VECTOR('',#19290,10.);
#5864=VECTOR('',#19291,10.);
#5865=VECTOR('',#19292,10.);
#5866=VECTOR('',#19295,10.);
#5867=VECTOR('',#19296,10.);
#5868=VECTOR('',#19297,10.);
#5869=VECTOR('',#19300,10.);
#5870=VECTOR('',#19301,10.);
#5871=VECTOR('',#19302,10.);
#5872=VECTOR('',#19305,10.);
#5873=VECTOR('',#19306,10.);
#5874=VECTOR('',#19307,10.);
#5875=VECTOR('',#19310,10.);
#5876=VECTOR('',#19311,10.);
#7218=VERTEX_POINT('',#57592);
#7219=VERTEX_POINT('',#57593);
#7220=VERTEX_POINT('',#57595);
#7221=VERTEX_POINT('',#57606);
#7222=VERTEX_POINT('',#57616);
#7223=VERTEX_POINT('',#57617);
#7224=VERTEX_POINT('',#57664);
#7225=VERTEX_POINT('',#57665);
#7226=VERTEX_POINT('',#57712);
#7227=VERTEX_POINT('',#57713);
#7228=VERTEX_POINT('',#57766);
#7229=VERTEX_POINT('',#57767);
#7230=VERTEX_POINT('',#57814);
#7231=VERTEX_POINT('',#57815);
#7232=VERTEX_POINT('',#57862);
#7233=VERTEX_POINT('',#57863);
#7234=VERTEX_POINT('',#57916);
#7235=VERTEX_POINT('',#57917);
#7236=VERTEX_POINT('',#57964);
#7237=VERTEX_POINT('',#57965);
#7238=VERTEX_POINT('',#58012);
#7239=VERTEX_POINT('',#58013);
#7240=VERTEX_POINT('',#58066);
#7241=VERTEX_POINT('',#58067);
#7242=VERTEX_POINT('',#58114);
#7243=VERTEX_POINT('',#58115);
#7244=VERTEX_POINT('',#58162);
#7245=VERTEX_POINT('',#58163);
#7246=VERTEX_POINT('',#58216);
#7247=VERTEX_POINT('',#58217);
#7248=VERTEX_POINT('',#58264);
#7249=VERTEX_POINT('',#58265);
#7250=VERTEX_POINT('',#58312);
#7251=VERTEX_POINT('',#58313);
#7252=VERTEX_POINT('',#58366);
#7253=VERTEX_POINT('',#58367);
#7254=VERTEX_POINT('',#58414);
#7255=VERTEX_POINT('',#58415);
#7256=VERTEX_POINT('',#58462);
#7257=VERTEX_POINT('',#58463);
#7258=VERTEX_POINT('',#58465);
#7259=VERTEX_POINT('',#58472);
#7260=VERTEX_POINT('',#58479);
#7261=VERTEX_POINT('',#58480);
#7262=VERTEX_POINT('',#58504);
#7263=VERTEX_POINT('',#58505);
#7264=VERTEX_POINT('',#58528);
#7265=VERTEX_POINT('',#58529);
#7266=VERTEX_POINT('',#58553);
#7267=VERTEX_POINT('',#58554);
#7268=VERTEX_POINT('',#58578);
#7269=VERTEX_POINT('',#58579);
#7270=VERTEX_POINT('',#58602);
#7271=VERTEX_POINT('',#58603);
#7272=VERTEX_POINT('',#58627);
#7273=VERTEX_POINT('',#58628);
#7274=VERTEX_POINT('',#58652);
#7275=VERTEX_POINT('',#58653);
#7276=VERTEX_POINT('',#58676);
#7277=VERTEX_POINT('',#58677);
#7278=VERTEX_POINT('',#58701);
#7279=VERTEX_POINT('',#58702);
#7280=VERTEX_POINT('',#58726);
#7281=VERTEX_POINT('',#58727);
#7282=VERTEX_POINT('',#58750);
#7283=VERTEX_POINT('',#58751);
#7284=VERTEX_POINT('',#58775);
#7285=VERTEX_POINT('',#58776);
#7286=VERTEX_POINT('',#58800);
#7287=VERTEX_POINT('',#58801);
#7288=VERTEX_POINT('',#58824);
#7289=VERTEX_POINT('',#58825);
#7290=VERTEX_POINT('',#58849);
#7291=VERTEX_POINT('',#58850);
#7292=VERTEX_POINT('',#58874);
#7293=VERTEX_POINT('',#58875);
#7294=VERTEX_POINT('',#58898);
#7295=VERTEX_POINT('',#58899);
#7296=VERTEX_POINT('',#58901);
#7297=VERTEX_POINT('',#58903);
#7298=VERTEX_POINT('',#58907);
#7299=VERTEX_POINT('',#58909);
#7300=VERTEX_POINT('',#58913);
#7301=VERTEX_POINT('',#58915);
#7302=VERTEX_POINT('',#58919);
#7303=VERTEX_POINT('',#58921);
#7304=VERTEX_POINT('',#58925);
#7305=VERTEX_POINT('',#58927);
#7306=VERTEX_POINT('',#59410);
#7307=VERTEX_POINT('',#59521);
#7308=VERTEX_POINT('',#59623);
#7309=VERTEX_POINT('',#60109);
#9416=EDGE_CURVE('',#7218,#7219,#5060,.T.);
#9417=EDGE_CURVE('',#7218,#7220,#1368,.T.);
#9418=EDGE_CURVE('',#7220,#7221,#2546,.F.);
#9419=EDGE_CURVE('',#7221,#7219,#1369,.T.);
#9420=EDGE_CURVE('',#7222,#7223,#5061,.T.);
#9421=EDGE_CURVE('',#7222,#7218,#1370,.T.);
#9422=EDGE_CURVE('',#7219,#7223,#1371,.T.);
#9423=EDGE_CURVE('',#7224,#7225,#5062,.T.);
#9424=EDGE_CURVE('',#7224,#7222,#1372,.T.);
#9425=EDGE_CURVE('',#7223,#7225,#1373,.T.);
#9426=EDGE_CURVE('',#7226,#7227,#5063,.T.);
#9427=EDGE_CURVE('',#7226,#7224,#1374,.T.);
#9428=EDGE_CURVE('',#7225,#7227,#1375,.T.);
#9429=EDGE_CURVE('',#7228,#7229,#5064,.T.);
#9430=EDGE_CURVE('',#7228,#7226,#1376,.T.);
#9431=EDGE_CURVE('',#7227,#7229,#1377,.T.);
#9432=EDGE_CURVE('',#7230,#7231,#5065,.T.);
#9433=EDGE_CURVE('',#7230,#7228,#1378,.T.);
#9434=EDGE_CURVE('',#7229,#7231,#1379,.T.);
#9435=EDGE_CURVE('',#7232,#7233,#5066,.T.);
#9436=EDGE_CURVE('',#7232,#7230,#1380,.T.);
#9437=EDGE_CURVE('',#7231,#7233,#1381,.T.);
#9438=EDGE_CURVE('',#7234,#7235,#5067,.T.);
#9439=EDGE_CURVE('',#7234,#7232,#1382,.T.);
#9440=EDGE_CURVE('',#7233,#7235,#1383,.T.);
#9441=EDGE_CURVE('',#7236,#7237,#5068,.T.);
#9442=EDGE_CURVE('',#7236,#7234,#1384,.T.);
#9443=EDGE_CURVE('',#7235,#7237,#1385,.T.);
#9444=EDGE_CURVE('',#7238,#7239,#5069,.T.);
#9445=EDGE_CURVE('',#7238,#7236,#1386,.T.);
#9446=EDGE_CURVE('',#7237,#7239,#1387,.T.);
#9447=EDGE_CURVE('',#7240,#7241,#5070,.T.);
#9448=EDGE_CURVE('',#7240,#7238,#1388,.T.);
#9449=EDGE_CURVE('',#7239,#7241,#1389,.T.);
#9450=EDGE_CURVE('',#7242,#7243,#5071,.T.);
#9451=EDGE_CURVE('',#7242,#7240,#1390,.T.);
#9452=EDGE_CURVE('',#7241,#7243,#1391,.T.);
#9453=EDGE_CURVE('',#7244,#7245,#5072,.T.);
#9454=EDGE_CURVE('',#7244,#7242,#1392,.T.);
#9455=EDGE_CURVE('',#7243,#7245,#1393,.T.);
#9456=EDGE_CURVE('',#7246,#7247,#5073,.T.);
#9457=EDGE_CURVE('',#7246,#7244,#1394,.T.);
#9458=EDGE_CURVE('',#7245,#7247,#1395,.T.);
#9459=EDGE_CURVE('',#7248,#7249,#5074,.T.);
#9460=EDGE_CURVE('',#7248,#7246,#1396,.T.);
#9461=EDGE_CURVE('',#7247,#7249,#1397,.T.);
#9462=EDGE_CURVE('',#7250,#7251,#5075,.T.);
#9463=EDGE_CURVE('',#7250,#7248,#1398,.T.);
#9464=EDGE_CURVE('',#7249,#7251,#1399,.T.);
#9465=EDGE_CURVE('',#7252,#7253,#5076,.T.);
#9466=EDGE_CURVE('',#7252,#7250,#1400,.T.);
#9467=EDGE_CURVE('',#7251,#7253,#1401,.T.);
#9468=EDGE_CURVE('',#7254,#7255,#5077,.T.);
#9469=EDGE_CURVE('',#7254,#7252,#1402,.T.);
#9470=EDGE_CURVE('',#7253,#7255,#1403,.T.);
#9471=EDGE_CURVE('',#7256,#7257,#5078,.T.);
#9472=EDGE_CURVE('',#7256,#7258,#1404,.T.);
#9473=EDGE_CURVE('',#7259,#7258,#2547,.T.);
#9474=EDGE_CURVE('',#7257,#7259,#1405,.T.);
#9475=EDGE_CURVE('',#7260,#7261,#5079,.T.);
#9476=EDGE_CURVE('',#7260,#7256,#1406,.T.);
#9477=EDGE_CURVE('',#7261,#7257,#1407,.T.);
#9478=EDGE_CURVE('',#7262,#7263,#5080,.T.);
#9479=EDGE_CURVE('',#7262,#7260,#1408,.T.);
#9480=EDGE_CURVE('',#7263,#7261,#1409,.T.);
#9481=EDGE_CURVE('',#7264,#7265,#5081,.T.);
#9482=EDGE_CURVE('',#7264,#7262,#1410,.T.);
#9483=EDGE_CURVE('',#7265,#7263,#1411,.T.);
#9484=EDGE_CURVE('',#7266,#7267,#5082,.T.);
#9485=EDGE_CURVE('',#7266,#7264,#1412,.T.);
#9486=EDGE_CURVE('',#7267,#7265,#1413,.T.);
#9487=EDGE_CURVE('',#7268,#7269,#5083,.T.);
#9488=EDGE_CURVE('',#7268,#7266,#1414,.T.);
#9489=EDGE_CURVE('',#7269,#7267,#1415,.T.);
#9490=EDGE_CURVE('',#7270,#7271,#5084,.T.);
#9491=EDGE_CURVE('',#7270,#7268,#1416,.T.);
#9492=EDGE_CURVE('',#7271,#7269,#1417,.T.);
#9493=EDGE_CURVE('',#7272,#7273,#5085,.T.);
#9494=EDGE_CURVE('',#7272,#7270,#1418,.T.);
#9495=EDGE_CURVE('',#7273,#7271,#1419,.T.);
#9496=EDGE_CURVE('',#7274,#7275,#5086,.T.);
#9497=EDGE_CURVE('',#7274,#7272,#1420,.T.);
#9498=EDGE_CURVE('',#7275,#7273,#1421,.T.);
#9499=EDGE_CURVE('',#7276,#7277,#5087,.T.);
#9500=EDGE_CURVE('',#7276,#7274,#1422,.T.);
#9501=EDGE_CURVE('',#7277,#7275,#1423,.T.);
#9502=EDGE_CURVE('',#7278,#7279,#5088,.T.);
#9503=EDGE_CURVE('',#7278,#7276,#1424,.T.);
#9504=EDGE_CURVE('',#7279,#7277,#1425,.T.);
#9505=EDGE_CURVE('',#7280,#7281,#5089,.T.);
#9506=EDGE_CURVE('',#7280,#7278,#1426,.T.);
#9507=EDGE_CURVE('',#7281,#7279,#1427,.T.);
#9508=EDGE_CURVE('',#7282,#7283,#5090,.T.);
#9509=EDGE_CURVE('',#7282,#7280,#1428,.T.);
#9510=EDGE_CURVE('',#7283,#7281,#1429,.T.);
#9511=EDGE_CURVE('',#7284,#7285,#5091,.T.);
#9512=EDGE_CURVE('',#7284,#7282,#1430,.T.);
#9513=EDGE_CURVE('',#7285,#7283,#1431,.T.);
#9514=EDGE_CURVE('',#7286,#7287,#5092,.T.);
#9515=EDGE_CURVE('',#7286,#7284,#1432,.T.);
#9516=EDGE_CURVE('',#7287,#7285,#1433,.T.);
#9517=EDGE_CURVE('',#7288,#7289,#5093,.T.);
#9518=EDGE_CURVE('',#7288,#7286,#1434,.T.);
#9519=EDGE_CURVE('',#7289,#7287,#1435,.T.);
#9520=EDGE_CURVE('',#7290,#7291,#5094,.T.);
#9521=EDGE_CURVE('',#7290,#7288,#1436,.T.);
#9522=EDGE_CURVE('',#7291,#7289,#1437,.T.);
#9523=EDGE_CURVE('',#7292,#7293,#5095,.T.);
#9524=EDGE_CURVE('',#7292,#7290,#1438,.T.);
#9525=EDGE_CURVE('',#7293,#7291,#1439,.T.);
#9526=EDGE_CURVE('',#7294,#7295,#5096,.T.);
#9527=EDGE_CURVE('',#7294,#7296,#5097,.T.);
#9528=EDGE_CURVE('',#7296,#7297,#5098,.T.);
#9529=EDGE_CURVE('',#7295,#7297,#5099,.T.);
#9530=EDGE_CURVE('',#7298,#7294,#5100,.T.);
#9531=EDGE_CURVE('',#7298,#7299,#5101,.T.);
#9532=EDGE_CURVE('',#7299,#7296,#5102,.T.);
#9533=EDGE_CURVE('',#7300,#7298,#5103,.T.);
#9534=EDGE_CURVE('',#7300,#7301,#5104,.T.);
#9535=EDGE_CURVE('',#7301,#7299,#5105,.T.);
#9536=EDGE_CURVE('',#7302,#7300,#5106,.T.);
#9537=EDGE_CURVE('',#7302,#7303,#5107,.T.);
#9538=EDGE_CURVE('',#7303,#7301,#5108,.T.);
#9539=EDGE_CURVE('',#7304,#7302,#5109,.T.);
#9540=EDGE_CURVE('',#7304,#7305,#5110,.T.);
#9541=EDGE_CURVE('',#7305,#7303,#5111,.T.);
#9542=EDGE_CURVE('',#7295,#7304,#5112,.T.);
#9543=EDGE_CURVE('',#7297,#7305,#5113,.T.);
#9544=EDGE_CURVE('',#7306,#7259,#1440,.T.);
#9545=EDGE_CURVE('',#7255,#7306,#1441,.T.);
#9546=EDGE_CURVE('',#7307,#7221,#1442,.T.);
#9547=EDGE_CURVE('',#7307,#7293,#1443,.T.);
#9548=EDGE_CURVE('',#7308,#7307,#2548,.T.);
#9549=EDGE_CURVE('',#7308,#7292,#1444,.T.);
#9550=EDGE_CURVE('',#7258,#7309,#1445,.T.);
#9551=EDGE_CURVE('',#7220,#7308,#1446,.T.);
#9552=EDGE_CURVE('',#7309,#7254,#1447,.T.);
#9553=EDGE_CURVE('',#7309,#7306,#2549,.F.);
#13654=ORIENTED_EDGE('',*,*,#9416,.F.);
#13655=ORIENTED_EDGE('',*,*,#9417,.T.);
#13656=ORIENTED_EDGE('',*,*,#9418,.T.);
#13657=ORIENTED_EDGE('',*,*,#9419,.T.);
#13658=ORIENTED_EDGE('',*,*,#9420,.F.);
#13659=ORIENTED_EDGE('',*,*,#9421,.T.);
#13660=ORIENTED_EDGE('',*,*,#9416,.T.);
#13661=ORIENTED_EDGE('',*,*,#9422,.T.);
#13662=ORIENTED_EDGE('',*,*,#9423,.F.);
#13663=ORIENTED_EDGE('',*,*,#9424,.T.);
#13664=ORIENTED_EDGE('',*,*,#9420,.T.);
#13665=ORIENTED_EDGE('',*,*,#9425,.T.);
#13666=ORIENTED_EDGE('',*,*,#9426,.F.);
#13667=ORIENTED_EDGE('',*,*,#9427,.T.);
#13668=ORIENTED_EDGE('',*,*,#9423,.T.);
#13669=ORIENTED_EDGE('',*,*,#9428,.T.);
#13670=ORIENTED_EDGE('',*,*,#9429,.F.);
#13671=ORIENTED_EDGE('',*,*,#9430,.T.);
#13672=ORIENTED_EDGE('',*,*,#9426,.T.);
#13673=ORIENTED_EDGE('',*,*,#9431,.T.);
#13674=ORIENTED_EDGE('',*,*,#9432,.F.);
#13675=ORIENTED_EDGE('',*,*,#9433,.T.);
#13676=ORIENTED_EDGE('',*,*,#9429,.T.);
#13677=ORIENTED_EDGE('',*,*,#9434,.T.);
#13678=ORIENTED_EDGE('',*,*,#9435,.F.);
#13679=ORIENTED_EDGE('',*,*,#9436,.T.);
#13680=ORIENTED_EDGE('',*,*,#9432,.T.);
#13681=ORIENTED_EDGE('',*,*,#9437,.T.);
#13682=ORIENTED_EDGE('',*,*,#9438,.F.);
#13683=ORIENTED_EDGE('',*,*,#9439,.T.);
#13684=ORIENTED_EDGE('',*,*,#9435,.T.);
#13685=ORIENTED_EDGE('',*,*,#9440,.T.);
#13686=ORIENTED_EDGE('',*,*,#9441,.F.);
#13687=ORIENTED_EDGE('',*,*,#9442,.T.);
#13688=ORIENTED_EDGE('',*,*,#9438,.T.);
#13689=ORIENTED_EDGE('',*,*,#9443,.T.);
#13690=ORIENTED_EDGE('',*,*,#9444,.F.);
#13691=ORIENTED_EDGE('',*,*,#9445,.T.);
#13692=ORIENTED_EDGE('',*,*,#9441,.T.);
#13693=ORIENTED_EDGE('',*,*,#9446,.T.);
#13694=ORIENTED_EDGE('',*,*,#9447,.F.);
#13695=ORIENTED_EDGE('',*,*,#9448,.T.);
#13696=ORIENTED_EDGE('',*,*,#9444,.T.);
#13697=ORIENTED_EDGE('',*,*,#9449,.T.);
#13698=ORIENTED_EDGE('',*,*,#9450,.F.);
#13699=ORIENTED_EDGE('',*,*,#9451,.T.);
#13700=ORIENTED_EDGE('',*,*,#9447,.T.);
#13701=ORIENTED_EDGE('',*,*,#9452,.T.);
#13702=ORIENTED_EDGE('',*,*,#9453,.F.);
#13703=ORIENTED_EDGE('',*,*,#9454,.T.);
#13704=ORIENTED_EDGE('',*,*,#9450,.T.);
#13705=ORIENTED_EDGE('',*,*,#9455,.T.);
#13706=ORIENTED_EDGE('',*,*,#9456,.F.);
#13707=ORIENTED_EDGE('',*,*,#9457,.T.);
#13708=ORIENTED_EDGE('',*,*,#9453,.T.);
#13709=ORIENTED_EDGE('',*,*,#9458,.T.);
#13710=ORIENTED_EDGE('',*,*,#9459,.F.);
#13711=ORIENTED_EDGE('',*,*,#9460,.T.);
#13712=ORIENTED_EDGE('',*,*,#9456,.T.);
#13713=ORIENTED_EDGE('',*,*,#9461,.T.);
#13714=ORIENTED_EDGE('',*,*,#9462,.F.);
#13715=ORIENTED_EDGE('',*,*,#9463,.T.);
#13716=ORIENTED_EDGE('',*,*,#9459,.T.);
#13717=ORIENTED_EDGE('',*,*,#9464,.T.);
#13718=ORIENTED_EDGE('',*,*,#9465,.F.);
#13719=ORIENTED_EDGE('',*,*,#9466,.T.);
#13720=ORIENTED_EDGE('',*,*,#9462,.T.);
#13721=ORIENTED_EDGE('',*,*,#9467,.T.);
#13722=ORIENTED_EDGE('',*,*,#9468,.F.);
#13723=ORIENTED_EDGE('',*,*,#9469,.T.);
#13724=ORIENTED_EDGE('',*,*,#9465,.T.);
#13725=ORIENTED_EDGE('',*,*,#9470,.T.);
#13726=ORIENTED_EDGE('',*,*,#9471,.F.);
#13727=ORIENTED_EDGE('',*,*,#9472,.T.);
#13728=ORIENTED_EDGE('',*,*,#9473,.F.);
#13729=ORIENTED_EDGE('',*,*,#9474,.F.);
#13730=ORIENTED_EDGE('',*,*,#9475,.F.);
#13731=ORIENTED_EDGE('',*,*,#9476,.T.);
#13732=ORIENTED_EDGE('',*,*,#9471,.T.);
#13733=ORIENTED_EDGE('',*,*,#9477,.F.);
#13734=ORIENTED_EDGE('',*,*,#9478,.F.);
#13735=ORIENTED_EDGE('',*,*,#9479,.T.);
#13736=ORIENTED_EDGE('',*,*,#9475,.T.);
#13737=ORIENTED_EDGE('',*,*,#9480,.F.);
#13738=ORIENTED_EDGE('',*,*,#9481,.F.);
#13739=ORIENTED_EDGE('',*,*,#9482,.T.);
#13740=ORIENTED_EDGE('',*,*,#9478,.T.);
#13741=ORIENTED_EDGE('',*,*,#9483,.F.);
#13742=ORIENTED_EDGE('',*,*,#9484,.F.);
#13743=ORIENTED_EDGE('',*,*,#9485,.T.);
#13744=ORIENTED_EDGE('',*,*,#9481,.T.);
#13745=ORIENTED_EDGE('',*,*,#9486,.F.);
#13746=ORIENTED_EDGE('',*,*,#9487,.F.);
#13747=ORIENTED_EDGE('',*,*,#9488,.T.);
#13748=ORIENTED_EDGE('',*,*,#9484,.T.);
#13749=ORIENTED_EDGE('',*,*,#9489,.F.);
#13750=ORIENTED_EDGE('',*,*,#9490,.F.);
#13751=ORIENTED_EDGE('',*,*,#9491,.T.);
#13752=ORIENTED_EDGE('',*,*,#9487,.T.);
#13753=ORIENTED_EDGE('',*,*,#9492,.F.);
#13754=ORIENTED_EDGE('',*,*,#9493,.F.);
#13755=ORIENTED_EDGE('',*,*,#9494,.T.);
#13756=ORIENTED_EDGE('',*,*,#9490,.T.);
#13757=ORIENTED_EDGE('',*,*,#9495,.F.);
#13758=ORIENTED_EDGE('',*,*,#9496,.F.);
#13759=ORIENTED_EDGE('',*,*,#9497,.T.);
#13760=ORIENTED_EDGE('',*,*,#9493,.T.);
#13761=ORIENTED_EDGE('',*,*,#9498,.F.);
#13762=ORIENTED_EDGE('',*,*,#9499,.F.);
#13763=ORIENTED_EDGE('',*,*,#9500,.T.);
#13764=ORIENTED_EDGE('',*,*,#9496,.T.);
#13765=ORIENTED_EDGE('',*,*,#9501,.F.);
#13766=ORIENTED_EDGE('',*,*,#9502,.F.);
#13767=ORIENTED_EDGE('',*,*,#9503,.T.);
#13768=ORIENTED_EDGE('',*,*,#9499,.T.);
#13769=ORIENTED_EDGE('',*,*,#9504,.F.);
#13770=ORIENTED_EDGE('',*,*,#9505,.F.);
#13771=ORIENTED_EDGE('',*,*,#9506,.T.);
#13772=ORIENTED_EDGE('',*,*,#9502,.T.);
#13773=ORIENTED_EDGE('',*,*,#9507,.F.);
#13774=ORIENTED_EDGE('',*,*,#9508,.F.);
#13775=ORIENTED_EDGE('',*,*,#9509,.T.);
#13776=ORIENTED_EDGE('',*,*,#9505,.T.);
#13777=ORIENTED_EDGE('',*,*,#9510,.F.);
#13778=ORIENTED_EDGE('',*,*,#9511,.F.);
#13779=ORIENTED_EDGE('',*,*,#9512,.T.);
#13780=ORIENTED_EDGE('',*,*,#9508,.T.);
#13781=ORIENTED_EDGE('',*,*,#9513,.F.);
#13782=ORIENTED_EDGE('',*,*,#9514,.F.);
#13783=ORIENTED_EDGE('',*,*,#9515,.T.);
#13784=ORIENTED_EDGE('',*,*,#9511,.T.);
#13785=ORIENTED_EDGE('',*,*,#9516,.F.);
#13786=ORIENTED_EDGE('',*,*,#9517,.F.);
#13787=ORIENTED_EDGE('',*,*,#9518,.T.);
#13788=ORIENTED_EDGE('',*,*,#9514,.T.);
#13789=ORIENTED_EDGE('',*,*,#9519,.F.);
#13790=ORIENTED_EDGE('',*,*,#9520,.F.);
#13791=ORIENTED_EDGE('',*,*,#9521,.T.);
#13792=ORIENTED_EDGE('',*,*,#9517,.T.);
#13793=ORIENTED_EDGE('',*,*,#9522,.F.);
#13794=ORIENTED_EDGE('',*,*,#9523,.F.);
#13795=ORIENTED_EDGE('',*,*,#9524,.T.);
#13796=ORIENTED_EDGE('',*,*,#9520,.T.);
#13797=ORIENTED_EDGE('',*,*,#9525,.F.);
#13798=ORIENTED_EDGE('',*,*,#9526,.F.);
#13799=ORIENTED_EDGE('',*,*,#9527,.T.);
#13800=ORIENTED_EDGE('',*,*,#9528,.T.);
#13801=ORIENTED_EDGE('',*,*,#9529,.F.);
#13802=ORIENTED_EDGE('',*,*,#9530,.F.);
#13803=ORIENTED_EDGE('',*,*,#9531,.T.);
#13804=ORIENTED_EDGE('',*,*,#9532,.T.);
#13805=ORIENTED_EDGE('',*,*,#9527,.F.);
#13806=ORIENTED_EDGE('',*,*,#9533,.F.);
#13807=ORIENTED_EDGE('',*,*,#9534,.T.);
#13808=ORIENTED_EDGE('',*,*,#9535,.T.);
#13809=ORIENTED_EDGE('',*,*,#9531,.F.);
#13810=ORIENTED_EDGE('',*,*,#9536,.F.);
#13811=ORIENTED_EDGE('',*,*,#9537,.T.);
#13812=ORIENTED_EDGE('',*,*,#9538,.T.);
#13813=ORIENTED_EDGE('',*,*,#9534,.F.);
#13814=ORIENTED_EDGE('',*,*,#9539,.F.);
#13815=ORIENTED_EDGE('',*,*,#9540,.T.);
#13816=ORIENTED_EDGE('',*,*,#9541,.T.);
#13817=ORIENTED_EDGE('',*,*,#9537,.F.);
#13818=ORIENTED_EDGE('',*,*,#9542,.F.);
#13819=ORIENTED_EDGE('',*,*,#9529,.T.);
#13820=ORIENTED_EDGE('',*,*,#9543,.T.);
#13821=ORIENTED_EDGE('',*,*,#9540,.F.);
#13822=ORIENTED_EDGE('',*,*,#9543,.F.);
#13823=ORIENTED_EDGE('',*,*,#9528,.F.);
#13824=ORIENTED_EDGE('',*,*,#9532,.F.);
#13825=ORIENTED_EDGE('',*,*,#9535,.F.);
#13826=ORIENTED_EDGE('',*,*,#9538,.F.);
#13827=ORIENTED_EDGE('',*,*,#9541,.F.);
#13828=ORIENTED_EDGE('',*,*,#9544,.F.);
#13829=ORIENTED_EDGE('',*,*,#9545,.F.);
#13830=ORIENTED_EDGE('',*,*,#9470,.F.);
#13831=ORIENTED_EDGE('',*,*,#9467,.F.);
#13832=ORIENTED_EDGE('',*,*,#9464,.F.);
#13833=ORIENTED_EDGE('',*,*,#9461,.F.);
#13834=ORIENTED_EDGE('',*,*,#9458,.F.);
#13835=ORIENTED_EDGE('',*,*,#9455,.F.);
#13836=ORIENTED_EDGE('',*,*,#9452,.F.);
#13837=ORIENTED_EDGE('',*,*,#9449,.F.);
#13838=ORIENTED_EDGE('',*,*,#9446,.F.);
#13839=ORIENTED_EDGE('',*,*,#9443,.F.);
#13840=ORIENTED_EDGE('',*,*,#9440,.F.);
#13841=ORIENTED_EDGE('',*,*,#9437,.F.);
#13842=ORIENTED_EDGE('',*,*,#9434,.F.);
#13843=ORIENTED_EDGE('',*,*,#9431,.F.);
#13844=ORIENTED_EDGE('',*,*,#9428,.F.);
#13845=ORIENTED_EDGE('',*,*,#9425,.F.);
#13846=ORIENTED_EDGE('',*,*,#9422,.F.);
#13847=ORIENTED_EDGE('',*,*,#9419,.F.);
#13848=ORIENTED_EDGE('',*,*,#9546,.F.);
#13849=ORIENTED_EDGE('',*,*,#9547,.T.);
#13850=ORIENTED_EDGE('',*,*,#9525,.T.);
#13851=ORIENTED_EDGE('',*,*,#9522,.T.);
#13852=ORIENTED_EDGE('',*,*,#9519,.T.);
#13853=ORIENTED_EDGE('',*,*,#9516,.T.);
#13854=ORIENTED_EDGE('',*,*,#9513,.T.);
#13855=ORIENTED_EDGE('',*,*,#9510,.T.);
#13856=ORIENTED_EDGE('',*,*,#9507,.T.);
#13857=ORIENTED_EDGE('',*,*,#9504,.T.);
#13858=ORIENTED_EDGE('',*,*,#9501,.T.);
#13859=ORIENTED_EDGE('',*,*,#9498,.T.);
#13860=ORIENTED_EDGE('',*,*,#9495,.T.);
#13861=ORIENTED_EDGE('',*,*,#9492,.T.);
#13862=ORIENTED_EDGE('',*,*,#9489,.T.);
#13863=ORIENTED_EDGE('',*,*,#9486,.T.);
#13864=ORIENTED_EDGE('',*,*,#9483,.T.);
#13865=ORIENTED_EDGE('',*,*,#9480,.T.);
#13866=ORIENTED_EDGE('',*,*,#9477,.T.);
#13867=ORIENTED_EDGE('',*,*,#9474,.T.);
#13868=ORIENTED_EDGE('',*,*,#9523,.T.);
#13869=ORIENTED_EDGE('',*,*,#9547,.F.);
#13870=ORIENTED_EDGE('',*,*,#9548,.F.);
#13871=ORIENTED_EDGE('',*,*,#9549,.T.);
#13872=ORIENTED_EDGE('',*,*,#9550,.F.);
#13873=ORIENTED_EDGE('',*,*,#9472,.F.);
#13874=ORIENTED_EDGE('',*,*,#9476,.F.);
#13875=ORIENTED_EDGE('',*,*,#9479,.F.);
#13876=ORIENTED_EDGE('',*,*,#9482,.F.);
#13877=ORIENTED_EDGE('',*,*,#9485,.F.);
#13878=ORIENTED_EDGE('',*,*,#9488,.F.);
#13879=ORIENTED_EDGE('',*,*,#9491,.F.);
#13880=ORIENTED_EDGE('',*,*,#9494,.F.);
#13881=ORIENTED_EDGE('',*,*,#9497,.F.);
#13882=ORIENTED_EDGE('',*,*,#9500,.F.);
#13883=ORIENTED_EDGE('',*,*,#9503,.F.);
#13884=ORIENTED_EDGE('',*,*,#9506,.F.);
#13885=ORIENTED_EDGE('',*,*,#9509,.F.);
#13886=ORIENTED_EDGE('',*,*,#9512,.F.);
#13887=ORIENTED_EDGE('',*,*,#9515,.F.);
#13888=ORIENTED_EDGE('',*,*,#9518,.F.);
#13889=ORIENTED_EDGE('',*,*,#9521,.F.);
#13890=ORIENTED_EDGE('',*,*,#9524,.F.);
#13891=ORIENTED_EDGE('',*,*,#9549,.F.);
#13892=ORIENTED_EDGE('',*,*,#9551,.F.);
#13893=ORIENTED_EDGE('',*,*,#9417,.F.);
#13894=ORIENTED_EDGE('',*,*,#9421,.F.);
#13895=ORIENTED_EDGE('',*,*,#9424,.F.);
#13896=ORIENTED_EDGE('',*,*,#9427,.F.);
#13897=ORIENTED_EDGE('',*,*,#9430,.F.);
#13898=ORIENTED_EDGE('',*,*,#9433,.F.);
#13899=ORIENTED_EDGE('',*,*,#9436,.F.);
#13900=ORIENTED_EDGE('',*,*,#9439,.F.);
#13901=ORIENTED_EDGE('',*,*,#9442,.F.);
#13902=ORIENTED_EDGE('',*,*,#9445,.F.);
#13903=ORIENTED_EDGE('',*,*,#9448,.F.);
#13904=ORIENTED_EDGE('',*,*,#9451,.F.);
#13905=ORIENTED_EDGE('',*,*,#9454,.F.);
#13906=ORIENTED_EDGE('',*,*,#9457,.F.);
#13907=ORIENTED_EDGE('',*,*,#9460,.F.);
#13908=ORIENTED_EDGE('',*,*,#9463,.F.);
#13909=ORIENTED_EDGE('',*,*,#9466,.F.);
#13910=ORIENTED_EDGE('',*,*,#9469,.F.);
#13911=ORIENTED_EDGE('',*,*,#9552,.F.);
#13912=ORIENTED_EDGE('',*,*,#9544,.T.);
#13913=ORIENTED_EDGE('',*,*,#9473,.T.);
#13914=ORIENTED_EDGE('',*,*,#9550,.T.);
#13915=ORIENTED_EDGE('',*,*,#9553,.T.);
#13916=ORIENTED_EDGE('',*,*,#9468,.T.);
#13917=ORIENTED_EDGE('',*,*,#9545,.T.);
#13918=ORIENTED_EDGE('',*,*,#9553,.F.);
#13919=ORIENTED_EDGE('',*,*,#9552,.T.);
#13920=ORIENTED_EDGE('',*,*,#9546,.T.);
#13921=ORIENTED_EDGE('',*,*,#9418,.F.);
#13922=ORIENTED_EDGE('',*,*,#9551,.T.);
#13923=ORIENTED_EDGE('',*,*,#9548,.T.);
#13924=ORIENTED_EDGE('',*,*,#9526,.T.);
#13925=ORIENTED_EDGE('',*,*,#9542,.T.);
#13926=ORIENTED_EDGE('',*,*,#9539,.T.);
#13927=ORIENTED_EDGE('',*,*,#9536,.T.);
#13928=ORIENTED_EDGE('',*,*,#9533,.T.);
#13929=ORIENTED_EDGE('',*,*,#9530,.T.);
#14596=PLANE('',#16570);
#14597=PLANE('',#16571);
#14598=PLANE('',#16572);
#14599=PLANE('',#16573);
#14600=PLANE('',#16574);
#14601=PLANE('',#16575);
#14602=PLANE('',#16576);
#14603=PLANE('',#16579);
#14604=PLANE('',#16582);
#15321=ADVANCED_FACE('',(#3341),#2287,.T.);
#15322=ADVANCED_FACE('',(#3342),#2288,.T.);
#15323=ADVANCED_FACE('',(#3343),#2289,.T.);
#15324=ADVANCED_FACE('',(#3344),#2290,.T.);
#15325=ADVANCED_FACE('',(#3345),#2291,.T.);
#15326=ADVANCED_FACE('',(#3346),#2292,.T.);
#15327=ADVANCED_FACE('',(#3347),#2293,.T.);
#15328=ADVANCED_FACE('',(#3348),#2294,.T.);
#15329=ADVANCED_FACE('',(#3349),#2295,.T.);
#15330=ADVANCED_FACE('',(#3350),#2296,.T.);
#15331=ADVANCED_FACE('',(#3351),#2297,.T.);
#15332=ADVANCED_FACE('',(#3352),#2298,.T.);
#15333=ADVANCED_FACE('',(#3353),#2299,.T.);
#15334=ADVANCED_FACE('',(#3354),#2300,.T.);
#15335=ADVANCED_FACE('',(#3355),#2301,.T.);
#15336=ADVANCED_FACE('',(#3356),#2302,.T.);
#15337=ADVANCED_FACE('',(#3357),#2303,.T.);
#15338=ADVANCED_FACE('',(#3358),#2304,.T.);
#15339=ADVANCED_FACE('',(#3359),#2305,.T.);
#15340=ADVANCED_FACE('',(#3360),#2306,.T.);
#15341=ADVANCED_FACE('',(#3361),#2307,.T.);
#15342=ADVANCED_FACE('',(#3362),#2308,.T.);
#15343=ADVANCED_FACE('',(#3363),#2309,.T.);
#15344=ADVANCED_FACE('',(#3364),#2310,.T.);
#15345=ADVANCED_FACE('',(#3365),#2311,.T.);
#15346=ADVANCED_FACE('',(#3366),#2312,.T.);
#15347=ADVANCED_FACE('',(#3367),#2313,.T.);
#15348=ADVANCED_FACE('',(#3368),#2314,.T.);
#15349=ADVANCED_FACE('',(#3369),#2315,.T.);
#15350=ADVANCED_FACE('',(#3370),#2316,.T.);
#15351=ADVANCED_FACE('',(#3371),#2317,.T.);
#15352=ADVANCED_FACE('',(#3372),#2318,.T.);
#15353=ADVANCED_FACE('',(#3373),#2319,.T.);
#15354=ADVANCED_FACE('',(#3374),#2320,.T.);
#15355=ADVANCED_FACE('',(#3375),#2321,.T.);
#15356=ADVANCED_FACE('',(#3376),#2322,.T.);
#15357=ADVANCED_FACE('',(#3377),#14596,.F.);
#15358=ADVANCED_FACE('',(#3378),#14597,.F.);
#15359=ADVANCED_FACE('',(#3379),#14598,.F.);
#15360=ADVANCED_FACE('',(#3380),#14599,.F.);
#15361=ADVANCED_FACE('',(#3381),#14600,.F.);
#15362=ADVANCED_FACE('',(#3382),#14601,.F.);
#15363=ADVANCED_FACE('',(#3383),#14602,.F.);
#15364=ADVANCED_FACE('',(#3384),#262,.F.);
#15365=ADVANCED_FACE('',(#3385),#2323,.T.);
#15366=ADVANCED_FACE('',(#3386),#263,.F.);
#15367=ADVANCED_FACE('',(#3387),#14603,.T.);
#15368=ADVANCED_FACE('',(#3388),#2324,.T.);
#15369=ADVANCED_FACE('',(#3389,#1691),#14604,.F.);
#15488=CLOSED_SHELL('',(#15321,#15322,#15323,#15324,#15325,#15326,#15327,
#15328,#15329,#15330,#15331,#15332,#15333,#15334,#15335,#15336,#15337,#15338,
#15339,#15340,#15341,#15342,#15343,#15344,#15345,#15346,#15347,#15348,#15349,
#15350,#15351,#15352,#15353,#15354,#15355,#15356,#15357,#15358,#15359,#15360,
#15361,#15362,#15363,#15364,#15365,#15366,#15367,#15368,#15369));
#16531=AXIS2_PLACEMENT_3D('',#57590,#19168,#19169);
#16532=AXIS2_PLACEMENT_3D('',#57591,#19170,#19171);
#16533=AXIS2_PLACEMENT_3D('',#57607,#19173,#19174);
#16534=AXIS2_PLACEMENT_3D('',#57615,#19175,#19176);
#16535=AXIS2_PLACEMENT_3D('',#57663,#19178,#19179);
#16536=AXIS2_PLACEMENT_3D('',#57711,#19181,#19182);
#16537=AXIS2_PLACEMENT_3D('',#57765,#19184,#19185);
#16538=AXIS2_PLACEMENT_3D('',#57813,#19187,#19188);
#16539=AXIS2_PLACEMENT_3D('',#57861,#19190,#19191);
#16540=AXIS2_PLACEMENT_3D('',#57915,#19193,#19194);
#16541=AXIS2_PLACEMENT_3D('',#57963,#19196,#19197);
#16542=AXIS2_PLACEMENT_3D('',#58011,#19199,#19200);
#16543=AXIS2_PLACEMENT_3D('',#58065,#19202,#19203);
#16544=AXIS2_PLACEMENT_3D('',#58113,#19205,#19206);
#16545=AXIS2_PLACEMENT_3D('',#58161,#19208,#19209);
#16546=AXIS2_PLACEMENT_3D('',#58215,#19211,#19212);
#16547=AXIS2_PLACEMENT_3D('',#58263,#19214,#19215);
#16548=AXIS2_PLACEMENT_3D('',#58311,#19217,#19218);
#16549=AXIS2_PLACEMENT_3D('',#58365,#19220,#19221);
#16550=AXIS2_PLACEMENT_3D('',#58413,#19223,#19224);
#16551=AXIS2_PLACEMENT_3D('',#58461,#19226,#19227);
#16552=AXIS2_PLACEMENT_3D('',#58473,#19229,#19230);
#16553=AXIS2_PLACEMENT_3D('',#58478,#19231,#19232);
#16554=AXIS2_PLACEMENT_3D('',#58503,#19234,#19235);
#16555=AXIS2_PLACEMENT_3D('',#58527,#19237,#19238);
#16556=AXIS2_PLACEMENT_3D('',#58552,#19240,#19241);
#16557=AXIS2_PLACEMENT_3D('',#58577,#19243,#19244);
#16558=AXIS2_PLACEMENT_3D('',#58601,#19246,#19247);
#16559=AXIS2_PLACEMENT_3D('',#58626,#19249,#19250);
#16560=AXIS2_PLACEMENT_3D('',#58651,#19252,#19253);
#16561=AXIS2_PLACEMENT_3D('',#58675,#19255,#19256);
#16562=AXIS2_PLACEMENT_3D('',#58700,#19258,#19259);
#16563=AXIS2_PLACEMENT_3D('',#58725,#19261,#19262);
#16564=AXIS2_PLACEMENT_3D('',#58749,#19264,#19265);
#16565=AXIS2_PLACEMENT_3D('',#58774,#19267,#19268);
#16566=AXIS2_PLACEMENT_3D('',#58799,#19270,#19271);
#16567=AXIS2_PLACEMENT_3D('',#58823,#19273,#19274);
#16568=AXIS2_PLACEMENT_3D('',#58848,#19276,#19277);
#16569=AXIS2_PLACEMENT_3D('',#58873,#19279,#19280);
#16570=AXIS2_PLACEMENT_3D('',#58897,#19282,#19283);
#16571=AXIS2_PLACEMENT_3D('',#58906,#19288,#19289);
#16572=AXIS2_PLACEMENT_3D('',#58912,#19293,#19294);
#16573=AXIS2_PLACEMENT_3D('',#58918,#19298,#19299);
#16574=AXIS2_PLACEMENT_3D('',#58924,#19303,#19304);
#16575=AXIS2_PLACEMENT_3D('',#58930,#19308,#19309);
#16576=AXIS2_PLACEMENT_3D('',#58933,#19312,#19313);
#16577=AXIS2_PLACEMENT_3D('',#59622,#19314,#19315);
#16578=AXIS2_PLACEMENT_3D('',#59624,#19316,#19317);
#16579=AXIS2_PLACEMENT_3D('',#60308,#19318,#19319);
#16580=AXIS2_PLACEMENT_3D('',#60309,#19320,#19321);
#16581=AXIS2_PLACEMENT_3D('',#60310,#19322,#19323);
#16582=AXIS2_PLACEMENT_3D('',#60311,#19324,#19325);
#19168=DIRECTION('axis',(0.,0.,1.));
#19169=DIRECTION('refdir',(1.,0.,0.));
#19170=DIRECTION('center_axis',(0.,0.,1.));
#19171=DIRECTION('ref_axis',(1.,0.,0.));
#19172=DIRECTION('',(0.,0.,-1.));
#19173=DIRECTION('center_axis',(0.,0.,-1.));
#19174=DIRECTION('ref_axis',(1.,0.,0.));
#19175=DIRECTION('center_axis',(0.,0.,1.));
#19176=DIRECTION('ref_axis',(1.,0.,0.));
#19177=DIRECTION('',(0.,0.,-1.));
#19178=DIRECTION('center_axis',(0.,0.,1.));
#19179=DIRECTION('ref_axis',(1.,0.,0.));
#19180=DIRECTION('',(0.,0.,-1.));
#19181=DIRECTION('center_axis',(0.,0.,1.));
#19182=DIRECTION('ref_axis',(1.,0.,0.));
#19183=DIRECTION('',(0.,0.,-1.));
#19184=DIRECTION('center_axis',(0.,0.,1.));
#19185=DIRECTION('ref_axis',(1.,0.,0.));
#19186=DIRECTION('',(0.,0.,-1.));
#19187=DIRECTION('center_axis',(0.,0.,1.));
#19188=DIRECTION('ref_axis',(1.,0.,0.));
#19189=DIRECTION('',(0.,0.,-1.));
#19190=DIRECTION('center_axis',(0.,0.,1.));
#19191=DIRECTION('ref_axis',(1.,0.,0.));
#19192=DIRECTION('',(0.,0.,-1.));
#19193=DIRECTION('center_axis',(0.,0.,1.));
#19194=DIRECTION('ref_axis',(1.,0.,0.));
#19195=DIRECTION('',(0.,0.,-1.));
#19196=DIRECTION('center_axis',(0.,0.,1.));
#19197=DIRECTION('ref_axis',(1.,0.,0.));
#19198=DIRECTION('',(0.,0.,-1.));
#19199=DIRECTION('center_axis',(0.,0.,1.));
#19200=DIRECTION('ref_axis',(1.,0.,0.));
#19201=DIRECTION('',(0.,0.,-1.));
#19202=DIRECTION('center_axis',(0.,0.,1.));
#19203=DIRECTION('ref_axis',(1.,0.,0.));
#19204=DIRECTION('',(0.,0.,-1.));
#19205=DIRECTION('center_axis',(0.,0.,1.));
#19206=DIRECTION('ref_axis',(1.,0.,0.));
#19207=DIRECTION('',(0.,0.,-1.));
#19208=DIRECTION('center_axis',(0.,0.,1.));
#19209=DIRECTION('ref_axis',(1.,0.,0.));
#19210=DIRECTION('',(0.,0.,-1.));
#19211=DIRECTION('center_axis',(0.,0.,1.));
#19212=DIRECTION('ref_axis',(1.,0.,0.));
#19213=DIRECTION('',(0.,0.,-1.));
#19214=DIRECTION('center_axis',(0.,0.,1.));
#19215=DIRECTION('ref_axis',(1.,0.,0.));
#19216=DIRECTION('',(0.,0.,-1.));
#19217=DIRECTION('center_axis',(0.,0.,1.));
#19218=DIRECTION('ref_axis',(1.,0.,0.));
#19219=DIRECTION('',(0.,0.,-1.));
#19220=DIRECTION('center_axis',(0.,0.,1.));
#19221=DIRECTION('ref_axis',(1.,0.,0.));
#19222=DIRECTION('',(0.,0.,-1.));
#19223=DIRECTION('center_axis',(0.,0.,1.));
#19224=DIRECTION('ref_axis',(1.,0.,0.));
#19225=DIRECTION('',(0.,0.,-1.));
#19226=DIRECTION('center_axis',(0.,0.,1.));
#19227=DIRECTION('ref_axis',(-0.457769008694702,-0.889071164012572,0.));
#19228=DIRECTION('',(0.,0.,1.));
#19229=DIRECTION('center_axis',(0.,0.,1.));
#19230=DIRECTION('ref_axis',(1.,1.45731777125179E-13,0.));
#19231=DIRECTION('center_axis',(0.,0.,1.));
#19232=DIRECTION('ref_axis',(1.,1.45731777125179E-13,0.));
#19233=DIRECTION('',(0.,0.,1.));
#19234=DIRECTION('center_axis',(0.,0.,1.));
#19235=DIRECTION('ref_axis',(1.,1.45731777125179E-13,0.));
#19236=DIRECTION('',(0.,0.,1.));
#19237=DIRECTION('center_axis',(0.,0.,1.));
#19238=DIRECTION('ref_axis',(1.,1.45731777125179E-13,0.));
#19239=DIRECTION('',(0.,0.,1.));
#19240=DIRECTION('center_axis',(0.,0.,1.));
#19241=DIRECTION('ref_axis',(1.,1.45731777125179E-13,0.));
#19242=DIRECTION('',(0.,0.,1.));
#19243=DIRECTION('center_axis',(0.,0.,1.));
#19244=DIRECTION('ref_axis',(1.,1.45731777125179E-13,0.));
#19245=DIRECTION('',(0.,0.,1.));
#19246=DIRECTION('center_axis',(0.,0.,1.));
#19247=DIRECTION('ref_axis',(1.,1.45731777125179E-13,0.));
#19248=DIRECTION('',(0.,0.,1.));
#19249=DIRECTION('center_axis',(0.,0.,1.));
#19250=DIRECTION('ref_axis',(1.,1.45731777125179E-13,0.));
#19251=DIRECTION('',(0.,0.,1.));
#19252=DIRECTION('center_axis',(0.,0.,1.));
#19253=DIRECTION('ref_axis',(1.,1.45731777125179E-13,0.));
#19254=DIRECTION('',(0.,0.,1.));
#19255=DIRECTION('center_axis',(0.,0.,1.));
#19256=DIRECTION('ref_axis',(1.,1.45731777125179E-13,0.));
#19257=DIRECTION('',(0.,0.,1.));
#19258=DIRECTION('center_axis',(0.,0.,1.));
#19259=DIRECTION('ref_axis',(1.,1.45731777125179E-13,0.));
#19260=DIRECTION('',(0.,0.,1.));
#19261=DIRECTION('center_axis',(0.,0.,1.));
#19262=DIRECTION('ref_axis',(1.,1.45731777125179E-13,0.));
#19263=DIRECTION('',(0.,0.,1.));
#19264=DIRECTION('center_axis',(0.,0.,1.));
#19265=DIRECTION('ref_axis',(1.,1.45731777125179E-13,0.));
#19266=DIRECTION('',(0.,0.,1.));
#19267=DIRECTION('center_axis',(0.,0.,1.));
#19268=DIRECTION('ref_axis',(1.,1.45731777125179E-13,0.));
#19269=DIRECTION('',(0.,0.,1.));
#19270=DIRECTION('center_axis',(0.,0.,1.));
#19271=DIRECTION('ref_axis',(1.,1.45731777125179E-13,0.));
#19272=DIRECTION('',(0.,0.,1.));
#19273=DIRECTION('center_axis',(0.,0.,1.));
#19274=DIRECTION('ref_axis',(1.,1.45731777125179E-13,0.));
#19275=DIRECTION('',(0.,0.,1.));
#19276=DIRECTION('center_axis',(0.,0.,1.));
#19277=DIRECTION('ref_axis',(1.,1.45731777125179E-13,0.));
#19278=DIRECTION('',(0.,0.,1.));
#19279=DIRECTION('center_axis',(0.,0.,1.));
#19280=DIRECTION('ref_axis',(1.,1.45731777125179E-13,0.));
#19281=DIRECTION('',(0.,0.,1.));
#19282=DIRECTION('center_axis',(-1.60246890531964E-16,-1.,0.));
#19283=DIRECTION('ref_axis',(1.,-1.60246890531964E-16,0.));
#19284=DIRECTION('',(1.,-1.60246890531964E-16,0.));
#19285=DIRECTION('',(0.,0.,1.));
#19286=DIRECTION('',(1.,-1.60246890531964E-16,0.));
#19287=DIRECTION('',(0.,0.,1.));
#19288=DIRECTION('center_axis',(-0.866025403784439,-0.5,0.));
#19289=DIRECTION('ref_axis',(0.5,-0.866025403784439,0.));
#19290=DIRECTION('',(0.5,-0.866025403784439,0.));
#19291=DIRECTION('',(0.,0.,1.));
#19292=DIRECTION('',(0.5,-0.866025403784439,0.));
#19293=DIRECTION('center_axis',(-0.866025403784439,0.5,0.));
#19294=DIRECTION('ref_axis',(-0.5,-0.866025403784439,0.));
#19295=DIRECTION('',(-0.5,-0.866025403784439,0.));
#19296=DIRECTION('',(0.,0.,1.));
#19297=DIRECTION('',(-0.5,-0.866025403784439,0.));
#19298=DIRECTION('center_axis',(1.60246890531964E-16,1.,0.));
#19299=DIRECTION('ref_axis',(-1.,1.60246890531964E-16,0.));
#19300=DIRECTION('',(-1.,1.60246890531964E-16,0.));
#19301=DIRECTION('',(0.,0.,1.));
#19302=DIRECTION('',(-1.,1.60246890531964E-16,0.));
#19303=DIRECTION('center_axis',(0.866025403784439,0.5,0.));
#19304=DIRECTION('ref_axis',(-0.5,0.866025403784439,0.));
#19305=DIRECTION('',(-0.5,0.866025403784439,0.));
#19306=DIRECTION('',(0.,0.,1.));
#19307=DIRECTION('',(-0.5,0.866025403784439,0.));
#19308=DIRECTION('center_axis',(0.866025403784439,-0.5,0.));
#19309=DIRECTION('ref_axis',(0.5,0.866025403784439,0.));
#19310=DIRECTION('',(0.5,0.866025403784439,0.));
#19311=DIRECTION('',(0.5,0.866025403784439,0.));
#19312=DIRECTION('center_axis',(0.,0.,1.));
#19313=DIRECTION('ref_axis',(1.,0.,0.));
#19314=DIRECTION('center_axis',(0.,0.,1.));
#19315=DIRECTION('ref_axis',(1.,1.45731777125179E-13,0.));
#19316=DIRECTION('center_axis',(0.,0.,-1.));
#19317=DIRECTION('ref_axis',(1.,1.45731777125179E-13,0.));
#19318=DIRECTION('center_axis',(0.,0.,1.));
#19319=DIRECTION('ref_axis',(1.,0.,0.));
#19320=DIRECTION('center_axis',(0.,0.,-1.));
#19321=DIRECTION('ref_axis',(1.,0.,0.));
#19322=DIRECTION('center_axis',(0.,0.,1.));
#19323=DIRECTION('ref_axis',(1.,0.,0.));
#19324=DIRECTION('center_axis',(0.,0.,1.));
#19325=DIRECTION('ref_axis',(1.,0.,0.));
#57590=CARTESIAN_POINT('',(0.,0.,0.));
#57591=CARTESIAN_POINT('Origin',(0.,0.,0.));
#57592=CARTESIAN_POINT('',(-2.94501217978886,0.00210964666656384,0.322176117089595));
#57593=CARTESIAN_POINT('',(-2.94453553094506,0.00313791388557197,0.177823882910385));
#57594=CARTESIAN_POINT('',(-2.942,-3.60291088309151E-16,0.));
#57595=CARTESIAN_POINT('',(1.28892185405323,2.64462557919717,0.));
#57596=CARTESIAN_POINT('Ctrl Pts',(-2.94501217978886,0.00210964666656384,
0.322176117089595));
#57597=CARTESIAN_POINT('Ctrl Pts',(-2.94591259769569,0.121087549437314,
0.315720264862594));
#57598=CARTESIAN_POINT('Ctrl Pts',(-2.93932205372645,0.239959279025233,
0.309264412635592));
#57599=CARTESIAN_POINT('Ctrl Pts',(-2.92490373823147,0.357866546097276,
0.302808560408591));
#57600=CARTESIAN_POINT('Ctrl Pts',(-2.80727159362702,1.31981558202748,0.250138347790759));
#57601=CARTESIAN_POINT('Ctrl Pts',(-2.16861137772223,2.21756856383993,0.197468135172927));
#57602=CARTESIAN_POINT('Ctrl Pts',(-1.29846211955926,2.64493763974705,0.144797922555096));
#57603=CARTESIAN_POINT('Ctrl Pts',(-0.501074003123223,3.03657047660083,
0.0965319483700637));
#57604=CARTESIAN_POINT('Ctrl Pts',(0.490707930428614,3.03319661211455,0.048265974185032));
#57605=CARTESIAN_POINT('Ctrl Pts',(1.29200466145509,2.64817921559509,2.28251534084349E-16));
#57606=CARTESIAN_POINT('',(-1.2889218540533,2.64462557919714,0.));
#57607=CARTESIAN_POINT('Origin',(0.,0.,0.));
#57608=CARTESIAN_POINT('Ctrl Pts',(-1.2889218540533,2.64462557919714,3.2612801348364E-15));
#57609=CARTESIAN_POINT('Ctrl Pts',(-2.16412553195878,2.21807402646555,0.0526702126178337));
#57610=CARTESIAN_POINT('Ctrl Pts',(-2.80369899883776,1.32688596224183,0.105340425235664));
#57611=CARTESIAN_POINT('Ctrl Pts',(-2.92359275294276,0.366672953034089,
0.158010637853495));
#57612=CARTESIAN_POINT('Ctrl Pts',(-2.93862645170598,0.246270074362799,
0.164615052872458));
#57613=CARTESIAN_POINT('Ctrl Pts',(-2.94548916698122,0.12478190859667,0.171219467891421));
#57614=CARTESIAN_POINT('Ctrl Pts',(-2.94453553094506,0.00313791388557197,
0.177823882910385));
#57615=CARTESIAN_POINT('Origin',(0.,0.,0.));
#57616=CARTESIAN_POINT('',(-2.9374626214221,0.000758590818191462,1.3221761170896));
#57617=CARTESIAN_POINT('',(-2.93743561631178,0.000732401129134809,1.17782388291039));
#57618=CARTESIAN_POINT('',(-2.942,-3.60291088309151E-16,0.));
#57619=CARTESIAN_POINT('Ctrl Pts',(-2.9374626214221,0.000758590818191462,
1.3221761170896));
#57620=CARTESIAN_POINT('Ctrl Pts',(-2.93848585913829,0.441702582020672,
1.29840820723625));
#57621=CARTESIAN_POINT('Ctrl Pts',(-2.84537551923226,0.882235445407197,
1.2746402973829));
#57622=CARTESIAN_POINT('Ctrl Pts',(-2.65590902315621,1.27645657866303,1.25087238752956));
#57623=CARTESIAN_POINT('Ctrl Pts',(-2.23604708772076,2.15005930751655,1.19820217491173));
#57624=CARTESIAN_POINT('Ctrl Pts',(-1.34300379394444,2.79623653247501,1.1455319622939));
#57625=CARTESIAN_POINT('Ctrl Pts',(-0.381914565919547,2.92186465652728,
1.09286174967606));
#57626=CARTESIAN_POINT('Ctrl Pts',(0.579174662105351,3.04749278057955,1.04019153705823));
#57627=CARTESIAN_POINT('Ctrl Pts',(1.60830982437882,2.65257180372564,0.987521324440401));
#57628=CARTESIAN_POINT('Ctrl Pts',(2.23860403446081,1.91621978819862,0.93485111182257));
#57629=CARTESIAN_POINT('Ctrl Pts',(2.8688982445428,1.17986777267159,0.882180899204738));
#57630=CARTESIAN_POINT('Ctrl Pts',(3.1003515024333,0.102084718471448,0.829510686586907));
#57631=CARTESIAN_POINT('Ctrl Pts',(2.82797713905364,-0.828099512194974,
0.776840473969075));
#57632=CARTESIAN_POINT('Ctrl Pts',(2.55560277567399,-1.7582837428614,0.724170261351243));
#57633=CARTESIAN_POINT('Ctrl Pts',(1.77940079102417,-2.5408691499941,0.671500048733411));
#57634=CARTESIAN_POINT('Ctrl Pts',(0.851475992729512,-2.82098153902745,
0.61882983611558));
#57635=CARTESIAN_POINT('Ctrl Pts',(-0.0764488055651469,-3.1010939280608,
0.566159623497748));
#57636=CARTESIAN_POINT('Ctrl Pts',(-1.15609641750466,-2.8787332989948,0.513489410879917));
#57637=CARTESIAN_POINT('Ctrl Pts',(-1.89761818682235,-2.25448043943784,
0.460819198262086));
#57638=CARTESIAN_POINT('Ctrl Pts',(-2.54825072809468,-1.70674301456925,
0.414604837871256));
#57639=CARTESIAN_POINT('Ctrl Pts',(-2.93856651836649,-0.849596291427123,
0.368390477480426));
#57640=CARTESIAN_POINT('Ctrl Pts',(-2.94501217978886,0.00210964666656384,
0.322176117089595));
#57641=CARTESIAN_POINT('Ctrl Pts',(-2.94453553094506,0.00313791388557197,
0.177823882910385));
#57642=CARTESIAN_POINT('Ctrl Pts',(-2.93788391918254,-0.845329001562565,
0.223889680509253));
#57643=CARTESIAN_POINT('Ctrl Pts',(-2.55096188398631,-1.70137709351185,
0.269955478108122));
#57644=CARTESIAN_POINT('Ctrl Pts',(-1.90410965994752,-2.24960573227557,
0.31602127570699));
#57645=CARTESIAN_POINT('Ctrl Pts',(-1.16451877151628,-2.87643345418565,
0.368691488324821));
#57646=CARTESIAN_POINT('Ctrl Pts',(-0.0851229533228073,-3.10085094381401,
0.421361700942653));
#57647=CARTESIAN_POINT('Ctrl Pts',(0.843672564211012,-2.82310443536429,
0.474031913560484));
#57648=CARTESIAN_POINT('Ctrl Pts',(1.77246808174483,-2.54535792691456,0.526702126178316));
#57649=CARTESIAN_POINT('Ctrl Pts',(2.550663298619,-1.76544742038675,0.579372338796147));
#57650=CARTESIAN_POINT('Ctrl Pts',(2.82559485726556,-0.836148642972677,
0.632042551413979));
#57651=CARTESIAN_POINT('Ctrl Pts',(3.10052641591212,0.0931501344413926,
0.684712764031811));
#57652=CARTESIAN_POINT('Ctrl Pts',(2.87219431633107,1.17183718274172,0.737382976649643));
#57653=CARTESIAN_POINT('Ctrl Pts',(2.24398891012547,1.91001338469769,0.790053189267474));
#57654=CARTESIAN_POINT('Ctrl Pts',(1.61578350391986,2.64818958665366,0.842723401885306));
#57655=CARTESIAN_POINT('Ctrl Pts',(0.587704791089698,3.04585494226529,0.895393614503137));
#57656=CARTESIAN_POINT('Ctrl Pts',(-0.373745257291813,2.92288626672173,
0.948063827120969));
#57657=CARTESIAN_POINT('Ctrl Pts',(-1.33519530567332,2.79991759117817,1.0007340397388));
#57658=CARTESIAN_POINT('Ctrl Pts',(-2.23001668960618,2.15631488447943,1.05340425235663));
#57659=CARTESIAN_POINT('Ctrl Pts',(-2.65231672176365,1.28390825032342,1.10607446497446));
#57660=CARTESIAN_POINT('Ctrl Pts',(-2.84407458005236,0.887766135751567,
1.12999093761977));
#57661=CARTESIAN_POINT('Ctrl Pts',(-2.93840404300437,0.444447318126731,
1.15390741026508));
#57662=CARTESIAN_POINT('Ctrl Pts',(-2.93743561631178,0.000732401129134809,
1.17782388291039));
#57663=CARTESIAN_POINT('Origin',(0.,0.,0.));
#57664=CARTESIAN_POINT('',(-2.94237337112349,-0.00260076937561138,2.32217611708959));
#57665=CARTESIAN_POINT('',(-2.94245565671171,-0.00259425957205793,2.17782388291038));
#57666=CARTESIAN_POINT('',(-2.942,-3.60291088309151E-16,0.));
#57667=CARTESIAN_POINT('Ctrl Pts',(-2.94237337112349,-0.00260076937561138,
2.32217611708959));
#57668=CARTESIAN_POINT('Ctrl Pts',(-2.93547687785472,0.756299906403093,
2.28109614960991));
#57669=CARTESIAN_POINT('Ctrl Pts',(-2.63517458379537,1.52004621893047,2.24001618213022));
#57670=CARTESIAN_POINT('Ctrl Pts',(-2.10656451366312,2.06047930091946,2.19893621465053));
#57671=CARTESIAN_POINT('Ctrl Pts',(-1.4288131303506,2.75338942428174,2.1462660020327));
#57672=CARTESIAN_POINT('Ctrl Pts',(-0.375751290551719,3.07919952181725,
2.09359578941486));
#57673=CARTESIAN_POINT('Ctrl Pts',(0.57488733383408,2.89010251009112,2.04092557679703));
#57674=CARTESIAN_POINT('Ctrl Pts',(1.52552595821988,2.70100549836499,1.9882553641792));
#57675=CARTESIAN_POINT('Ctrl Pts',(2.3737413671926,1.99700137737721,1.93558515156137));
#57676=CARTESIAN_POINT('Ctrl Pts',(2.73473061221906,1.09746893276964,1.88291493894354));
#57677=CARTESIAN_POINT('Ctrl Pts',(3.09571985724552,0.197936488162073,1.83024472632571));
#57678=CARTESIAN_POINT('Ctrl Pts',(2.96948293832572,-0.897124280065286,
1.77757451370788));
#57679=CARTESIAN_POINT('Ctrl Pts',(2.41328900736074,-1.69092464359517,1.72490430109004));
#57680=CARTESIAN_POINT('Ctrl Pts',(1.85709507639575,-2.48472500712505,1.67223408847221));
#57681=CARTESIAN_POINT('Ctrl Pts',(0.870944133385572,-2.97726496595745,
1.61956387585438));
#57682=CARTESIAN_POINT('Ctrl Pts',(-0.0977855553122216,-2.94510122718995,
1.56689366323655));
#57683=CARTESIAN_POINT('Ctrl Pts',(-1.06651524401001,-2.91293748842246,
1.51422345061872));
#57684=CARTESIAN_POINT('Ctrl Pts',(-2.01782367839542,-2.35607005205505,
1.46155323800089));
#57685=CARTESIAN_POINT('Ctrl Pts',(-2.52013760704083,-1.52712221749706,
1.40888302538305));
#57686=CARTESIAN_POINT('Ctrl Pts',(-2.79577783188422,-1.07224459123419,
1.37998072261857));
#57687=CARTESIAN_POINT('Ctrl Pts',(-2.93621834178389,-0.535439030872177,
1.35107841985408));
#57688=CARTESIAN_POINT('Ctrl Pts',(-2.9374626214221,0.000758590818191462,
1.3221761170896));
#57689=CARTESIAN_POINT('Ctrl Pts',(-2.93743561631178,0.000732401129134809,
1.17782388291039));
#57690=CARTESIAN_POINT('Ctrl Pts',(-2.93627131881214,-0.532726839892435,
1.20657762288291));
#57691=CARTESIAN_POINT('Ctrl Pts',(-2.79736142917079,-1.06675861135357,
1.23533136285543));
#57692=CARTESIAN_POINT('Ctrl Pts',(-2.52440827067989,-1.5200691062172,1.26408510282796));
#57693=CARTESIAN_POINT('Ctrl Pts',(-2.02442110705658,-2.35042926698854,
1.31675531544579));
#57694=CARTESIAN_POINT('Ctrl Pts',(-1.07466809942789,-2.90993902691792,
1.36942552806362));
#57695=CARTESIAN_POINT('Ctrl Pts',(-0.10603039660911,-2.94481076457264,
1.42209574068145));
#57696=CARTESIAN_POINT('Ctrl Pts',(0.862607306209672,-2.97968250222737,
1.47476595329928));
#57697=CARTESIAN_POINT('Ctrl Pts',(1.85012970421854,-2.48991621760742,1.52743616591712));
#57698=CARTESIAN_POINT('Ctrl Pts',(2.40854344014417,-1.69767888635459,1.58010637853495));
#57699=CARTESIAN_POINT('Ctrl Pts',(2.96695717606981,-0.905441555101753,
1.63277659115278));
#57700=CARTESIAN_POINT('Ctrl Pts',(3.09626224991221,0.189266822783965,1.68544680377061));
#57701=CARTESIAN_POINT('Ctrl Pts',(2.73779389621599,1.08980795795695,1.73811701638844));
#57702=CARTESIAN_POINT('Ctrl Pts',(2.37932554251976,1.99034909312994,1.79078722900627));
#57703=CARTESIAN_POINT('Ctrl Pts',(1.53308376128489,2.6967229855902,1.8434574416241));
#57704=CARTESIAN_POINT('Ctrl Pts',(0.582978083752645,2.88848071032948,1.89612765424194));
#57705=CARTESIAN_POINT('Ctrl Pts',(-0.367127593779598,3.08023843506875,
1.94879786685977));
#57706=CARTESIAN_POINT('Ctrl Pts',(-1.42109716760921,2.75737999208705,2.0014680794776));
#57707=CARTESIAN_POINT('Ctrl Pts',(-2.10078617833213,2.06637082890199,2.05413829209543));
#57708=CARTESIAN_POINT('Ctrl Pts',(-2.63282464108198,1.5254713187922,2.09536682236708));
#57709=CARTESIAN_POINT('Ctrl Pts',(-2.93553206539509,0.758996677917738,
2.13659535263873));
#57710=CARTESIAN_POINT('Ctrl Pts',(-2.94245565671171,-0.00259425957205793,
2.17782388291038));
#57711=CARTESIAN_POINT('Origin',(0.,0.,0.));
#57712=CARTESIAN_POINT('',(-2.94537017639144,0.00174029209860913,3.3221761170896));
#57713=CARTESIAN_POINT('',(-2.94530715728325,0.00177620926833399,3.17782388291039));
#57714=CARTESIAN_POINT('',(-2.942,-3.60291088309151E-16,0.));
#57715=CARTESIAN_POINT('Ctrl Pts',(-2.94537017639144,0.00174029209860913,
3.3221761170896));
#57716=CARTESIAN_POINT('Ctrl Pts',(-2.94611224026602,0.107164636136391,
3.31645430460139));
#57717=CARTESIAN_POINT('Ctrl Pts',(-2.94093746113258,0.212515376889504,
3.31073249211319));
#57718=CARTESIAN_POINT('Ctrl Pts',(-2.9296029501889,0.317199180230514,3.30501067962499));
#57719=CARTESIAN_POINT('Ctrl Pts',(-2.82526693733401,1.28083058041764,3.25234046700716));
#57720=CARTESIAN_POINT('Ctrl Pts',(-2.19898596937906,2.18794903031096,3.19967025438933));
#57721=CARTESIAN_POINT('Ctrl Pts',(-1.33487969482344,2.62702968627763,3.1470000417715));
#57722=CARTESIAN_POINT('Ctrl Pts',(-0.470773420267829,3.06611034224429,
3.09432982915367));
#57723=CARTESIAN_POINT('Ctrl Pts',(0.631158160888449,3.03715320428431,3.04165961653583));
#57724=CARTESIAN_POINT('Ctrl Pts',(1.47101096812166,2.55329502437494,2.988989403918));
#57725=CARTESIAN_POINT('Ctrl Pts',(2.31086377535488,2.06943684446558,2.93631919130017));
#57726=CARTESIAN_POINT('Ctrl Pts',(2.88863780866502,1.13067762260682,2.88364897868234));
#57727=CARTESIAN_POINT('Ctrl Pts',(2.94221915242109,0.162896383790171,2.83097876606451));
#57728=CARTESIAN_POINT('Ctrl Pts',(2.99580049617715,-0.804884855026484,
2.77830855344668));
#57729=CARTESIAN_POINT('Ctrl Pts',(2.52518915037914,-1.80168811080104,2.72563834082884));
#57730=CARTESIAN_POINT('Ctrl Pts',(1.74388343367472,-2.37530195478797,2.67296812821101));
#57731=CARTESIAN_POINT('Ctrl Pts',(0.962577716970292,-2.94891579877489,
2.62029791559318));
#57732=CARTESIAN_POINT('Ctrl Pts',(-0.129422370640539,-3.09934023097417,
2.56762770297535));
#57733=CARTESIAN_POINT('Ctrl Pts',(-1.03671829650871,-2.75833352334838,
2.51495749035752));
#57734=CARTESIAN_POINT('Ctrl Pts',(-1.94401422237688,-2.4173268157226,2.46228727773969));
#57735=CARTESIAN_POINT('Ctrl Pts',(-2.66660598650239,-1.58488896827175,
2.40961706512185));
#57736=CARTESIAN_POINT('Ctrl Pts',(-2.87668140515208,-0.638664969951807,
2.35694685250402));
#57737=CARTESIAN_POINT('Ctrl Pts',(-2.92290915853737,-0.430445417551361,
2.34535660736588));
#57738=CARTESIAN_POINT('Ctrl Pts',(-2.94431913818423,-0.216715955131923,
2.33376636222774));
#57739=CARTESIAN_POINT('Ctrl Pts',(-2.94237337112349,-0.00260076937561138,
2.32217611708959));
#57740=CARTESIAN_POINT('Ctrl Pts',(-2.94245565671171,-0.00259425957205793,
2.17782388291038));
#57741=CARTESIAN_POINT('Ctrl Pts',(-2.94437708180297,-0.213949879747532,
2.18926556525656));
#57742=CARTESIAN_POINT('Ctrl Pts',(-2.92351825621533,-0.424929373931882,
2.20070724760275));
#57743=CARTESIAN_POINT('Ctrl Pts',(-2.87845884965989,-0.630607025085498,
2.21214892994893));
#57744=CARTESIAN_POINT('Ctrl Pts',(-2.67103406264848,-1.57741583249951,
2.26481914256676));
#57745=CARTESIAN_POINT('Ctrl Pts',(-1.95077604100943,-2.4118735639391,2.31748935518459));
#57746=CARTESIAN_POINT('Ctrl Pts',(-1.04443851765628,-2.75541959458595,
2.37015956780242));
#57747=CARTESIAN_POINT('Ctrl Pts',(-0.138100994303129,-3.0989656252328,
2.42282978042025));
#57748=CARTESIAN_POINT('Ctrl Pts',(0.954316030764116,-2.95159995508691,
2.47549999303808));
#57749=CARTESIAN_POINT('Ctrl Pts',(1.73722502222407,-2.38017629855023,2.52817020565592));
#57750=CARTESIAN_POINT('Ctrl Pts',(2.52013401368403,-1.80875264201355,2.58084041827375));
#57751=CARTESIAN_POINT('Ctrl Pts',(2.9935349715367,-0.81327099908608,2.63351063089158));
#57752=CARTESIAN_POINT('Ctrl Pts',(2.94266396081319,0.154656572499768,2.68618084350941));
#57753=CARTESIAN_POINT('Ctrl Pts',(2.89179295008968,1.12258414408561,2.73885105612724));
#57754=CARTESIAN_POINT('Ctrl Pts',(2.31664997079,2.06295764432982,2.79152126874507));
#57755=CARTESIAN_POINT('Ctrl Pts',(1.47815537025573,2.54916581364531,2.8441914813629));
#57756=CARTESIAN_POINT('Ctrl Pts',(0.639660769721456,3.03537398296079,2.89686169398074));
#57757=CARTESIAN_POINT('Ctrl Pts',(-0.462185452047399,3.06741682134755,
2.94953190659857));
#57758=CARTESIAN_POINT('Ctrl Pts',(-1.32751795973283,2.63075765975438,3.0022021192164));
#57759=CARTESIAN_POINT('Ctrl Pts',(-2.19285046741827,2.19409849816122,3.05487233183423));
#57760=CARTESIAN_POINT('Ctrl Pts',(-2.82166926102029,1.28873733658814,3.10754254445206));
#57761=CARTESIAN_POINT('Ctrl Pts',(-2.92870336695306,0.325401832213201,
3.1602127570699));
#57762=CARTESIAN_POINT('Ctrl Pts',(-2.94063288723355,0.218032967530236,
3.16608313235006));
#57763=CARTESIAN_POINT('Ctrl Pts',(-2.9460806479325,0.109943928873562,3.17195350763022));
#57764=CARTESIAN_POINT('Ctrl Pts',(-2.94530715728325,0.00177620926833399,
3.17782388291039));
#57765=CARTESIAN_POINT('Origin',(0.,0.,0.));
#57766=CARTESIAN_POINT('',(-2.93758307183925,0.000962932756501389,4.32217611708959));
#57767=CARTESIAN_POINT('',(-2.93755662075233,0.00092146372069949,4.17782388291039));
#57768=CARTESIAN_POINT('',(-2.942,-3.60291088309151E-16,0.));
#57769=CARTESIAN_POINT('Ctrl Pts',(-2.93758307183925,0.000962932756501389,
4.32217611708959));
#57770=CARTESIAN_POINT('Ctrl Pts',(-2.93884998778206,0.428244162000401,
4.29914224697505));
#57771=CARTESIAN_POINT('Ctrl Pts',(-2.85162805316606,0.855032782237186,
4.2761083768605));
#57772=CARTESIAN_POINT('Ctrl Pts',(-2.67331627298244,1.23958415202432,4.25307450674596));
#57773=CARTESIAN_POINT('Ctrl Pts',(-2.26558108441747,2.11891542846389,4.20040429412813));
#57774=CARTESIAN_POINT('Ctrl Pts',(-1.38156157854408,2.77739947577446,4.1477340815103));
#57775=CARTESIAN_POINT('Ctrl Pts',(-0.422303489371249,2.91630734463971,
4.09506386889247));
#57776=CARTESIAN_POINT('Ctrl Pts',(0.536954599801574,3.05521521350496,4.04239365627464));
#57777=CARTESIAN_POINT('Ctrl Pts',(1.57145127227383,2.6745469039249,3.9897234436568));
#57778=CARTESIAN_POINT('Ctrl Pts',(2.21187507673207,1.94699702363172,3.93705323103897));
#57779=CARTESIAN_POINT('Ctrl Pts',(2.8522988811903,1.21944714333852,3.88438301842114));
#57780=CARTESIAN_POINT('Ctrl Pts',(3.0986498176345,0.145015692332194,3.83171280580331));
#57781=CARTESIAN_POINT('Ctrl Pts',(2.83916791750172,-0.788869001505497,
3.77904259318548));
#57782=CARTESIAN_POINT('Ctrl Pts',(2.57968601736894,-1.72275369534319,3.72637238056765));
#57783=CARTESIAN_POINT('Ctrl Pts',(1.81437128065917,-2.51609163201224,3.67370216794981));
#57784=CARTESIAN_POINT('Ctrl Pts',(0.890417641887139,-2.80897582571963,
3.62103195533198));
#57785=CARTESIAN_POINT('Ctrl Pts',(-0.0335359968848904,-3.10186001942701,
3.56836174271415));
#57786=CARTESIAN_POINT('Ctrl Pts',(-1.11612853771918,-2.89429047017273,
3.51569153009632));
#57787=CARTESIAN_POINT('Ctrl Pts',(-1.86622927925891,-2.28043352030513,
3.46302131747849));
#57788=CARTESIAN_POINT('Ctrl Pts',(-2.53484305545271,-1.73326273301688,
3.41607291734886));
#57789=CARTESIAN_POINT('Ctrl Pts',(-2.93928142186174,-0.863283561356046,
3.36912451721922));
#57790=CARTESIAN_POINT('Ctrl Pts',(-2.94537017639144,0.00174029209860913,
3.3221761170896));
#57791=CARTESIAN_POINT('Ctrl Pts',(-2.94530715728325,0.00177620926833399,
3.17782388291039));
#57792=CARTESIAN_POINT('Ctrl Pts',(-2.93914073097497,-0.860559065925464,
3.22462372024805));
#57793=CARTESIAN_POINT('Ctrl Pts',(-2.53757609018917,-1.72789499208641,
3.27142355758572));
#57794=CARTESIAN_POINT('Ctrl Pts',(-1.87260805478389,-2.27519863184659,
3.31822339492339));
#57795=CARTESIAN_POINT('Ctrl Pts',(-1.1242292184184,-2.89115374435464,3.37089360754122));
#57796=CARTESIAN_POINT('Ctrl Pts',(-0.0422221274238752,-3.10175412219396,
3.42356382015905));
#57797=CARTESIAN_POINT('Ctrl Pts',(0.882548115976509,-2.81145844473756,
3.47623403277689));
#57798=CARTESIAN_POINT('Ctrl Pts',(1.80731835937689,-2.52116276728116,3.52890424539472));
#57799=CARTESIAN_POINT('Ctrl Pts',(2.57485175518313,-1.72997103452906,3.58157445801255));
#57800=CARTESIAN_POINT('Ctrl Pts',(2.83694784679655,-0.796816585890936,
3.63424467063038));
#57801=CARTESIAN_POINT('Ctrl Pts',(3.09904393840998,0.136337862747188,3.68691488324821));
#57802=CARTESIAN_POINT('Ctrl Pts',(2.85570272583058,1.21145502727133,3.73958509586604));
#57803=CARTESIAN_POINT('Ctrl Pts',(2.21731878219618,1.9407954999751,3.79225530848387));
#57804=CARTESIAN_POINT('Ctrl Pts',(1.57893483856177,2.67013597267886,3.84492552110171));
#57805=CARTESIAN_POINT('Ctrl Pts',(0.545508163872345,3.05369975356224,3.89759573371954));
#57806=CARTESIAN_POINT('Ctrl Pts',(-0.414135207932496,2.91747866955439,
3.95026594633737));
#57807=CARTESIAN_POINT('Ctrl Pts',(-1.37377857973734,2.78125758554654,4.0029361589552));
#57808=CARTESIAN_POINT('Ctrl Pts',(-2.2596386486576,2.12525163664746,4.05560637157303));
#57809=CARTESIAN_POINT('Ctrl Pts',(-2.66983468761848,1.24706555457053,4.10827658419087));
#57810=CARTESIAN_POINT('Ctrl Pts',(-2.85037966131594,0.860537972559507,
4.13145901709737));
#57811=CARTESIAN_POINT('Ctrl Pts',(-2.93877615178763,0.430968325170985,
4.15464145000388));
#57812=CARTESIAN_POINT('Ctrl Pts',(-2.93755662075233,0.00092146372069949,
4.17782388291039));
#57813=CARTESIAN_POINT('Origin',(0.,0.,0.));
#57814=CARTESIAN_POINT('',(-2.94196835289677,-0.002621025841609,5.32217611708959));
#57815=CARTESIAN_POINT('',(-2.94205032665991,-0.00261853614193573,5.17782388291038));
#57816=CARTESIAN_POINT('',(-2.942,-3.60291088309151E-16,0.));
#57817=CARTESIAN_POINT('Ctrl Pts',(-2.94196835289677,-0.002621025841609,
5.32217611708959));
#57818=CARTESIAN_POINT('Ctrl Pts',(-2.93523282994335,0.742982230700457,
5.2818301893487));
#57819=CARTESIAN_POINT('Ctrl Pts',(-2.64664255795984,1.49322716005967,5.24148426160782));
#57820=CARTESIAN_POINT('Ctrl Pts',(-2.13487143198777,2.03113582368275,5.20113833386693));
#57821=CARTESIAN_POINT('Ctrl Pts',(-1.46677193531172,2.73335697135233,5.1484681212491));
#57822=CARTESIAN_POINT('Ctrl Pts',(-0.41831872112528,3.07370618157001,5.09579790863126));
#57823=CARTESIAN_POINT('Ctrl Pts',(0.534845211695748,2.89778007531554,5.04312769601343));
#57824=CARTESIAN_POINT('Ctrl Pts',(1.48800914451678,2.72185396906108,4.9904574833956));
#57825=CARTESIAN_POINT('Ctrl Pts',(2.34588379597239,2.02965254633447,4.93778727077777));
#57826=CARTESIAN_POINT('Ctrl Pts',(2.71928434946264,1.13520103599745,4.88511705815994));
#57827=CARTESIAN_POINT('Ctrl Pts',(3.09268490295289,0.240749525660442,4.83244684554211));
#57828=CARTESIAN_POINT('Ctrl Pts',(2.98161135847777,-0.855952072286972,
4.77977663292428));
#57829=CARTESIAN_POINT('Ctrl Pts',(2.43645352177545,-1.65737231833663,4.72710642030644));
#57830=CARTESIAN_POINT('Ctrl Pts',(1.89129568507313,-2.4587925643863,4.67443620768861));
#57831=CARTESIAN_POINT('Ctrl Pts',(0.912053556143593,-2.9649314585382,4.62176599507078));
#57832=CARTESIAN_POINT('Ctrl Pts',(-0.0570282802002683,-2.94617320275787,
4.56909578245295));
#57833=CARTESIAN_POINT('Ctrl Pts',(-1.02611011654413,-2.92741494697754,
4.51642556983512));
#57834=CARTESIAN_POINT('Ctrl Pts',(-1.98503166030232,-2.38375954126497,
4.46375535721729));
#57835=CARTESIAN_POINT('Ctrl Pts',(-2.49876699655314,-1.5618425856244,4.41108514459945));
#57836=CARTESIAN_POINT('Ctrl Pts',(-2.78783430090679,-1.09936842431115,
4.38144880209617));
#57837=CARTESIAN_POINT('Ctrl Pts',(-2.93595300469825,-0.548795001629907,
4.35181245959288));
#57838=CARTESIAN_POINT('Ctrl Pts',(-2.93758307183925,0.000962932756501389,
4.32217611708959));
#57839=CARTESIAN_POINT('Ctrl Pts',(-2.93755662075233,0.00092146372069949,
4.17782388291039));
#57840=CARTESIAN_POINT('Ctrl Pts',(-2.93600539173918,-0.54609304364936,
4.20731166262171));
#57841=CARTESIAN_POINT('Ctrl Pts',(-2.78945957767235,-1.09387966133746,
4.23679944233303));
#57842=CARTESIAN_POINT('Ctrl Pts',(-2.50313103055653,-1.55483915575367,
4.26628722204436));
#57843=CARTESIAN_POINT('Ctrl Pts',(-1.99169932553219,-2.37819156874617,
4.31895743466219));
#57844=CARTESIAN_POINT('Ctrl Pts',(-1.034303906482,-2.92453017947639,4.37162764728002));
#57845=CARTESIAN_POINT('Ctrl Pts',(-0.065278344036315,-2.94600212060899,
4.42429785989785));
#57846=CARTESIAN_POINT('Ctrl Pts',(0.903747218409357,-2.96747406174159,
4.47696807251569));
#57847=CARTESIAN_POINT('Ctrl Pts',(1.88440292425052,-2.46407933327658,4.52963828513352));
#57848=CARTESIAN_POINT('Ctrl Pts',(2.43180290302967,-1.6641888106397,4.58230849775135));
#57849=CARTESIAN_POINT('Ctrl Pts',(2.97920288180883,-0.864298288002814,
4.63497871036918));
#57850=CARTESIAN_POINT('Ctrl Pts',(3.09334713352597,0.232088028805956,4.68764892298701));
#57851=CARTESIAN_POINT('Ctrl Pts',(2.72245279039328,1.12758173127816,4.74031913560485));
#57852=CARTESIAN_POINT('Ctrl Pts',(2.35155844726061,2.02307543375035,4.79298934822268));
#57853=CARTESIAN_POINT('Ctrl Pts',(1.49562550927813,2.71767652188598,4.8456595608405));
#57854=CARTESIAN_POINT('Ctrl Pts',(0.542957912128918,2.89627113066901,4.89832977345833));
#57855=CARTESIAN_POINT('Ctrl Pts',(-0.409709685020296,3.07486573945205,
4.95099998607617));
#57856=CARTESIAN_POINT('Ctrl Pts',(-1.45911194133625,2.73745386888248,5.003670198694));
#57857=CARTESIAN_POINT('Ctrl Pts',(-2.12917531393477,2.0371063396864,5.05634041131183));
#57858=CARTESIAN_POINT('Ctrl Pts',(-2.64434078507083,1.49865747112924,5.09683490184468));
#57859=CARTESIAN_POINT('Ctrl Pts',(-2.93527864115445,0.745676951205884,
5.13732939237753));
#57860=CARTESIAN_POINT('Ctrl Pts',(-2.94205032665991,-0.00261853614193573,
5.17782388291038));
#57861=CARTESIAN_POINT('Origin',(0.,0.,0.));
#57862=CARTESIAN_POINT('',(-2.94566657928398,0.00155368773417593,6.3221761170896));
#57863=CARTESIAN_POINT('',(-2.94560897709112,0.00159264369063789,6.17782388291039));
#57864=CARTESIAN_POINT('',(-2.942,-3.60291088309151E-16,0.));
#57865=CARTESIAN_POINT('Ctrl Pts',(-2.94566657928398,0.00155368773417593,
6.3221761170896));
#57866=CARTESIAN_POINT('Ctrl Pts',(-2.94625783004801,0.0934289955880153,
6.3171883443402));
#57867=CARTESIAN_POINT('Ctrl Pts',(-2.94232816000304,0.185253079238273,
6.31220057159079));
#57868=CARTESIAN_POINT('Ctrl Pts',(-2.93371125763113,0.276635178916858,
6.30721279884139));
#57869=CARTESIAN_POINT('Ctrl Pts',(-2.8427179219604,1.24161791998335,6.25454258622356));
#57870=CARTESIAN_POINT('Ctrl Pts',(-2.22904768583453,2.15731468667283,6.20187237360573));
#57871=CARTESIAN_POINT('Ctrl Pts',(-1.37109919163641,2.60830898707571,6.1492021609879));
#57872=CARTESIAN_POINT('Ctrl Pts',(-0.513150697438283,3.05930328747859,
6.09653194837006));
#57873=CARTESIAN_POINT('Ctrl Pts',(0.589076054832107,3.04559512159484,6.04386173575223));
#57874=CARTESIAN_POINT('Ctrl Pts',(1.43554307511773,2.57340335836564,5.9911915231344));
#57875=CARTESIAN_POINT('Ctrl Pts',(2.28201009540335,2.10121159513645,5.93852131051657));
#57876=CARTESIAN_POINT('Ctrl Pts',(2.87271738370421,1.17053623456181,5.88585109789874));
#57877=CARTESIAN_POINT('Ctrl Pts',(2.93968370608133,0.203588981936339,5.83318088528091));
#57878=CARTESIAN_POINT('Ctrl Pts',(3.00665002845845,-0.763358270689132,
5.78051067266308));
#57879=CARTESIAN_POINT('Ctrl Pts',(2.54987538491182,-1.76657741536544,5.72784046004524));
#57880=CARTESIAN_POINT('Ctrl Pts',(1.77658090684437,-2.35094641512771,5.67517024742741));
#57881=CARTESIAN_POINT('Ctrl Pts',(1.00328642877692,-2.93531541488997,5.62250003480958));
#57882=CARTESIAN_POINT('Ctrl Pts',(-0.0865278838113344,-3.1008342697382,
5.56982982219175));
#57883=CARTESIAN_POINT('Ctrl Pts',(-0.998455088538058,-2.77241342543621,
5.51715960957392));
#57884=CARTESIAN_POINT('Ctrl Pts',(-1.91038229326477,-2.44399258113422,
5.46448939695609));
#57885=CARTESIAN_POINT('Ctrl Pts',(-2.64442239012996,-1.621632037682,5.41181918433825));
#57886=CARTESIAN_POINT('Ctrl Pts',(-2.86756954897972,-0.67840522339516,
5.35914897172042));
#57887=CARTESIAN_POINT('Ctrl Pts',(-2.91978367568354,-0.457699906574275,
5.34682468684348));
#57888=CARTESIAN_POINT('Ctrl Pts',(-2.94402582209679,-0.230377021386298,
5.33450040196653));
#57889=CARTESIAN_POINT('Ctrl Pts',(-2.94196835289677,-0.002621025841609,
5.32217611708959));
#57890=CARTESIAN_POINT('Ctrl Pts',(-2.94205032665991,-0.00261853614193573,
5.17782388291038));
#57891=CARTESIAN_POINT('Ctrl Pts',(-2.94408641007957,-0.227613042098249,
5.18999960499536));
#57892=CARTESIAN_POINT('Ctrl Pts',(-2.92043214775034,-0.452183992687412,
5.20217532708034));
#57893=CARTESIAN_POINT('Ctrl Pts',(-2.86945823375718,-0.670372434833386,
5.21435104916532));
#57894=CARTESIAN_POINT('Ctrl Pts',(-2.64895329209997,-1.61422049233453,
5.26702126178316));
#57895=CARTESIAN_POINT('Ctrl Pts',(-1.91721891990443,-2.43863341951423,
5.31969147440099));
#57896=CARTESIAN_POINT('Ctrl Pts',(-1.00621492850077,-2.76960670029717,
5.37236168701883));
#57897=CARTESIAN_POINT('Ctrl Pts',(-0.0952109370971131,-3.1005799810801,
5.42503189963666));
#57898=CARTESIAN_POINT('Ctrl Pts',(0.995062673514658,-2.93811361546629,
5.47770211225449));
#57899=CARTESIAN_POINT('Ctrl Pts',(1.76999059505944,-2.35591236043814,5.53037232487231));
#57900=CARTESIAN_POINT('Ctrl Pts',(2.54491851660422,-1.77371110540999,5.58304253749014));
#57901=CARTESIAN_POINT('Ctrl Pts',(3.00450074908201,-0.77177496096749,5.63571275010798));
#57902=CARTESIAN_POINT('Ctrl Pts',(2.94024246570664,0.195356083908528,5.68838296272581));
#57903=CARTESIAN_POINT('Ctrl Pts',(2.87598418233127,1.16248712878457,5.74105317534364));
#57904=CARTESIAN_POINT('Ctrl Pts',(2.28788538310274,2.09481307409411,5.79372338796148));
#57905=CARTESIAN_POINT('Ctrl Pts',(1.44274393054363,2.56937340757336,5.84639360057931));
#57906=CARTESIAN_POINT('Ctrl Pts',(0.597602477984537,3.0439337410526,5.89906381319714));
#57907=CARTESIAN_POINT('Ctrl Pts',(-0.504581627905147,3.06072846270153,
5.95173402581497));
#57908=CARTESIAN_POINT('Ctrl Pts',(-1.36378974409505,2.61213845164572,6.0044042384328));
#57909=CARTESIAN_POINT('Ctrl Pts',(-2.22299786028497,2.1635484405899,6.05707445105063));
#57910=CARTESIAN_POINT('Ctrl Pts',(-2.83922998677511,1.24957369682933,6.10974466366847));
#57911=CARTESIAN_POINT('Ctrl Pts',(-2.93292524981251,0.284849496536871,
6.1624148762863));
#57912=CARTESIAN_POINT('Ctrl Pts',(-2.94206229873784,0.190770757316082,
6.16755121182766));
#57913=CARTESIAN_POINT('Ctrl Pts',(-2.94623006655259,0.0962093950817709,
6.17268754736903));
#57914=CARTESIAN_POINT('Ctrl Pts',(-2.94560897709112,0.00159264369063789,
6.17782388291039));
#57915=CARTESIAN_POINT('Origin',(0.,0.,0.));
#57916=CARTESIAN_POINT('',(-2.93773181355748,0.00116367510156062,7.3221761170896));
#57917=CARTESIAN_POINT('',(-2.93769958596831,0.00112364184895479,7.17782388291039));
#57918=CARTESIAN_POINT('',(-2.942,-3.60291088309151E-16,0.));
#57919=CARTESIAN_POINT('Ctrl Pts',(-2.93773181355748,0.00116367510156062,
7.3221761170896));
#57920=CARTESIAN_POINT('Ctrl Pts',(-2.93921846510379,0.414775956166668,
7.29987628671385));
#57921=CARTESIAN_POINT('Ctrl Pts',(-2.85767291508901,0.827828420512208,
7.2775764563381));
#57922=CARTESIAN_POINT('Ctrl Pts',(-2.69021112169706,1.20247781104825,7.25527662596236));
#57923=CARTESIAN_POINT('Ctrl Pts',(-2.29468128516027,2.08736629334525,7.20260641334453));
#57924=CARTESIAN_POINT('Ctrl Pts',(-1.4198571053233,2.75801849948865,7.14993620072669));
#57925=CARTESIAN_POINT('Ctrl Pts',(-0.462612749536846,2.91018525343868,
7.09726598810886));
#57926=CARTESIAN_POINT('Ctrl Pts',(0.494631606249605,3.0623520073887,7.04459577549103));
#57927=CARTESIAN_POINT('Ctrl Pts',(1.53429613798554,2.69603330914537,6.9919255628732));
#57928=CARTESIAN_POINT('Ctrl Pts',(2.18472493484141,1.97741389811242,6.93925535025537));
#57929=CARTESIAN_POINT('Ctrl Pts',(2.83515373169728,1.25879448707948,6.88658513763754));
#57930=CARTESIAN_POINT('Ctrl Pts',(3.09634679367307,0.187874363256921,6.83391492501971));
#57931=CARTESIAN_POINT('Ctrl Pts',(2.84981084934511,-0.749511099531479,
6.78124471240188));
#57932=CARTESIAN_POINT('Ctrl Pts',(2.60327490501715,-1.68689656231988,6.72857449978404));
#57933=CARTESIAN_POINT('Ctrl Pts',(1.84900995438544,-2.49074736407413,6.67590428716621));
#57934=CARTESIAN_POINT('Ctrl Pts',(0.929197067821797,-2.79638723615263,
6.62323407454838));
#57935=CARTESIAN_POINT('Ctrl Pts',(0.00938418125816035,-3.10202710823113,
6.57056386193055));
#57936=CARTESIAN_POINT('Ctrl Pts',(-1.07597664123741,-2.90945605063389,
6.51789364931272));
#57937=CARTESIAN_POINT('Ctrl Pts',(-1.83449883487741,-2.30603616411352,
6.46522343669488));
#57938=CARTESIAN_POINT('Ctrl Pts',(-2.52119036486117,-1.75975903659949,
6.41754099682645));
#57939=CARTESIAN_POINT('Ctrl Pts',(-2.94001430111904,-0.87676195779301,
6.36985855695803));
#57940=CARTESIAN_POINT('Ctrl Pts',(-2.94566657928398,0.00155368773417593,
6.3221761170896));
#57941=CARTESIAN_POINT('Ctrl Pts',(-2.94560897709112,0.00159264369063789,
6.17782388291039));
#57942=CARTESIAN_POINT('Ctrl Pts',(-2.93986114580615,-0.87403181537772,
6.22535775998686));
#57943=CARTESIAN_POINT('Ctrl Pts',(-2.52397381508728,-1.75440005354465,
6.27289163706332));
#57944=CARTESIAN_POINT('Ctrl Pts',(-1.84094942996504,-2.30089003495964,
6.32042551413979));
#57945=CARTESIAN_POINT('Ctrl Pts',(-1.08411994749553,-2.90643170933934,
6.37309572675762));
#57946=CARTESIAN_POINT('Ctrl Pts',(0.000697417028111963,-3.10204140127437,
6.42576593937545));
#57947=CARTESIAN_POINT('Ctrl Pts',(0.921362644850236,-2.79897849819174,
6.47843615199329));
#57948=CARTESIAN_POINT('Ctrl Pts',(1.84202787267235,-2.49591559510911,6.53110636461112));
#57949=CARTESIAN_POINT('Ctrl Pts',(2.59854096379293,-1.69418009700883,6.58377657722895));
#57950=CARTESIAN_POINT('Ctrl Pts',(2.84770095275134,-0.757488640419289,
6.63644678984678));
#57951=CARTESIAN_POINT('Ctrl Pts',(3.09686094170975,0.179202816170267,6.68911700246461));
#57952=CARTESIAN_POINT('Ctrl Pts',(2.83866782850598,1.25085023124908,6.74178721508244));
#57953=CARTESIAN_POINT('Ctrl Pts',(2.19025392290029,1.9712882868533,6.79445742770027));
#57954=CARTESIAN_POINT('Ctrl Pts',(1.5418400172946,2.69172634245752,6.8471276403181));
#57955=CARTESIAN_POINT('Ctrl Pts',(0.50320531928699,3.06095503858714,6.89979785293594));
#57956=CARTESIAN_POINT('Ctrl Pts',(-0.454461456345466,2.91146948144086,
6.95246806555377));
#57957=CARTESIAN_POINT('Ctrl Pts',(-1.41212823197794,2.76198392429457,7.0051382781716));
#57958=CARTESIAN_POINT('Ctrl Pts',(-2.28882708523526,2.09378411387235,7.05780849078943));
#57959=CARTESIAN_POINT('Ctrl Pts',(-2.68683338135866,1.21000666836259,7.11047870340727));
#57960=CARTESIAN_POINT('Ctrl Pts',(-2.85646629860981,0.833334872607608,
7.13292709657497));
#57961=CARTESIAN_POINT('Ctrl Pts',(-2.93914371675611,0.417502950847913,
7.15537548974268));
#57962=CARTESIAN_POINT('Ctrl Pts',(-2.93769958596831,0.00112364184895479,
7.17782388291039));
#57963=CARTESIAN_POINT('Origin',(0.,0.,0.));
#57964=CARTESIAN_POINT('',(-2.94156648412342,-0.00262140296731356,8.3221761170896));
#57965=CARTESIAN_POINT('',(-2.94164760189786,-0.00262292145090667,8.17782388291039));
#57966=CARTESIAN_POINT('',(-2.942,-3.60291088309151E-16,0.));
#57967=CARTESIAN_POINT('Ctrl Pts',(-2.94156648412342,-0.00262140296731356,
8.3221761170896));
#57968=CARTESIAN_POINT('Ctrl Pts',(-2.93503453701149,0.72967238878934,8.28256422908751));
#57969=CARTESIAN_POINT('Ctrl Pts',(-2.65787464556332,1.46638000617809,8.24295234108542));
#57970=CARTESIAN_POINT('Ctrl Pts',(-2.16276963608865,2.00140357413964,8.20334045308333));
#57971=CARTESIAN_POINT('Ctrl Pts',(-1.50444993883493,2.7128012504786,8.15067024046549));
#57972=CARTESIAN_POINT('Ctrl Pts',(-0.46080611438605,3.06762415690109,8.09800002784767));
#57973=CARTESIAN_POINT('Ctrl Pts',(0.494700673992003,2.90490275371101,8.04532981522984));
#57974=CARTESIAN_POINT('Ctrl Pts',(1.45020746237007,2.74218135052094,7.99265960261201));
#57975=CARTESIAN_POINT('Ctrl Pts',(2.31757721467732,2.06191563771829,7.93998938999417));
#57976=CARTESIAN_POINT('Ctrl Pts',(2.70331755134067,1.17271607048742,7.88731917737634));
#57977=CARTESIAN_POINT('Ctrl Pts',(3.08905788800402,0.283516503256563,7.8346489647585));
#57978=CARTESIAN_POINT('Ctrl Pts',(2.99316880902349,-0.814616918402493,
7.78197875214068));
#57979=CARTESIAN_POINT('Ctrl Pts',(2.45915151070291,-1.62350319148857,7.72930853952285));
#57980=CARTESIAN_POINT('Ctrl Pts',(1.92513421238232,-2.43238946457466,7.67663832690502));
#57981=CARTESIAN_POINT('Ctrl Pts',(0.952988694721666,-2.95202858908774,
7.62396811428717));
#57982=CARTESIAN_POINT('Ctrl Pts',(-0.0162599177366882,-2.9466802304358,
7.57129790166934));
#57983=CARTESIAN_POINT('Ctrl Pts',(-0.985508530195028,-2.94133187178385,
7.51862768905151));
#57984=CARTESIAN_POINT('Ctrl Pts',(-1.95186023745108,-2.41099602996689,
7.46595747643369));
#57985=CARTESIAN_POINT('Ctrl Pts',(-2.47691834446078,-1.59626572983311,
7.41328726381586));
#57986=CARTESIAN_POINT('Ctrl Pts',(-2.77967420240452,-1.12648082847323,
7.38291688157377));
#57987=CARTESIAN_POINT('Ctrl Pts',(-2.93570712659971,-0.562139402290024,
7.35254649933169));
#57988=CARTESIAN_POINT('Ctrl Pts',(-2.93773181355748,0.00116367510156062,
7.3221761170896));
#57989=CARTESIAN_POINT('Ctrl Pts',(-2.93769958596831,0.00112364184895479,
7.17782388291039));
#57990=CARTESIAN_POINT('Ctrl Pts',(-2.93575538178383,-0.559439432992209,
7.20804570236051));
#57991=CARTESIAN_POINT('Ctrl Pts',(-2.78134344073081,-1.12099463047756,
7.23826752181064));
#57992=CARTESIAN_POINT('Ctrl Pts',(-2.48137885938122,-1.58932335063733,
7.26848934126076));
#57993=CARTESIAN_POINT('Ctrl Pts',(-1.95860430229089,-2.40552084353022,
7.32115955387859));
#57994=CARTESIAN_POINT('Ctrl Pts',(-0.993741449120738,-2.93856074871869,
7.37382976649642));
#57995=CARTESIAN_POINT('Ctrl Pts',(-0.0245115589366341,-2.94662331154554,
7.42649997911425));
#57996=CARTESIAN_POINT('Ctrl Pts',(0.944718331247456,-2.95468587437239,
7.47917019173208));
#57997=CARTESIAN_POINT('Ctrl Pts',(1.9183152584455,-2.43777109483764,7.53184040434991));
#57998=CARTESIAN_POINT('Ctrl Pts',(2.45459564929204,-1.63038337673742,7.58451061696775));
#57999=CARTESIAN_POINT('Ctrl Pts',(2.99087604013859,-0.822995658637189,
7.63718082958558));
#58000=CARTESIAN_POINT('Ctrl Pts',(3.08983989463362,0.274864998028533,7.68985104220341));
#58001=CARTESIAN_POINT('Ctrl Pts',(2.7065911087876,1.16514133327123,7.74252125482124));
#58002=CARTESIAN_POINT('Ctrl Pts',(2.32334232294156,2.05541766851393,7.79519146743908));
#58003=CARTESIAN_POINT('Ctrl Pts',(1.45788089675451,2.7381096823336,7.8478616800569));
#58004=CARTESIAN_POINT('Ctrl Pts',(0.502833475452543,2.90350619986069,7.90053189267474));
#58005=CARTESIAN_POINT('Ctrl Pts',(-0.452213945849419,3.06890271738777,
7.95320210529257));
#58006=CARTESIAN_POINT('Ctrl Pts',(-1.49684736226627,2.71700373862224,8.0058723179104));
#58007=CARTESIAN_POINT('Ctrl Pts',(-2.15715667062231,2.0074523294601,8.05854253052823));
#58008=CARTESIAN_POINT('Ctrl Pts',(-2.6556204978759,1.47181591396764,8.09830298132228));
#58009=CARTESIAN_POINT('Ctrl Pts',(-2.93507122923162,0.732365674690379,
8.13806343211634));
#58010=CARTESIAN_POINT('Ctrl Pts',(-2.94164760189786,-0.00262292145090667,
8.17782388291039));
#58011=CARTESIAN_POINT('Origin',(0.,0.,0.));
#58012=CARTESIAN_POINT('',(-2.945934045911,0.00135292032082991,9.3221761170896));
#58013=CARTESIAN_POINT('',(-2.94588259210377,0.00139462648580093,9.1778238829104));
#58014=CARTESIAN_POINT('',(-2.942,-3.60291088309151E-16,0.));
#58015=CARTESIAN_POINT('Ctrl Pts',(-2.945934045911,0.00135292032082991,
9.3221761170896));
#58016=CARTESIAN_POINT('Ctrl Pts',(-2.94638425749025,0.0796883308965953,
9.317922384079));
#58017=CARTESIAN_POINT('Ctrl Pts',(-2.94352772129697,0.15799040718347,9.31366865106839));
#58018=CARTESIAN_POINT('Ctrl Pts',(-2.93725793323127,0.236018217593314,
9.30941491805779));
#58019=CARTESIAN_POINT('Ctrl Pts',(-2.85962469445823,1.20216756315553,9.25674470543996));
#58020=CARTESIAN_POINT('Ctrl Pts',(-2.25868267116007,2.12626734773872,9.20407449282213));
#58021=CARTESIAN_POINT('Ctrl Pts',(-1.40705620388363,2.58908895260061,9.1514042802043));
#58022=CARTESIAN_POINT('Ctrl Pts',(-0.555429736607181,3.05191055746251,
9.09873406758647));
#58023=CARTESIAN_POINT('Ctrl Pts',(0.54688117464756,3.05345398260311,9.04606385496863));
#58024=CARTESIAN_POINT('Ctrl Pts',(1.39980036012117,2.59301903525034,8.9933936423508));
#58025=CARTESIAN_POINT('Ctrl Pts',(2.25271954559477,2.13258408789758,8.94072342973297));
#58026=CARTESIAN_POINT('Ctrl Pts',(2.85624700528725,1.21017076805146,8.88805321711514));
#58027=CARTESIAN_POINT('Ctrl Pts',(2.93658548535115,0.24424261010507,8.83538300449731));
#58028=CARTESIAN_POINT('Ctrl Pts',(3.01692396541504,-0.721685547841337,
8.78271279187948));
#58029=CARTESIAN_POINT('Ctrl Pts',(2.57407346585034,-1.73112854388803,8.73004257926165));
#58030=CARTESIAN_POINT('Ctrl Pts',(1.80893826814173,-2.32614081848421,8.67737236664381));
#58031=CARTESIAN_POINT('Ctrl Pts',(1.04380307043313,-2.92115309308037,8.62470215402598));
#58032=CARTESIAN_POINT('Ctrl Pts',(-0.0436168254193812,-3.10173464622604,
8.57203194140814));
#58033=CARTESIAN_POINT('Ctrl Pts',(-0.960000732043568,-2.78596255535529,
8.51936172879031));
#58034=CARTESIAN_POINT('Ctrl Pts',(-1.87638463866775,-2.47019046448454,
8.46669151617249));
#58035=CARTESIAN_POINT('Ctrl Pts',(-2.62173255606362,-1.65806472959736,
8.41402130355466));
#58036=CARTESIAN_POINT('Ctrl Pts',(-2.85790872973228,-0.718015639026068,
8.36135109093683));
#58037=CARTESIAN_POINT('Ctrl Pts',(-2.91646298628421,-0.484952858959428,
8.34829276632109));
#58038=CARTESIAN_POINT('Ctrl Pts',(-2.94371978430835,-0.244026964003591,
8.33523444170534));
#58039=CARTESIAN_POINT('Ctrl Pts',(-2.94156648412342,-0.00262140296731356,
8.3221761170896));
#58040=CARTESIAN_POINT('Ctrl Pts',(-2.94164760189786,-0.00262292145090667,
8.17782388291039));
#58041=CARTESIAN_POINT('Ctrl Pts',(-2.94378287458944,-0.241265279117494,
8.19073364473417));
#58042=CARTESIAN_POINT('Ctrl Pts',(-2.91715101380018,-0.479437278615387,
8.20364340655795));
#58043=CARTESIAN_POINT('Ctrl Pts',(-2.85990837443616,-0.710009750985903,
8.21655316838173));
#58044=CARTESIAN_POINT('Ctrl Pts',(-2.62636556959873,-1.65071658271101,
8.26922338099956));
#58045=CARTESIAN_POINT('Ctrl Pts',(-1.88329475962863,-2.46492640660245,
8.32189359361739));
#58046=CARTESIAN_POINT('Ctrl Pts',(-0.96779866274798,-2.78326346310376,
8.37456380623522));
#58047=CARTESIAN_POINT('Ctrl Pts',(-0.0523025658673351,-3.10160051960507,
8.42723401885305));
#58048=CARTESIAN_POINT('Ctrl Pts',(1.03561881792387,-2.92406480871623,8.47990423147088));
#58049=CARTESIAN_POINT('Ctrl Pts',(1.80241729541542,-2.33119747122643,8.53257444408871));
#58050=CARTESIAN_POINT('Ctrl Pts',(2.56921577290696,-1.73833013373663,8.58524465670654));
#58051=CARTESIAN_POINT('Ctrl Pts',(3.01489134409887,-0.730131169645851,
8.63791486932438));
#58052=CARTESIAN_POINT('Ctrl Pts',(2.9372581008944,0.236018231065629,8.69058508194221));
#58053=CARTESIAN_POINT('Ctrl Pts',(2.85962485768992,1.20216763177713,8.74325529456004));
#58054=CARTESIAN_POINT('Ctrl Pts',(2.25868280008906,2.12626746910933,8.79592550717788));
#58055=CARTESIAN_POINT('Ctrl Pts',(1.40705628420046,2.58908910038977,8.84859571979571));
#58056=CARTESIAN_POINT('Ctrl Pts',(0.555429768311884,3.0519107316702,8.90126593241354));
#58057=CARTESIAN_POINT('Ctrl Pts',(-0.546881205864421,3.05345415689887,
8.95393614503137));
#58058=CARTESIAN_POINT('Ctrl Pts',(-1.39980044002393,2.59301918326378,9.0066063576492));
#58059=CARTESIAN_POINT('Ctrl Pts',(-2.25271967418346,2.13258420962867,9.05927657026703));
#58060=CARTESIAN_POINT('Ctrl Pts',(-2.85624716832619,1.21017083712978,9.11194678288487));
#58061=CARTESIAN_POINT('Ctrl Pts',(-2.9365856529759,0.244242624046729,9.1646169955027));
#58062=CARTESIAN_POINT('Ctrl Pts',(-2.94330052569389,0.163508153713587,
9.16901929130527));
#58063=CARTESIAN_POINT('Ctrl Pts',(-2.94636040237331,0.0824696889022224,
9.17342158710783));
#58064=CARTESIAN_POINT('Ctrl Pts',(-2.94588259210377,0.00139462648580093,
9.1778238829104));
#58065=CARTESIAN_POINT('Origin',(0.,0.,0.));
#58066=CARTESIAN_POINT('',(-2.937908603757,0.00135649600012097,10.3221761170896));
#58067=CARTESIAN_POINT('',(-2.93787076970937,0.00131817605956517,10.1778238829104));
#58068=CARTESIAN_POINT('',(-2.942,-3.60291088309151E-16,0.));
#58069=CARTESIAN_POINT('Ctrl Pts',(-2.937908603757,0.00135649600012097,
10.3221761170896));
#58070=CARTESIAN_POINT('Ctrl Pts',(-2.93959056192569,0.401293686681912,
10.3006103264527));
#58071=CARTESIAN_POINT('Ctrl Pts',(-2.86351195754617,0.800618114023186,
10.2790445358157));
#58072=CARTESIAN_POINT('Ctrl Pts',(-2.70659095429132,1.16514126676313,10.2574787451788));
#58073=CARTESIAN_POINT('Ctrl Pts',(-2.32334219032173,2.05541755118752,10.2048085325609));
#58074=CARTESIAN_POINT('Ctrl Pts',(-1.45788081353651,2.73810952603814,10.1521383199431));
#58075=CARTESIAN_POINT('Ctrl Pts',(-0.502833446750087,2.90350603412416,
10.0994681073253));
#58076=CARTESIAN_POINT('Ctrl Pts',(0.452213920036317,3.06890254221017,10.0467978947074));
#58077=CARTESIAN_POINT('Ctrl Pts',(1.49684727682391,2.71700358353159,9.99412768208959));
#58078=CARTESIAN_POINT('Ctrl Pts',(2.15715654748851,2.00745221487173,9.94145746947176));
#58079=CARTESIAN_POINT('Ctrl Pts',(2.81746581815312,1.29790084621186,9.88878725685393));
#58080=CARTESIAN_POINT('Ctrl Pts',(3.09345100269472,0.230697067570708,9.83611704423611));
#58081=CARTESIAN_POINT('Ctrl Pts',(2.85990821118827,-0.710009710457437,
9.78344683161828));
#58082=CARTESIAN_POINT('Ctrl Pts',(2.62636541968183,-1.65071648848557,9.73077661900045));
#58083=CARTESIAN_POINT('Ctrl Pts',(1.88329465212736,-2.46492626590069,9.67810640638261));
#58084=CARTESIAN_POINT('Ctrl Pts',(0.967798607504626,-2.78326330423086,
9.62543619376478));
#58085=CARTESIAN_POINT('Ctrl Pts',(0.0523025628818791,-3.10160034256102,
9.57276598114694));
#58086=CARTESIAN_POINT('Ctrl Pts',(-1.03561875880913,-2.92406464180621,
9.52009576852912));
#58087=CARTESIAN_POINT('Ctrl Pts',(-1.80241719253068,-2.33119733815818,
9.46742555591129));
#58088=CARTESIAN_POINT('Ctrl Pts',(-2.50728772340386,-1.78621097318669,
9.41900907630406));
#58089=CARTESIAN_POINT('Ctrl Pts',(-2.94080968580394,-0.890269755388179,
9.37059259669683));
#58090=CARTESIAN_POINT('Ctrl Pts',(-2.945934045911,0.00135292032082991,
9.3221761170896));
#58091=CARTESIAN_POINT('Ctrl Pts',(-2.94588259210377,0.00139462648580093,
9.1778238829104));
#58092=CARTESIAN_POINT('Ctrl Pts',(-2.9406437559651,-0.887533456499498,
9.22609179972566));
#58093=CARTESIAN_POINT('Ctrl Pts',(-2.51012187433051,-1.78086112066889,
9.27435971654092));
#58094=CARTESIAN_POINT('Ctrl Pts',(-1.80893837139867,-2.32614095126385,
9.32262763335619));
#58095=CARTESIAN_POINT('Ctrl Pts',(-1.04380313001497,-2.92115325982423,
9.37529784597402));
#58096=CARTESIAN_POINT('Ctrl Pts',(0.0436168279091599,-3.10173482327776,
9.42796805859185));
#58097=CARTESIAN_POINT('Ctrl Pts',(0.96000078684194,-2.78596271438223,9.48063827120969));
#58098=CARTESIAN_POINT('Ctrl Pts',(1.8763847457747,-2.4701906054867,9.53330848382752));
#58099=CARTESIAN_POINT('Ctrl Pts',(2.62173270571613,-1.65806482424214,9.58597869644535));
#58100=CARTESIAN_POINT('Ctrl Pts',(2.85790889286606,-0.718015680011411,
9.63864890906318));
#58101=CARTESIAN_POINT('Ctrl Pts',(3.09408508001598,0.222033464219328,9.69131912168101));
#58102=CARTESIAN_POINT('Ctrl Pts',(2.82108949437439,1.29000597143625,9.74398933429884));
#58103=CARTESIAN_POINT('Ctrl Pts',(2.16276975954276,2.00140368838285,9.79665954691667));
#58104=CARTESIAN_POINT('Ctrl Pts',(1.50445002471113,2.71280140532944,9.8493297595345));
#58105=CARTESIAN_POINT('Ctrl Pts',(0.460806140689482,3.06762433200573,9.90199997215234));
#58106=CARTESIAN_POINT('Ctrl Pts',(-0.494700702230345,2.90490291952725,
9.95467018477017));
#58107=CARTESIAN_POINT('Ctrl Pts',(-1.45020754515017,2.74218150704877,10.007340397388));
#58108=CARTESIAN_POINT('Ctrl Pts',(-2.31757734696816,2.06191575541552,10.0600106100058));
#58109=CARTESIAN_POINT('Ctrl Pts',(-2.70331770565014,1.1727161374278,10.1126808226237));
#58110=CARTESIAN_POINT('Ctrl Pts',(-2.86234691901197,0.806125728652842,
10.1343951760526));
#58111=CARTESIAN_POINT('Ctrl Pts',(-2.93951519940773,0.404023534891029,
10.1561095294815));
#58112=CARTESIAN_POINT('Ctrl Pts',(-2.93787076970937,0.00131817605956517,
10.1778238829104));
#58113=CARTESIAN_POINT('Origin',(0.,0.,0.));
#58114=CARTESIAN_POINT('',(-2.94117042680329,-0.00260214605593889,11.3221761170896));
#58115=CARTESIAN_POINT('',(-2.94125015913141,-0.00260761204136433,11.1778238829104));
#58116=CARTESIAN_POINT('',(-2.942,-3.60291088309151E-16,0.));
#58117=CARTESIAN_POINT('Ctrl Pts',(-2.94117042680329,-0.00260214605593889,
11.3221761170896));
#58118=CARTESIAN_POINT('Ctrl Pts',(-2.93488023009645,0.716368602336758,
11.2832982688263));
#58119=CARTESIAN_POINT('Ctrl Pts',(-2.66887225681339,1.43950600718068,11.244420420563));
#58120=CARTESIAN_POINT('Ctrl Pts',(-2.19025379787731,1.97128817432916,11.2055425722997));
#58121=CARTESIAN_POINT('Ctrl Pts',(-1.54183992928408,2.69172618880969,11.1528723596819));
#58122=CARTESIAN_POINT('Ctrl Pts',(-0.503205290563314,3.06095486386319,
11.1002021470641));
#58123=CARTESIAN_POINT('Ctrl Pts',(0.454461430404082,2.91146931524978,11.0475319344462));
#58124=CARTESIAN_POINT('Ctrl Pts',(1.41212815137148,2.76198376663637,10.9948617218284));
#58125=CARTESIAN_POINT('Ctrl Pts',(2.28882695458549,2.09378399435604,10.9421915092106));
#58126=CARTESIAN_POINT('Ctrl Pts',(2.68683322799011,1.21000659929365,10.8895212965927));
#58127=CARTESIAN_POINT('Ctrl Pts',(3.08483950139474,0.326229204231253,10.8368510839749));
#58128=CARTESIAN_POINT('Ctrl Pts',(3.00415324498994,-0.77312581361321,10.7841808713571));
#58129=CARTESIAN_POINT('Ctrl Pts',(2.48137871774039,-1.58932325991632,10.7315106587392));
#58130=CARTESIAN_POINT('Ctrl Pts',(1.95860419049084,-2.40552070621941,10.6788404461214));
#58131=CARTESIAN_POINT('Ctrl Pts',(0.993741392396532,-2.93856058098118,
10.6261702335036));
#58132=CARTESIAN_POINT('Ctrl Pts',(0.0245115575375578,-2.94662314334783,
10.5735000208857));
#58133=CARTESIAN_POINT('Ctrl Pts',(-0.944718277321443,-2.95468570571448,
10.5208298082679));
#58134=CARTESIAN_POINT('Ctrl Pts',(-1.91831514894513,-2.43777095568602,
10.4681595956501));
#58135=CARTESIAN_POINT('Ctrl Pts',(-2.45459550917999,-1.6303832836727,10.4154893830323));
#58136=CARTESIAN_POINT('Ctrl Pts',(-2.77129616018816,-1.15358006598522,
10.3843849610514));
#58137=CARTESIAN_POINT('Ctrl Pts',(-2.93548270908362,-0.575474437501757,
10.3532805390705));
#58138=CARTESIAN_POINT('Ctrl Pts',(-2.937908603757,0.00135649600012097,
10.3221761170896));
#58139=CARTESIAN_POINT('Ctrl Pts',(-2.93787076970937,0.00131817605956517,
10.1778238829104));
#58140=CARTESIAN_POINT('Ctrl Pts',(-2.93552648005067,-0.572776301283541,
10.2087797420993));
#58141=CARTESIAN_POINT('Ctrl Pts',(-2.7730096063261,-1.14809660257953,10.2397356012882));
#58142=CARTESIAN_POINT('Ctrl Pts',(-2.45915165107498,-1.62350328416062,
10.2706914604772));
#58143=CARTESIAN_POINT('Ctrl Pts',(-1.92513432227186,-2.43238960341916,
10.323361673095));
#58144=CARTESIAN_POINT('Ctrl Pts',(-0.95298874911967,-2.95202875759402,
10.3760318857128));
#58145=CARTESIAN_POINT('Ctrl Pts',(0.0162599186648668,-2.94668039863677,
10.4287020983307));
#58146=CARTESIAN_POINT('Ctrl Pts',(0.985508586449376,-2.94133203967952,
10.4813723109485));
#58147=CARTESIAN_POINT('Ctrl Pts',(1.95186034886621,-2.41099616759018,10.5340425235663));
#58148=CARTESIAN_POINT('Ctrl Pts',(2.47691848584703,-1.59626582095038,10.5867127361841));
#58149=CARTESIAN_POINT('Ctrl Pts',(3.00197662282786,-0.781535474310547,
10.639382948802));
#58150=CARTESIAN_POINT('Ctrl Pts',(3.08574113437262,0.317589346879808,10.6920531614198));
#58151=CARTESIAN_POINT('Ctrl Pts',(2.69021127525836,1.20247787968758,10.7447233740376));
#58152=CARTESIAN_POINT('Ctrl Pts',(2.2946814161441,2.08736641249534,10.7973935866555));
#58153=CARTESIAN_POINT('Ctrl Pts',(1.41985718637085,2.75801865692054,10.8500637992733));
#58154=CARTESIAN_POINT('Ctrl Pts',(0.462612775943444,2.91018541955646,10.9027340118911));
#58155=CARTESIAN_POINT('Ctrl Pts',(-0.494631634483977,3.06235218219239,
10.955404224509));
#58156=CARTESIAN_POINT('Ctrl Pts',(-1.53429622556554,2.69603346303901,11.0080744371268));
#58157=CARTESIAN_POINT('Ctrl Pts',(-2.18472505954886,1.97741401098616,11.0607446497446));
#58158=CARTESIAN_POINT('Ctrl Pts',(-2.6666654538549,1.44494723832272,11.0997710607999));
#58159=CARTESIAN_POINT('Ctrl Pts',(-2.93490816391246,0.719060797998435,
11.1387974718551));
#58160=CARTESIAN_POINT('Ctrl Pts',(-2.94125015913141,-0.00260761204136433,
11.1778238829104));
#58161=CARTESIAN_POINT('Origin',(0.,0.,0.));
#58162=CARTESIAN_POINT('',(-2.94616893643284,0.00113950433258347,12.3221761170896));
#58163=CARTESIAN_POINT('',(-2.94612437222716,0.00118363909654153,12.1778238829104));
#58164=CARTESIAN_POINT('',(-2.942,-3.60291088309151E-16,0.));
#58165=CARTESIAN_POINT('Ctrl Pts',(-2.94616893643284,0.00113950433258347,
12.3221761170896));
#58166=CARTESIAN_POINT('Ctrl Pts',(-2.94649117204446,0.0659433585993606,
12.3186564238178));
#58167=CARTESIAN_POINT('Ctrl Pts',(-2.94453636511729,0.130727428441818,
12.315136730546));
#58168=CARTESIAN_POINT('Ctrl Pts',(-2.94024229787316,0.195356072757268,
12.3116170372742));
#58169=CARTESIAN_POINT('Ctrl Pts',(-2.87598401816576,1.16248706242799,12.2589468246564));
#58170=CARTESIAN_POINT('Ctrl Pts',(-2.28788525250681,2.09481295451898,12.2062766120385));
#58171=CARTESIAN_POINT('Ctrl Pts',(-1.44274384818968,2.56937326090962,12.1536063994207));
#58172=CARTESIAN_POINT('Ctrl Pts',(-0.597602443872523,3.04393356730027,
12.1009361868029));
#58173=CARTESIAN_POINT('Ctrl Pts',(0.504581599102847,3.06072828799054,12.048265974185));
#58174=CARTESIAN_POINT('Ctrl Pts',(1.36378966624788,2.61213830254091,11.9955957615672));
#58175=CARTESIAN_POINT('Ctrl Pts',(2.22299773339287,2.16354831709129,11.9429255489494));
#58176=CARTESIAN_POINT('Ctrl Pts',(2.83922982470756,1.24957362550181,11.8902553363315));
#58177=CARTESIAN_POINT('Ctrl Pts',(2.9329250823967,0.28484948027729,11.8375851237137));
#58178=CARTESIAN_POINT('Ctrl Pts',(3.02662034008585,-0.679874664947257,
11.7849149110959));
#58179=CARTESIAN_POINT('Ctrl Pts',(2.59777876414943,-1.69534826380686,11.732244698478));
#58180=CARTESIAN_POINT('Ctrl Pts',(1.8409493248809,-2.30088990362134,11.6795744858602));
#58181=CARTESIAN_POINT('Ctrl Pts',(1.08411988561237,-2.90643154343581,11.6269042732424));
#58182=CARTESIAN_POINT('Ctrl Pts',(-0.000697416988240523,-3.10204122420515,
11.5742340606246));
#58183=CARTESIAN_POINT('Ctrl Pts',(-0.921362592257407,-2.79897833842183,
11.5215638480067));
#58184=CARTESIAN_POINT('Ctrl Pts',(-1.84202776752656,-2.49591545263851,
11.4688936353889));
#58185=CARTESIAN_POINT('Ctrl Pts',(-2.59854081546425,-1.69418000030252,
11.4162234227711));
#58186=CARTESIAN_POINT('Ctrl Pts',(-2.84770079020025,-0.75748859718075,
11.3635532101532));
#58187=CARTESIAN_POINT('Ctrl Pts',(-2.91294649518841,-0.512204052511054,
11.3497608457987));
#58188=CARTESIAN_POINT('Ctrl Pts',(-2.94340194651742,-0.2576652980836,11.3359684814441));
#58189=CARTESIAN_POINT('Ctrl Pts',(-2.94117042680329,-0.00260214605593889,
11.3221761170896));
#58190=CARTESIAN_POINT('Ctrl Pts',(-2.94125015913141,-0.00260761204136433,
11.1778238829104));
#58191=CARTESIAN_POINT('Ctrl Pts',(-2.94346734800271,-0.25490599957757,
11.191467684473));
#58192=CARTESIAN_POINT('Ctrl Pts',(-2.91367420009343,-0.506688846062122,
11.2051114860356));
#58193=CARTESIAN_POINT('Ctrl Pts',(-2.84981101201662,-0.749511142314743,
11.2187552875981));
#58194=CARTESIAN_POINT('Ctrl Pts',(-2.603275053616,-1.68689665861052,11.271425500216));
#58195=CARTESIAN_POINT('Ctrl Pts',(-1.84901005992971,-2.49074750624977,
11.3240957128338));
#58196=CARTESIAN_POINT('Ctrl Pts',(-0.929197120861756,-2.79638739577465,
11.3767659254516));
#58197=CARTESIAN_POINT('Ctrl Pts',(-0.00938418179379202,-3.10202728529954,
11.4294361380694));
#58198=CARTESIAN_POINT('Ctrl Pts',(1.07597670265583,-2.90945621671003,11.4821063506873));
#58199=CARTESIAN_POINT('Ctrl Pts',(1.83449893959343,-2.30603629574552,11.5347765633051));
#58200=CARTESIAN_POINT('Ctrl Pts',(2.59302117653101,-1.70261637478102,11.587446775923));
#58201=CARTESIAN_POINT('Ctrl Pts',(3.02470476595658,-0.688347601441517,
11.6401169885408));
#58202=CARTESIAN_POINT('Ctrl Pts',(2.93371142509181,0.27663519470765,11.6927872011586));
#58203=CARTESIAN_POINT('Ctrl Pts',(2.84271808422703,1.24161799085682,11.7454574137764));
#58204=CARTESIAN_POINT('Ctrl Pts',(2.22904781307192,2.15731480981565,11.7981276263943));
#58205=CARTESIAN_POINT('Ctrl Pts',(1.3710992699008,2.60830913596195,11.8507978390121));
#58206=CARTESIAN_POINT('Ctrl Pts',(0.513150726729663,3.05930346210826,11.9034680516299));
#58207=CARTESIAN_POINT('Ctrl Pts',(-0.5890760884575,3.04559529544201,11.9561382642478));
#58208=CARTESIAN_POINT('Ctrl Pts',(-1.43554315706074,2.57340350525938,12.0088084768656));
#58209=CARTESIAN_POINT('Ctrl Pts',(-2.28201022566397,2.10121171507676,12.0614786894834));
#58210=CARTESIAN_POINT('Ctrl Pts',(-2.87271754768328,1.17053630137777,12.1141489021013));
#58211=CARTESIAN_POINT('Ctrl Pts',(-2.93968387388293,0.203588993557491,
12.1668191147191));
#58212=CARTESIAN_POINT('Ctrl Pts',(-2.94434779339152,0.136245230376003,
12.1704873707829));
#58213=CARTESIAN_POINT('Ctrl Pts',(-2.94647129177883,0.0687255293040883,
12.1741556268466));
#58214=CARTESIAN_POINT('Ctrl Pts',(-2.94612437222716,0.00118363909654153,
12.1778238829104));
#58215=CARTESIAN_POINT('Origin',(0.,0.,0.));
#58216=CARTESIAN_POINT('',(-2.93811251051794,0.00154004898993351,13.3221761170896));
#58217=CARTESIAN_POINT('',(-2.93806927092397,0.00150371129981597,13.1778238829104));
#58218=CARTESIAN_POINT('',(-2.942,-3.60291088309151E-16,0.));
#58219=CARTESIAN_POINT('Ctrl Pts',(-2.93811251051794,0.00154004898993351,
13.3221761170896));
#58220=CARTESIAN_POINT('Ctrl Pts',(-2.93996482549542,0.387797276424435,
13.3013443661915));
#58221=CARTESIAN_POINT('Ctrl Pts',(-2.86914614049725,0.773402335775176,
13.2805126152933));
#58222=CARTESIAN_POINT('Ctrl Pts',(-2.72245263499158,1.12758166691397,13.2596808643952));
#58223=CARTESIAN_POINT('Ctrl Pts',(-2.35155831303012,2.02307531827001,13.2070106517773));
#58224=CARTESIAN_POINT('Ctrl Pts',(-1.49562542390561,2.71767636675688,13.1543404391595));
#58225=CARTESIAN_POINT('Ctrl Pts',(-0.542957881136105,2.8962709653455,13.1016702265417));
#58226=CARTESIAN_POINT('Ctrl Pts',(0.40970966163339,3.07486556393412,13.0490000139238));
#58227=CARTESIAN_POINT('Ctrl Pts',(1.45911185804788,2.7374537126245,12.996329801306));
#58228=CARTESIAN_POINT('Ctrl Pts',(2.12917519239819,2.03710622340532,12.9436595886882));
#58229=CARTESIAN_POINT('Ctrl Pts',(2.7992385267485,1.33675873418614,12.8909893760703));
#58230=CARTESIAN_POINT('Ctrl Pts',(3.08996299903463,0.273475607057396,12.8383191634525));
#58231=CARTESIAN_POINT('Ctrl Pts',(2.86945806996418,-0.67037239656747,12.7856489508347));
#58232=CARTESIAN_POINT('Ctrl Pts',(2.64895314089373,-1.61422040019232,12.7329787382168));
#58233=CARTESIAN_POINT('Ctrl Pts',(1.91721881046673,-2.4386332803133,12.680308525599));
#58234=CARTESIAN_POINT('Ctrl Pts',(1.00621487106457,-2.76960654220381,12.6276383129812));
#58235=CARTESIAN_POINT('Ctrl Pts',(0.095210931662416,-3.10057980409432,
12.5749681003633));
#58236=CARTESIAN_POINT('Ctrl Pts',(-0.9950626167149,-2.93811344775435,12.5222978877455));
#58237=CARTESIAN_POINT('Ctrl Pts',(-1.76999049402564,-2.35591222595915,
12.4696276751277));
#58238=CARTESIAN_POINT('Ctrl Pts',(-2.49313372304392,-1.81261667059929,
12.4204771557817));
#58239=CARTESIAN_POINT('Ctrl Pts',(-2.94166909896414,-0.903809548572848,
12.3713266364356));
#58240=CARTESIAN_POINT('Ctrl Pts',(-2.94616893643284,0.00113950433258347,
12.3221761170896));
#58241=CARTESIAN_POINT('Ctrl Pts',(-2.94612437222716,0.00118363909654153,
12.1778238829104));
#58242=CARTESIAN_POINT('Ctrl Pts',(-2.94149008920459,-0.901066561542921,
12.2268258394645));
#58243=CARTESIAN_POINT('Ctrl Pts',(-2.49601885931619,-1.80727633139181,
12.2758277960185));
#58244=CARTESIAN_POINT('Ctrl Pts',(-1.77658100825427,-2.35094654932331,
12.3248297525726));
#58245=CARTESIAN_POINT('Ctrl Pts',(-1.003286486046,-2.93531558244223,12.3774999651904));
#58246=CARTESIAN_POINT('Ctrl Pts',(0.0865278887505246,-3.10083444673851,
12.4301701778083));
#58247=CARTESIAN_POINT('Ctrl Pts',(0.998455145531424,-2.77241358368975,
12.4828403904261));
#58248=CARTESIAN_POINT('Ctrl Pts',(1.91038240231234,-2.44399272064099,12.5355106030439));
#58249=CARTESIAN_POINT('Ctrl Pts',(2.64442254107762,-1.62163213024718,12.5881808156617));
#58250=CARTESIAN_POINT('Ctrl Pts',(2.86756971266494,-0.678405262119501,
12.6408510282796));
#58251=CARTESIAN_POINT('Ctrl Pts',(3.09071688425225,0.264821606008148,12.6935212408974));
#58252=CARTESIAN_POINT('Ctrl Pts',(2.80297108866163,1.32891475186965,12.7461914535152));
#58253=CARTESIAN_POINT('Ctrl Pts',(2.13487155384946,2.03113593962306,12.7988616661331));
#58254=CARTESIAN_POINT('Ctrl Pts',(1.46677201903727,2.73335712737651,12.8515318787509));
#58255=CARTESIAN_POINT('Ctrl Pts',(0.418318745003505,3.07370635702182,12.9042020913687));
#58256=CARTESIAN_POINT('Ctrl Pts',(-0.534845242225581,2.8977802407252,12.9568723039866));
#58257=CARTESIAN_POINT('Ctrl Pts',(-1.48800922945464,2.7218541244286,13.0095425166044));
#58258=CARTESIAN_POINT('Ctrl Pts',(-2.34588392987902,2.02965266219009,13.0622127292222));
#58259=CARTESIAN_POINT('Ctrl Pts',(-2.71928450468353,1.13520110079642,13.1148829418401));
#58260=CARTESIAN_POINT('Ctrl Pts',(-2.86802248773115,0.778911019440369,
13.1358632555302));
#58261=CARTESIAN_POINT('Ctrl Pts',(-2.93988914006044,0.390529989491183,
13.1568435692203));
#58262=CARTESIAN_POINT('Ctrl Pts',(-2.93806927092397,0.00150371129981597,
13.1778238829104));
#58263=CARTESIAN_POINT('Origin',(0.,0.,0.));
#58264=CARTESIAN_POINT('',(-2.94078272534365,-0.002563628642199,14.3221761170896));
#58265=CARTESIAN_POINT('',(-2.94086056680551,-0.00257295723724145,14.1778238829104));
#58266=CARTESIAN_POINT('',(-2.942,-3.60291088309151E-16,0.));
#58267=CARTESIAN_POINT('Ctrl Pts',(-2.94078272534365,-0.002563628642199,
14.3221761170896));
#58268=CARTESIAN_POINT('Ctrl Pts',(-2.93476812227256,0.703069216740828,
14.2840323085651));
#58269=CARTESIAN_POINT('Ctrl Pts',(-2.67963677265994,1.41260648754648,14.2458885000406));
#58270=CARTESIAN_POINT('Ctrl Pts',(-2.21731865562784,1.9407953891895,14.2077446915161));
#58271=CARTESIAN_POINT('Ctrl Pts',(-1.578934748433,2.67013582025984,14.1550744788983));
#58272=CARTESIAN_POINT('Ctrl Pts',(-0.545508132734048,3.05369957925265,
14.1024042662805));
#58273=CARTESIAN_POINT('Ctrl Pts',(0.414135184292706,2.91747850302139,14.0497340536626));
#58274=CARTESIAN_POINT('Ctrl Pts',(1.37377850131946,2.78125742679014,13.9970638410448));
#58275=CARTESIAN_POINT('Ctrl Pts',(2.25963851967401,2.1252515153348,13.944393628427));
#58276=CARTESIAN_POINT('Ctrl Pts',(2.66983453522042,1.24706548338559,13.8917234158091));
#58277=CARTESIAN_POINT('Ctrl Pts',(3.08003055076681,0.368879451436385,13.8390532031913));
#58278=CARTESIAN_POINT('Ctrl Pts',(3.01456256350507,-0.73148670100669,13.7863829905735));
#58279=CARTESIAN_POINT('Ctrl Pts',(2.50313088767398,-1.55483906700073,13.7337127779556));
#58280=CARTESIAN_POINT('Ctrl Pts',(1.99169921184288,-2.37819143299479,13.6810425653378));
#58281=CARTESIAN_POINT('Ctrl Pts',(1.03430384744242,-2.9245300125398,13.62837235272));
#58282=CARTESIAN_POINT('Ctrl Pts',(0.0652783403102106,-2.94600195244691,
13.5757021401021));
#58283=CARTESIAN_POINT('Ctrl Pts',(-0.903747166821985,-2.96747389235401,
13.5230319274843));
#58284=CARTESIAN_POINT('Ctrl Pts',(-1.88440281668593,-2.46407919262322,
13.4703617148665));
#58285=CARTESIAN_POINT('Ctrl Pts',(-2.43180276421869,-1.66418871564523,
13.4176915022487));
#58286=CARTESIAN_POINT('Ctrl Pts',(-2.76269894649418,-1.18066527677114,
13.385853040529));
#58287=CARTESIAN_POINT('Ctrl Pts',(-2.9352815022272,-0.588800917055224,
13.3540145788093));
#58288=CARTESIAN_POINT('Ctrl Pts',(-2.93811251051794,0.00154004898993351,
13.3221761170896));
#58289=CARTESIAN_POINT('Ctrl Pts',(-2.93806927092397,0.00150371129981597,
13.1778238829104));
#58290=CARTESIAN_POINT('Ctrl Pts',(-2.93532043361636,-0.586104444526946,
13.2095137818381));
#58291=CARTESIAN_POINT('Ctrl Pts',(-2.76445685036328,-1.17518472499942,
13.2412036807658));
#58292=CARTESIAN_POINT('Ctrl Pts',(-2.43645366085186,-1.65737241294204,
13.2728935796936));
#58293=CARTESIAN_POINT('Ctrl Pts',(-1.89129579303109,-2.45879270473794,
13.3255637923114));
#58294=CARTESIAN_POINT('Ctrl Pts',(-0.912053608204924,-2.96493162778095,
13.3782340049292));
#58295=CARTESIAN_POINT('Ctrl Pts',(0.0570282834555854,-2.94617337092987,
13.4309042175471));
#58296=CARTESIAN_POINT('Ctrl Pts',(1.02611017511611,-2.9274151140788,13.4835744301649));
#58297=CARTESIAN_POINT('Ctrl Pts',(1.98503177361097,-2.38375967733365,13.5362446427827));
#58298=CARTESIAN_POINT('Ctrl Pts',(2.49876713918657,-1.56184267477676,13.5889148554006));
#58299=CARTESIAN_POINT('Ctrl Pts',(3.01250250476216,-0.739925672219871,
13.6415850680184));
#58300=CARTESIAN_POINT('Ctrl Pts',(3.08105163741847,0.360252896148758,13.6942552806362));
#58301=CARTESIAN_POINT('Ctrl Pts',(2.67331642557935,1.23958422278181,13.746925493254));
#58302=CARTESIAN_POINT('Ctrl Pts',(2.26558121374023,2.11891554941484,13.7995957058719));
#58303=CARTESIAN_POINT('Ctrl Pts',(1.38156165740569,2.77739963431232,13.8522659184897));
#58304=CARTESIAN_POINT('Ctrl Pts',(0.422303513476949,2.91630751110678,13.9049361311075));
#58305=CARTESIAN_POINT('Ctrl Pts',(-0.536954630451802,3.05521538790123,
13.9576063437254));
#58306=CARTESIAN_POINT('Ctrl Pts',(-1.57145136197473,2.67454705659267,14.0102765563432));
#58307=CARTESIAN_POINT('Ctrl Pts',(-2.2118752029893,1.94699713476955,14.062946768961));
#58308=CARTESIAN_POINT('Ctrl Pts',(-2.67747703562242,1.41805277755094,14.1012391402775));
#58309=CARTESIAN_POINT('Ctrl Pts',(-2.9347876598567,0.70576065041498,14.1395315115939));
#58310=CARTESIAN_POINT('Ctrl Pts',(-2.94086056680551,-0.00257295723724145,
14.1778238829104));
#58311=CARTESIAN_POINT('Origin',(0.,0.,0.));
#58312=CARTESIAN_POINT('',(-2.94636756759144,0.000915173715594336,15.3221761170896));
#58313=CARTESIAN_POINT('',(-2.94633063485147,0.000961351460667442,15.1778238829104));
#58314=CARTESIAN_POINT('',(-2.942,-3.60291088309151E-16,0.));
#58315=CARTESIAN_POINT('Ctrl Pts',(-2.94636756759144,0.000915173715594336,
15.3221761170896));
#58316=CARTESIAN_POINT('Ctrl Pts',(-2.94657828982524,0.0521948370493097,
15.3193904635566));
#58317=CARTESIAN_POINT('Ctrl Pts',(-2.94535428898749,0.10346423759929,15.3166048100236));
#58318=CARTESIAN_POINT('Ctrl Pts',(-2.94266379286899,0.154656563808966,
15.3138191564906));
#58319=CARTESIAN_POINT('Ctrl Pts',(-2.89179278506782,1.12258408024949,15.2611489438728));
#58320=CARTESIAN_POINT('Ctrl Pts',(-2.31664983854732,2.06295752655595,15.2084787312549));
#58321=CARTESIAN_POINT('Ctrl Pts',(-1.47815528586474,2.54916566805956,15.1558085186371));
#58322=CARTESIAN_POINT('Ctrl Pts',(-0.63966073318215,3.03537380956318,15.1031383060193));
#58323=CARTESIAN_POINT('Ctrl Pts',(0.462185425662502,3.06741664626393,15.0504680934014));
#58324=CARTESIAN_POINT('Ctrl Pts',(1.32751788394718,2.63075750962818,14.9977978807836));
#58325=CARTESIAN_POINT('Ctrl Pts',(2.19285034223184,2.19409837299243,14.9451276681658));
#58326=CARTESIAN_POINT('Ctrl Pts',(2.82166909995653,1.28873726302021,14.8924574555479));
#58327=CARTESIAN_POINT('Ctrl Pts',(2.92870319978326,0.325401813616169,14.8397872429301));
#58328=CARTESIAN_POINT('Ctrl Pts',(3.03573729960999,-0.637933635787871,
14.7871170303123));
#58329=CARTESIAN_POINT('Ctrl Pts',(2.62098674153875,-1.65924342462374,14.7344468176944));
#58330=CARTESIAN_POINT('Ctrl Pts',(1.87260794788981,-2.27519850196241,14.6817766050766));
#58331=CARTESIAN_POINT('Ctrl Pts',(1.12422915424088,-2.89115357930107,14.6291063924588));
#58332=CARTESIAN_POINT('Ctrl Pts',(0.0422221250142511,-3.10175394514255,
14.576436179841));
#58333=CARTESIAN_POINT('Ctrl Pts',(-0.882548065597691,-2.81145828426204,
14.5237659672231));
#58334=CARTESIAN_POINT('Ctrl Pts',(-1.80731825620963,-2.52116262338152,
14.4710957546053));
#58335=CARTESIAN_POINT('Ctrl Pts',(-2.57485160820688,-1.72997093577902,
14.4184255419874));
#58336=CARTESIAN_POINT('Ctrl Pts',(-2.83694768486014,-0.796816540403842,
14.3657553293696));
#58337=CARTESIAN_POINT('Ctrl Pts',(-2.90923358103393,-0.539453276521613,
14.3512289252763));
#58338=CARTESIAN_POINT('Ctrl Pts',(-2.94307328200413,-0.271291588698562,
14.3367025211829));
#58339=CARTESIAN_POINT('Ctrl Pts',(-2.94078272534365,-0.002563628642199,
14.3221761170896));
#58340=CARTESIAN_POINT('Ctrl Pts',(-2.94086056680551,-0.00257295723724145,
14.1778238829104));
#58341=CARTESIAN_POINT('Ctrl Pts',(-2.94314079363258,-0.268534762399236,
14.1922017242118));
#58342=CARTESIAN_POINT('Ctrl Pts',(-2.91000109139948,-0.533938488619848,
14.2065795655132));
#58343=CARTESIAN_POINT('Ctrl Pts',(-2.83916807956566,-0.788869046535997,
14.2209574068145));
#58344=CARTESIAN_POINT('Ctrl Pts',(-2.57968616462127,-1.72275379368075,
14.2736276194324));
#58345=CARTESIAN_POINT('Ctrl Pts',(-1.81437138422634,-2.51609177563258,
14.3262978320502));
#58346=CARTESIAN_POINT('Ctrl Pts',(-0.890417692713573,-2.80897598605912,
14.378968044668));
#58347=CARTESIAN_POINT('Ctrl Pts',(0.0335359987991893,-3.10186019648566,
14.4316382572858));
#58348=CARTESIAN_POINT('Ctrl Pts',(1.11612860142979,-2.89429063538687,14.4843084699037));
#58349=CARTESIAN_POINT('Ctrl Pts',(1.86622938578629,-2.28043365047774,14.5369786825215));
#58350=CARTESIAN_POINT('Ctrl Pts',(2.61633017014279,-1.66657666556861,14.5896488951393));
#58351=CARTESIAN_POINT('Ctrl Pts',(3.03393913622522,-0.646432256849133,
14.6423191077572));
#58352=CARTESIAN_POINT('Ctrl Pts',(2.92960311741482,0.317199198340533,14.694989320375));
#58353=CARTESIAN_POINT('Ctrl Pts',(2.82526709860441,1.28083065353021,14.7476595329928));
#58354=CARTESIAN_POINT('Ctrl Pts',(2.19898609490117,2.18794915519006,14.8003297456107));
#58355=CARTESIAN_POINT('Ctrl Pts',(1.33487977102078,2.62702983622557,14.8529999582285));
#58356=CARTESIAN_POINT('Ctrl Pts',(0.470773447140396,3.06611051726107,14.9056701708463));
#58357=CARTESIAN_POINT('Ctrl Pts',(-0.631158196917155,3.03715337767223,
14.9583403834642));
#58358=CARTESIAN_POINT('Ctrl Pts',(-1.47101105209001,2.55329517013352,15.011010596082));
#58359=CARTESIAN_POINT('Ctrl Pts',(-2.31086390726285,2.06943696259481,15.0636808086998));
#58360=CARTESIAN_POINT('Ctrl Pts',(-2.88863797355103,1.13067768710628,15.1163510213177));
#58361=CARTESIAN_POINT('Ctrl Pts',(-2.94221932036621,0.162896393065324,
15.1690212339355));
#58362=CARTESIAN_POINT('Ctrl Pts',(-2.94520429526425,0.108982054564796,
15.1719554502605));
#58363=CARTESIAN_POINT('Ctrl Pts',(-2.94656242919711,0.0549776457391388,
15.1748896665854));
#58364=CARTESIAN_POINT('Ctrl Pts',(-2.94633063485147,0.000961351460667442,
15.1778238829104));
#58365=CARTESIAN_POINT('Origin',(0.,0.,0.));
#58366=CARTESIAN_POINT('',(-2.93834196467696,0.0017116903336982,16.3221761170896));
#58367=CARTESIAN_POINT('',(-2.93829399889148,0.00167873273706156,16.1778238829104));
#58368=CARTESIAN_POINT('',(-2.942,-3.60291088309151E-16,0.));
#58369=CARTESIAN_POINT('Ctrl Pts',(-2.93834196467696,0.0017116903336982,
16.3221761170896));
#58370=CARTESIAN_POINT('Ctrl Pts',(-2.9403397843927,0.374286552436328,16.3020784059303));
#58371=CARTESIAN_POINT('Ctrl Pts',(-2.87457680364825,0.746182656532499,
16.2819806947709));
#58372=CARTESIAN_POINT('Ctrl Pts',(-2.73779374054997,1.08980790041183,16.2618829836116));
#58373=CARTESIAN_POINT('Ctrl Pts',(-2.37932540757495,1.99034898752761,16.2092127709937));
#58374=CARTESIAN_POINT('Ctrl Pts',(-1.53308367358257,2.69672283094819,16.1565425583759));
#58375=CARTESIAN_POINT('Ctrl Pts',(-0.582978050092166,2.88848054283463,
16.1038723457581));
#58376=CARTESIAN_POINT('Ctrl Pts',(0.367127573398249,3.08023825472107,16.0512021331402));
#58377=CARTESIAN_POINT('Ctrl Pts',(1.4210970863867,2.75737983507336,15.9985319205224));
#58378=CARTESIAN_POINT('Ctrl Pts',(2.10078605818236,2.06637071241156,15.9458617079046));
#58379=CARTESIAN_POINT('Ctrl Pts',(2.78047502997801,1.37536158974976,15.8931914952867));
#58380=CARTESIAN_POINT('Ctrl Pts',(3.08588346058089,0.316201764073922,15.8405212826689));
#58381=CARTESIAN_POINT('Ctrl Pts',(2.87845868549279,-0.630606989902349,
15.7878510700511));
#58382=CARTESIAN_POINT('Ctrl Pts',(2.67103391040469,-1.57741574387861,15.7351808574333));
#58383=CARTESIAN_POINT('Ctrl Pts',(1.95077592962559,-2.41187342615528,15.6825106448154));
#58384=CARTESIAN_POINT('Ctrl Pts',(1.04443845795601,-2.75541943685174,15.6298404321976));
#58385=CARTESIAN_POINT('Ctrl Pts',(0.138100986286415,-3.0989654475482,15.5771702195797));
#58386=CARTESIAN_POINT('Ctrl Pts',(-0.954315976273691,-2.95159978666445,
15.5245000069619));
#58387=CARTESIAN_POINT('Ctrl Pts',(-1.73722492301283,-2.38017616293528,
15.4718297943441));
#58388=CARTESIAN_POINT('Ctrl Pts',(-2.47872691570511,-1.83897433169884,
15.4219452352593));
#58389=CARTESIAN_POINT('Ctrl Pts',(-2.94259402375403,-0.917384020750813,
15.3720606761744));
#58390=CARTESIAN_POINT('Ctrl Pts',(-2.94636756759144,0.000915173715594336,
15.3221761170896));
#58391=CARTESIAN_POINT('Ctrl Pts',(-2.94633063485147,0.000961351460667442,
15.1778238829104));
#58392=CARTESIAN_POINT('Ctrl Pts',(-2.94240163935874,-0.914633790291091,
15.2275598792033));
#58393=CARTESIAN_POINT('Ctrl Pts',(-2.48166336201514,-1.83364379373038,
15.2772958754961));
#58394=CARTESIAN_POINT('Ctrl Pts',(-1.74388353322011,-2.37530209033153,
15.327031871789));
#58395=CARTESIAN_POINT('Ctrl Pts',(-0.962577771916698,-2.94891596709401,
15.3797020844068));
#58396=CARTESIAN_POINT('Ctrl Pts',(0.129422378032284,-3.09934040802562,
15.4323722970246));
#58397=CARTESIAN_POINT('Ctrl Pts',(1.03671835568921,-2.75833368087526,15.4850425096425));
#58398=CARTESIAN_POINT('Ctrl Pts',(1.94401433334615,-2.4173269537249,15.5377127222603));
#58399=CARTESIAN_POINT('Ctrl Pts',(2.66660613871103,-1.58488905849257,15.5903829348781));
#58400=CARTESIAN_POINT('Ctrl Pts',(2.87668156935298,-0.638665006267767,
15.643053147496));
#58401=CARTESIAN_POINT('Ctrl Pts',(3.08675699999493,0.307559045957031,15.6957233601138));
#58402=CARTESIAN_POINT('Ctrl Pts',(2.78431605591395,1.36756925517429,15.7483935727317));
#58403=CARTESIAN_POINT('Ctrl Pts',(2.10656463391492,2.06047941828124,15.8010637853495));
#58404=CARTESIAN_POINT('Ctrl Pts',(1.42881321191589,2.75338958138818,15.8537339979673));
#58405=CARTESIAN_POINT('Ctrl Pts',(0.375751311998833,3.07919969838482,15.9064042105851));
#58406=CARTESIAN_POINT('Ctrl Pts',(-0.574887366656207,2.8901026755206,15.959074423203));
#58407=CARTESIAN_POINT('Ctrl Pts',(-1.52552604531125,2.70100565265638,16.0117446358208));
#58408=CARTESIAN_POINT('Ctrl Pts',(-2.37374150270427,1.9970014899313,16.0644148484386));
#58409=CARTESIAN_POINT('Ctrl Pts',(-2.73473076831818,1.09746899458998,16.1170850610565));
#58410=CARTESIAN_POINT('Ctrl Pts',(-2.87349397434761,0.751691363864775,
16.1373313350078));
#58411=CARTESIAN_POINT('Ctrl Pts',(-2.94026410906292,0.377022254332635,
16.1575776089591));
#58412=CARTESIAN_POINT('Ctrl Pts',(-2.93829399889148,0.00167873273706156,
16.1778238829104));
#58413=CARTESIAN_POINT('Origin',(0.,0.,0.));
#58414=CARTESIAN_POINT('',(-2.94033980469539,-0.00268911818531531,17.3221761170896));
#58415=CARTESIAN_POINT('',(-2.94047623996122,-0.00254690177668123,17.1778238829104));
#58416=CARTESIAN_POINT('',(-2.942,-3.60291088309151E-16,0.));
#58417=CARTESIAN_POINT('Ctrl Pts',(-2.94033980469539,-0.00268911818531531,
17.3221761170896));
#58418=CARTESIAN_POINT('Ctrl Pts',(-2.9346462523403,0.689633572098389,17.2847663483039));
#58419=CARTESIAN_POINT('Ctrl Pts',(-2.69018060245738,1.38571321721952,17.2473565795182));
#58420=CARTESIAN_POINT('Ctrl Pts',(-2.24398877650981,1.91001340457724,17.2099468107325));
#58421=CARTESIAN_POINT('Ctrl Pts',(-1.61578338781506,2.64818964142855,17.1572765981147));
#58422=CARTESIAN_POINT('Ctrl Pts',(-0.587704750385148,3.04585473995439,
17.1046063854969));
#58423=CARTESIAN_POINT('Ctrl Pts',(0.373745236161002,2.92288602380855,17.051936172879));
#58424=CARTESIAN_POINT('Ctrl Pts',(1.33519522270717,2.79991730766271,16.9992659602612));
#58425=CARTESIAN_POINT('Ctrl Pts',(2.23001655836957,2.15631477684517,16.9465957476434));
#58426=CARTESIAN_POINT('Ctrl Pts',(2.65231656865006,1.28390822131956,16.8939255350255));
#58427=CARTESIAN_POINT('Ctrl Pts',(3.07461657893055,0.411501665793941,16.8412553224077));
#58428=CARTESIAN_POINT('Ctrl Pts',(3.02439526382914,-0.689708914439747,
16.7885851097899));
#58429=CARTESIAN_POINT('Ctrl Pts',(2.52440812832174,-1.52006904496187,16.735914897172));
#58430=CARTESIAN_POINT('Ctrl Pts',(2.02442099281435,-2.35042917548398,16.6832446845542));
#58431=CARTESIAN_POINT('Ctrl Pts',(1.074668036901,-2.90993885629453,16.6305744719364));
#58432=CARTESIAN_POINT('Ctrl Pts',(0.106030389206343,-2.94481058190328,
16.5779042593186));
#58433=CARTESIAN_POINT('Ctrl Pts',(-0.862607258488317,-2.97968230751204,
16.5252340467007));
#58434=CARTESIAN_POINT('Ctrl Pts',(-1.85012959796428,-2.489916077919,16.4725638340829));
#58435=CARTESIAN_POINT('Ctrl Pts',(-2.40854330172345,-1.69767879771699,
16.4198936214651));
#58436=CARTESIAN_POINT('Ctrl Pts',(-2.75387950365051,-1.20774058250446,
16.3873211200066));
#58437=CARTESIAN_POINT('Ctrl Pts',(-2.93510408424925,-0.602123002234626,
16.3547486185481));
#58438=CARTESIAN_POINT('Ctrl Pts',(-2.93834196467696,0.0017116903336982,
16.3221761170896));
#58439=CARTESIAN_POINT('Ctrl Pts',(-2.93829399889148,0.00167873273706156,
16.1778238829104));
#58440=CARTESIAN_POINT('Ctrl Pts',(-2.93513891309551,-0.599425221124181,
16.2102478215769));
#58441=CARTESIAN_POINT('Ctrl Pts',(-2.75568379353507,-1.20225885851725,
16.2426717602434));
#58442=CARTESIAN_POINT('Ctrl Pts',(-2.41328914510403,-1.69092473863608,
16.27509569891));
#58443=CARTESIAN_POINT('Ctrl Pts',(-1.85709518244114,-2.48472514856328,
16.3277659115278));
#58444=CARTESIAN_POINT('Ctrl Pts',(-0.870944183280553,-2.97726514046012,
16.3804361241456));
#58445=CARTESIAN_POINT('Ctrl Pts',(0.0977855608398415,-2.94510139794416,
16.4331063367635));
#58446=CARTESIAN_POINT('Ctrl Pts',(1.06651530496021,-2.9129376554282,16.4857765493813));
#58447=CARTESIAN_POINT('Ctrl Pts',(2.01782379404038,-2.35607017849948,16.5384467619991));
#58448=CARTESIAN_POINT('Ctrl Pts',(2.52013775106141,-1.5271222999678,16.591116974617));
#58449=CARTESIAN_POINT('Ctrl Pts',(3.02245170808247,-0.698174421436078,
16.6437871872348));
#58450=CARTESIAN_POINT('Ctrl Pts',(3.07577113304434,0.40285385869867,16.6964573998526));
#58451=CARTESIAN_POINT('Ctrl Pts',(2.65590917431802,1.27645664321552,16.7491276124704));
#58452=CARTESIAN_POINT('Ctrl Pts',(2.23604721559172,2.15005942773234,16.8017978250883));
#58453=CARTESIAN_POINT('Ctrl Pts',(1.34300387317732,2.79623671663129,16.8544680377061));
#58454=CARTESIAN_POINT('Ctrl Pts',(0.38191458879571,2.92186483790969,16.9071382503239));
#58455=CARTESIAN_POINT('Ctrl Pts',(-0.579174695585912,3.04749295918809,
16.9598084629418));
#58456=CARTESIAN_POINT('Ctrl Pts',(-1.60830992193471,2.65257191284588,17.0124786755596));
#58457=CARTESIAN_POINT('Ctrl Pts',(-2.2386041647435,1.91621987213004,17.0651488881774));
#58458=CARTESIAN_POINT('Ctrl Pts',(-2.68805745126554,1.39113837485648,17.1027072197551));
#58459=CARTESIAN_POINT('Ctrl Pts',(-2.93470407488486,0.69244262168104,17.1402655513327));
#58460=CARTESIAN_POINT('Ctrl Pts',(-2.94047623996122,-0.00254690177668123,
17.1778238829104));
#58461=CARTESIAN_POINT('Origin',(0.,0.,-1.848589891905));
#58462=CARTESIAN_POINT('',(-2.3704116015589,-0.00216788445160201,17.651410108095));
#58463=CARTESIAN_POINT('',(-2.37524114860369,0.000101641450047634,17.848589891905));
#58464=CARTESIAN_POINT('',(-2.37175,-3.45929798001232E-13,-1.848589891905));
#58465=CARTESIAN_POINT('',(1.37994918219948,-1.93347698736443,18.));
#58466=CARTESIAN_POINT('Ctrl Pts',(-2.3704116015589,-0.00216788445160182,
17.651410108095));
#58467=CARTESIAN_POINT('Ctrl Pts',(-2.37228397167149,-0.229843724195573,
17.6666705519271));
#58468=CARTESIAN_POINT('Ctrl Pts',(-2.23803403881605,-1.24108118812309,
17.7346012083771));
#58469=CARTESIAN_POINT('Ctrl Pts',(-0.854011012564108,-2.62815348477828,
17.8507978390121));
#58470=CARTESIAN_POINT('Ctrl Pts',(0.794121156913562,-2.34631857250555,
17.951734025815));
#58471=CARTESIAN_POINT('Ctrl Pts',(1.37994918219948,-1.93347698736443,18.));
#58472=CARTESIAN_POINT('',(-1.37702479013092,-1.93106208855772,18.));
#58473=CARTESIAN_POINT('Origin',(0.,0.,18.));
#58474=CARTESIAN_POINT('Ctrl Pts',(-2.37524114860369,0.000101641450047495,
17.848589891905));
#58475=CARTESIAN_POINT('Ctrl Pts',(-2.37291161402036,-0.747323183496906,
17.8990599279367));
#58476=CARTESIAN_POINT('Ctrl Pts',(-1.98938888825758,-1.49439019245295,
17.9495299639683));
#58477=CARTESIAN_POINT('Ctrl Pts',(-1.37702479013086,-1.93106208855776,
18.));
#58478=CARTESIAN_POINT('Origin',(0.,0.,-1.848589891905));
#58479=CARTESIAN_POINT('',(-2.36880100432447,0.00137991215103788,16.651410108095));
#58480=CARTESIAN_POINT('',(-2.37052159147792,-0.00205323395313789,16.848589891905));
#58481=CARTESIAN_POINT('',(-2.37175,-3.45929798001232E-13,-1.848589891905));
#58482=CARTESIAN_POINT('Ctrl Pts',(-2.36880100432447,0.00137991215103789,
16.651410108095));
#58483=CARTESIAN_POINT('Ctrl Pts',(-2.36619072461524,-0.485413062729584,
16.6839826095535));
#58484=CARTESIAN_POINT('Ctrl Pts',(-1.98385093138572,-1.76311887753393,
16.7692253236298));
#58485=CARTESIAN_POINT('Ctrl Pts',(0.100702699977133,-2.79696280349387,
16.9071382503239));
#58486=CARTESIAN_POINT('Ctrl Pts',(2.39768764884266,-1.44378426631252,17.0651488881774));
#58487=CARTESIAN_POINT('Ctrl Pts',(2.51914829203609,1.21950213103884,17.2231595260309));
#58488=CARTESIAN_POINT('Ctrl Pts',(0.35501589619246,2.77605988338393,17.3811701638844));
#58489=CARTESIAN_POINT('Ctrl Pts',(-1.89126576511015,1.90718878185824,17.5239203579058));
#58490=CARTESIAN_POINT('Ctrl Pts',(-2.36582163459831,0.555961395181473,
17.6140003393093));
#58491=CARTESIAN_POINT('Ctrl Pts',(-2.3704116015589,-0.00216788445160182,
17.651410108095));
#58492=CARTESIAN_POINT('Ctrl Pts',(-2.37052159147792,-0.0020532339531374,
16.848589891905));
#58493=CARTESIAN_POINT('Ctrl Pts',(-2.37239389915549,-0.227485840854584,
16.8637017729452));
#58494=CARTESIAN_POINT('Ctrl Pts',(-2.23978575228814,-1.23646065412646,
16.9314838666032));
#58495=CARTESIAN_POINT('Ctrl Pts',(-0.80874814078054,-2.6792673034923,17.051936172879));
#58496=CARTESIAN_POINT('Ctrl Pts',(1.80238833174315,-2.14148580062739,17.2099468107325));
#58497=CARTESIAN_POINT('Ctrl Pts',(2.77800430721521,0.340253358304015,17.367957448586));
#58498=CARTESIAN_POINT('Ctrl Pts',(1.23340008456365,2.51147754111133,17.5259680864395));
#58499=CARTESIAN_POINT('Ctrl Pts',(-1.43092211742628,2.4074435208734,17.683978724293));
#58500=CARTESIAN_POINT('Ctrl Pts',(-2.35980886491538,0.845292509076889,
17.7915193261149));
#58501=CARTESIAN_POINT('Ctrl Pts',(-2.37534270168053,0.0326846695014218,
17.8463897153189));
#58502=CARTESIAN_POINT('Ctrl Pts',(-2.37524114860369,0.000101641450047495,
17.848589891905));
#58503=CARTESIAN_POINT('Origin',(0.,0.,-1.848589891905));
#58504=CARTESIAN_POINT('',(-2.37527099878824,0.000737784928405548,15.651410108095));
#58505=CARTESIAN_POINT('',(-2.36876233578207,0.00135334274909457,15.848589891905));
#58506=CARTESIAN_POINT('',(-2.37175,-3.45929798001232E-13,-1.848589891905));
#58507=CARTESIAN_POINT('Ctrl Pts',(-2.37527099878824,0.000737784928405679,
15.651410108095));
#58508=CARTESIAN_POINT('Ctrl Pts',(-2.37222888369763,-0.739566808707072,
15.7012946671798));
#58509=CARTESIAN_POINT('Ctrl Pts',(-1.60343564769808,-2.26697063865214,
15.8038494388825));
#58510=CARTESIAN_POINT('Ctrl Pts',(0.992005759747417,-2.61709238831523,
15.959074423203));
#58511=CARTESIAN_POINT('Ctrl Pts',(2.73395531710238,-0.598949960096589,
16.1170850610565));
#58512=CARTESIAN_POINT('Ctrl Pts',(1.99532264006382,1.96263635861182,16.2750956989099));
#58513=CARTESIAN_POINT('Ctrl Pts',(-0.553710866833194,2.74347197057582,
16.4331063367635));
#58514=CARTESIAN_POINT('Ctrl Pts',(-2.17845584047471,1.38726687514169,16.5585444731585));
#58515=CARTESIAN_POINT('Ctrl Pts',(-2.37041158519152,0.301738317722773,
16.6313123969356));
#58516=CARTESIAN_POINT('Ctrl Pts',(-2.36880100432447,0.00137991215103789,
16.651410108095));
#58517=CARTESIAN_POINT('Ctrl Pts',(-2.36876233578207,0.00135334274909471,
15.848589891905));
#58518=CARTESIAN_POINT('Ctrl Pts',(-2.36621880256085,-0.483238194494291,
15.8810138305715));
#58519=CARTESIAN_POINT('Ctrl Pts',(-1.98654027620114,-1.75867122558308,
15.9661079818559));
#58520=CARTESIAN_POINT('Ctrl Pts',(0.0928761949570627,-2.79725027962867,
16.1038723457581));
#58521=CARTESIAN_POINT('Ctrl Pts',(2.39362321294746,-1.45046193319176,16.2618829836116));
#58522=CARTESIAN_POINT('Ctrl Pts',(2.52257665905884,1.21238356994498,16.4198936214651));
#58523=CARTESIAN_POINT('Ctrl Pts',(0.362744353785385,2.77516839483905,16.5779042593186));
#58524=CARTESIAN_POINT('Ctrl Pts',(-1.88818603203603,1.91139484938775,16.7208030161319));
#58525=CARTESIAN_POINT('Ctrl Pts',(-2.36586824935706,0.558225964640069,
16.8110315603274));
#58526=CARTESIAN_POINT('Ctrl Pts',(-2.37052159147792,-0.0020532339531374,
16.848589891905));
#58527=CARTESIAN_POINT('Origin',(0.,0.,-1.848589891905));
#58528=CARTESIAN_POINT('',(-2.37076867057573,-0.00206671863790898,14.651410108095));
#58529=CARTESIAN_POINT('',(-2.37524122474812,0.000775012007393425,14.848589891905));
#58530=CARTESIAN_POINT('',(-2.37175,-3.45929798001232E-13,-1.848589891905));
#58531=CARTESIAN_POINT('Ctrl Pts',(-2.37076867057573,-0.00206671863790864,
14.651410108095));
#58532=CARTESIAN_POINT('Ctrl Pts',(-2.37261524697255,-0.218706942724769,
14.6659365121883));
#58533=CARTESIAN_POINT('Ctrl Pts',(-2.24642027727927,-1.21873516689608,
14.7331331288995));
#58534=CARTESIAN_POINT('Ctrl Pts',(-0.838242639893101,-2.67031826549166,
14.8529999582285));
#58535=CARTESIAN_POINT('Ctrl Pts',(1.77859981921798,-2.16097963427009,15.011010596082));
#58536=CARTESIAN_POINT('Ctrl Pts',(2.78167728635466,0.309066074436347,15.1690212339355));
#58537=CARTESIAN_POINT('Ctrl Pts',(1.26087420481122,2.49868899684622,15.327031871789));
#58538=CARTESIAN_POINT('Ctrl Pts',(-1.40394934437959,2.42119314578055,15.4850425096425));
#58539=CARTESIAN_POINT('Ctrl Pts',(-2.35579694789029,0.86489793832459,15.5931685884112));
#58540=CARTESIAN_POINT('Ctrl Pts',(-2.37544087657819,0.0420778738175528,
15.648624454562));
#58541=CARTESIAN_POINT('Ctrl Pts',(-2.37527099878824,0.000737784928405679,
15.651410108095));
#58542=CARTESIAN_POINT('Ctrl Pts',(-2.37524122474812,0.000775012007393572,
14.848589891905));
#58543=CARTESIAN_POINT('Ctrl Pts',(-2.37207378930956,-0.737349657417977,
14.8983258881979));
#58544=CARTESIAN_POINT('Ctrl Pts',(-1.60729470532651,-2.26281359901547,
15.0007320971086));
#58545=CARTESIAN_POINT('Ctrl Pts',(0.984673310924482,-2.61986056441679,
15.1558085186371));
#58546=CARTESIAN_POINT('Ctrl Pts',(2.73226724128555,-0.606603006955222,
15.3138191564906));
#58547=CARTESIAN_POINT('Ctrl Pts',(2.0008114535995,1.95703997099618,15.4718297943441));
#58548=CARTESIAN_POINT('Ctrl Pts',(-0.546026983988871,2.74501428607443,
15.6298404321976));
#58549=CARTESIAN_POINT('Ctrl Pts',(-2.17649017174337,1.39175803337991,15.7554271313846));
#58550=CARTESIAN_POINT('Ctrl Pts',(-2.37035057806599,0.303943756530424,
15.8283436179537));
#58551=CARTESIAN_POINT('Ctrl Pts',(-2.36876233578207,0.00135334274909471,
15.848589891905));
#58552=CARTESIAN_POINT('Origin',(0.,0.,-1.848589891905));
#58553=CARTESIAN_POINT('',(-2.36861602543199,0.00124154017382057,13.651410108095));
#58554=CARTESIAN_POINT('',(-2.37083142397042,-0.00207423906479154,13.848589891905));
#58555=CARTESIAN_POINT('',(-2.37175,-3.45929798001232E-13,-1.848589891905));
#58556=CARTESIAN_POINT('Ctrl Pts',(-2.36861602543199,0.00124154017382031,
13.651410108095));
#58557=CARTESIAN_POINT('Ctrl Pts',(-2.36633375353748,-0.474673207010919,
13.6832485698147));
#58558=CARTESIAN_POINT('Ctrl Pts',(-1.99703967034429,-1.74115118427591,
13.7677572441522));
#58559=CARTESIAN_POINT('Ctrl Pts',(0.0620012558310767,-2.79810760818394,
13.9049361311075));
#58560=CARTESIAN_POINT('Ctrl Pts',(2.37746942936956,-1.4767834823825,14.062946768961));
#58561=CARTESIAN_POINT('Ctrl Pts',(2.53580426837836,1.18446065975573,14.2209574068145));
#58562=CARTESIAN_POINT('Ctrl Pts',(0.393344888501637,2.77101608514062,14.378968044668));
#58563=CARTESIAN_POINT('Ctrl Pts',(-1.87623249328146,1.9286460332593,14.5224522784282));
#58564=CARTESIAN_POINT('Ctrl Pts',(-2.36591988239296,0.56679279904984,14.6132662995705));
#58565=CARTESIAN_POINT('Ctrl Pts',(-2.37076867057573,-0.00206671863790864,
14.651410108095));
#58566=CARTESIAN_POINT('Ctrl Pts',(-2.37083142397042,-0.00207423906479159,
13.848589891905));
#58567=CARTESIAN_POINT('Ctrl Pts',(-2.37266967277294,-0.216484474072482,
13.8629677332064));
#58568=CARTESIAN_POINT('Ctrl Pts',(-2.24808422025942,-1.21424369041544,
13.9300157871256));
#58569=CARTESIAN_POINT('Ctrl Pts',(-0.845717199230744,-2.66796058040481,
14.0497340536626));
#58570=CARTESIAN_POINT('Ctrl Pts',(1.77254147373567,-2.16595197414774,14.2077446915161));
#58571=CARTESIAN_POINT('Ctrl Pts',(2.78253202299393,0.301275253636565,14.3657553293696));
#58572=CARTESIAN_POINT('Ctrl Pts',(1.26786651939106,2.49514844158187,14.5237659672231));
#58573=CARTESIAN_POINT('Ctrl Pts',(-1.3971637764554,2.42511537310475,14.6817766050766));
#58574=CARTESIAN_POINT('Ctrl Pts',(-2.3546796192857,0.86935693510682,14.7900512466373));
#58575=CARTESIAN_POINT('Ctrl Pts',(-2.37542809022715,0.0443212886747152,
14.8456556755801));
#58576=CARTESIAN_POINT('Ctrl Pts',(-2.37524122474812,0.000775012007393572,
14.848589891905));
#58577=CARTESIAN_POINT('Origin',(0.,0.,-1.848589891905));
#58578=CARTESIAN_POINT('',(-2.37511086845159,0.000918633378760274,12.651410108095));
#58579=CARTESIAN_POINT('',(-2.36858116699997,0.0012122458443739,12.848589891905));
#58580=CARTESIAN_POINT('',(-2.37175,-3.45929798001232E-13,-1.848589891905));
#58581=CARTESIAN_POINT('Ctrl Pts',(-2.37511086845159,0.000918633378760338,
12.651410108095));
#58582=CARTESIAN_POINT('Ctrl Pts',(-2.37148323775257,-0.728623486345359,
12.700560627441));
#58583=CARTESIAN_POINT('Ctrl Pts',(-1.62239833212739,-2.24639384244693,
12.8023813594049));
#58584=CARTESIAN_POINT('Ctrl Pts',(0.955701160956647,-2.63056754962948,
12.9568723039866));
#58585=CARTESIAN_POINT('Ctrl Pts',(2.725406359655,-0.636718553952737,13.1148829418401));
#58586=CARTESIAN_POINT('Ctrl Pts',(2.02228695060197,1.93484000155462,13.2728935796935));
#58587=CARTESIAN_POINT('Ctrl Pts',(-0.515700465454569,2.75087320176898,
13.4309042175471));
#58588=CARTESIAN_POINT('Ctrl Pts',(-2.16866858426475,1.4094673473738,13.5570763936809));
#58589=CARTESIAN_POINT('Ctrl Pts',(-2.37010930485004,0.312630248252637,
13.6305783571968));
#58590=CARTESIAN_POINT('Ctrl Pts',(-2.36861602543199,0.00124154017382031,
13.651410108095));
#58591=CARTESIAN_POINT('Ctrl Pts',(-2.36858116699997,0.00121224584437404,
12.848589891905));
#58592=CARTESIAN_POINT('Ctrl Pts',(-2.36636513882711,-0.472499393714349,
12.8802797908327));
#58593=CARTESIAN_POINT('Ctrl Pts',(-1.9996810697703,-1.73670297725242,12.9646399023783));
#58594=CARTESIAN_POINT('Ctrl Pts',(0.0541653659420804,-2.79827042111378,
13.1016702265417));
#58595=CARTESIAN_POINT('Ctrl Pts',(2.37332474856975,-1.48343549715007,13.2596808643952));
#58596=CARTESIAN_POINT('Ctrl Pts',(2.53911136180312,1.17735497143754,13.4176915022487));
#58597=CARTESIAN_POINT('Ctrl Pts',(0.401103153710141,2.76990387866618,13.5757021401021));
#58598=CARTESIAN_POINT('Ctrl Pts',(-1.87317672244244,1.93302706793983,13.7193349366543));
#58599=CARTESIAN_POINT('Ctrl Pts',(-2.365935632993,0.568962550177037,13.8102975205886));
#58600=CARTESIAN_POINT('Ctrl Pts',(-2.37083142397042,-0.00207423906479159,
13.848589891905));
#58601=CARTESIAN_POINT('Origin',(0.,0.,-1.848589891905));
#58602=CARTESIAN_POINT('',(-2.37108122357944,-0.00209777019329237,11.651410108095));
#58603=CARTESIAN_POINT('',(-2.37507494215832,0.000954213469080735,11.848589891905));
#58604=CARTESIAN_POINT('',(-2.37175,-3.45929798001232E-13,-1.848589891905));
#58605=CARTESIAN_POINT('Ctrl Pts',(-2.37108122357943,-0.00209777019329208,
11.651410108095));
#58606=CARTESIAN_POINT('Ctrl Pts',(-2.37288020620416,-0.207721845931398,
11.6652024724495));
#58607=CARTESIAN_POINT('Ctrl Pts',(-2.25456795023167,-1.19654496148464,
11.7316650494219));
#58608=CARTESIAN_POINT('Ctrl Pts',(-0.875108611891469,-2.65846483136416,
11.8507978390121));
#58609=CARTESIAN_POINT('Ctrl Pts',(1.7485305153448,-2.18538128918389,12.0088084768656));
#58610=CARTESIAN_POINT('Ctrl Pts',(2.78568721934935,0.270549548438745,12.1668191147191));
#58611=CARTESIAN_POINT('Ctrl Pts',(1.29532508891864,2.48100448532931,12.3248297525726));
#58612=CARTESIAN_POINT('Ctrl Pts',(-1.37031563568376,2.44038632204184,12.4828403904261));
#58613=CARTESIAN_POINT('Ctrl Pts',(-2.35021221135085,0.886934755038215,
12.5917005089335));
#58614=CARTESIAN_POINT('Ctrl Pts',(-2.37537064490022,0.0531615094349561,
12.6478904148232));
#58615=CARTESIAN_POINT('Ctrl Pts',(-2.37511086845159,0.000918633378760338,
12.651410108095));
#58616=CARTESIAN_POINT('Ctrl Pts',(-2.37507494215832,0.000954213469080692,
11.848589891905));
#58617=CARTESIAN_POINT('Ctrl Pts',(-2.37133892558484,-0.72641217448684,
11.8975918484591));
#58618=CARTESIAN_POINT('Ctrl Pts',(-1.62620459990655,-2.24221827031134,
11.999264017631));
#58619=CARTESIAN_POINT('Ctrl Pts',(0.948330986936765,-2.63323367282349,
12.1536063994207));
#58620=CARTESIAN_POINT('Ctrl Pts',(2.72361280112762,-0.644348155896335,
12.3116170372742));
#58621=CARTESIAN_POINT('Ctrl Pts',(2.02769734494933,1.92916943624887,12.4696276751277));
#58622=CARTESIAN_POINT('Ctrl Pts',(-0.507995094910846,2.75230670893191,
12.6276383129812));
#58623=CARTESIAN_POINT('Ctrl Pts',(-2.16666393885777,1.41396091253342,12.753959051907));
#58624=CARTESIAN_POINT('Ctrl Pts',(-2.37004828957801,0.314833277557734,
12.8276095782149));
#58625=CARTESIAN_POINT('Ctrl Pts',(-2.36858116699997,0.00121224584437404,
12.848589891905));
#58626=CARTESIAN_POINT('Origin',(0.,0.,-1.848589891905));
#58627=CARTESIAN_POINT('',(-2.36845164206684,0.00109356539350533,10.651410108095));
#58628=CARTESIAN_POINT('',(-2.3711455013324,-0.00210217670305768,10.848589891905));
#58629=CARTESIAN_POINT('',(-2.37175,-3.45929798001232E-13,-1.848589891905));
#58630=CARTESIAN_POINT('Ctrl Pts',(-2.36845164206685,0.00109356539350527,
10.651410108095));
#58631=CARTESIAN_POINT('Ctrl Pts',(-2.36649596032256,-0.463929808682954,
10.6825145300759));
#58632=CARTESIAN_POINT('Ctrl Pts',(-2.0100003207014,-1.71916135585423,10.7662891646746));
#58633=CARTESIAN_POINT('Ctrl Pts',(0.0232810353625256,-2.79869761417686,
10.9027340118911));
#58634=CARTESIAN_POINT('Ctrl Pts',(2.35680925566857,-1.50953650986048,11.0607446497446));
#58635=CARTESIAN_POINT('Ctrl Pts',(2.5519495975734,1.1492621953461,11.2187552875981));
#58636=CARTESIAN_POINT('Ctrl Pts',(0.431646688134689,2.76530856846557,11.3767659254516));
#58637=CARTESIAN_POINT('Ctrl Pts',(-1.86103764780764,1.95027239682527,11.5209841989506));
#58638=CARTESIAN_POINT('Ctrl Pts',(-2.36601026027579,0.577514355061797,
11.6125322598317));
#58639=CARTESIAN_POINT('Ctrl Pts',(-2.37108122357943,-0.00209777019329208,
11.651410108095));
#58640=CARTESIAN_POINT('Ctrl Pts',(-2.3711455013324,-0.00210217670305756,
10.848589891905));
#58641=CARTESIAN_POINT('Ctrl Pts',(-2.37293293087196,-0.205497384262076,
10.8622336934676));
#58642=CARTESIAN_POINT('Ctrl Pts',(-2.25619484795045,-1.19205465912958,
10.928547707648));
#58643=CARTESIAN_POINT('Ctrl Pts',(-0.882549833739827,-2.656003958476,11.0475319344462));
#58644=CARTESIAN_POINT('Ctrl Pts',(1.74240395044783,-2.190269323608,11.2055425722998));
#58645=CARTESIAN_POINT('Ctrl Pts',(2.78643408629422,0.262747634075224,11.3635532101532));
#58646=CARTESIAN_POINT('Ctrl Pts',(1.3022677379473,2.47736754947181,11.5215638480067));
#58647=CARTESIAN_POINT('Ctrl Pts',(-1.36347643158376,2.44421424122154,11.6795744858602));
#58648=CARTESIAN_POINT('Ctrl Pts',(-2.34906262124821,0.891396457168339,
11.7885831671597));
#58649=CARTESIAN_POINT('Ctrl Pts',(-2.37535461804095,0.0554044099680877,
11.8449216358413));
#58650=CARTESIAN_POINT('Ctrl Pts',(-2.37507494215832,0.000954213469080692,
11.848589891905));
#58651=CARTESIAN_POINT('Origin',(0.,0.,-1.848589891905));
#58652=CARTESIAN_POINT('',(-2.37492150693046,0.00109068279076694,9.65141010809499));
#58653=CARTESIAN_POINT('',(-2.36842114142019,0.00106267303466426,9.84858989190503));
#58654=CARTESIAN_POINT('',(-2.37175,-3.45929798001232E-13,-1.848589891905));
#58655=CARTESIAN_POINT('Ctrl Pts',(-2.37492150693046,0.00109068279076715,
9.65141010809499));
#58656=CARTESIAN_POINT('Ctrl Pts',(-2.37079040527034,-0.71770812112247,
9.69982658770222));
#58657=CARTESIAN_POINT('Ctrl Pts',(-1.64110086305732,-2.22572615427059,
9.80091327992728));
#58658=CARTESIAN_POINT('Ctrl Pts',(0.919213459631522,-2.64353871880838,
9.95467018477016));
#58659=CARTESIAN_POINT('Ctrl Pts',(2.71633592014881,-0.674366006791661,
10.1126808226237));
#58660=CARTESIAN_POINT('Ctrl Pts',(2.04886359373486,1.90667467504938,10.2706914604772));
#58661=CARTESIAN_POINT('Ctrl Pts',(-0.477590346402141,2.75774505769302,
10.4287020983307));
#58662=CARTESIAN_POINT('Ctrl Pts',(-2.15868340525892,1.43166769474736,10.5556083142033));
#58663=CARTESIAN_POINT('Ctrl Pts',(-2.36980758506028,0.323510639492646,
10.629844317458));
#58664=CARTESIAN_POINT('Ctrl Pts',(-2.36845164206685,0.00109356539350527,
10.651410108095));
#58665=CARTESIAN_POINT('Ctrl Pts',(-2.36842114142019,0.00106267303466433,
9.84858989190503));
#58666=CARTESIAN_POINT('Ctrl Pts',(-2.36653124713118,-0.461754654170688,
9.87954575109394));
#58667=CARTESIAN_POINT('Ctrl Pts',(-2.01259622806101,-1.71470763772158,
9.96317182290069));
#58668=CARTESIAN_POINT('Ctrl Pts',(0.0154436428957695,-2.79875199515222,
10.0994681073253));
#58669=CARTESIAN_POINT('Ctrl Pts',(2.35257293505637,-1.51613054243843,10.2574787451788));
#58670=CARTESIAN_POINT('Ctrl Pts',(2.5551580610824,1.14211143036047,10.4154893830323));
#58671=CARTESIAN_POINT('Ctrl Pts',(0.439388822165221,2.7640891265353,10.5735000208858));
#58672=CARTESIAN_POINT('Ctrl Pts',(-1.85793312538704,1.9546434259417,10.7178668571767));
#58673=CARTESIAN_POINT('Ctrl Pts',(-2.36603277965999,0.579684720479897,
10.8095634808498));
#58674=CARTESIAN_POINT('Ctrl Pts',(-2.3711455013324,-0.00210217670305756,
10.848589891905));
#58675=CARTESIAN_POINT('Origin',(0.,0.,-1.848589891905));
#58676=CARTESIAN_POINT('',(-2.37140051282111,-0.00211329452352801,8.65141010809499));
#58677=CARTESIAN_POINT('',(-2.37488002645211,0.00112430501927618,8.84858989190502));
#58678=CARTESIAN_POINT('',(-2.37175,-3.45929798001232E-13,-1.848589891905));
#58679=CARTESIAN_POINT('Ctrl Pts',(-2.37140051282111,-0.00211329452352778,
8.65141010809499));
#58680=CARTESIAN_POINT('Ctrl Pts',(-2.37313643726488,-0.196727040066591,
8.66446843271073));
#58681=CARTESIAN_POINT('Ctrl Pts',(-2.2625332649159,-1.17436088610827,8.7301969699443));
#58682=CARTESIAN_POINT('Ctrl Pts',(-0.911807050875725,-2.64610246290276,
8.8485957197957));
#58683=CARTESIAN_POINT('Ctrl Pts',(1.7181264684868,-2.20936456486744,9.0066063576492));
#58684=CARTESIAN_POINT('Ctrl Pts',(2.78916386380546,0.231981212706065,9.16461699550269));
#58685=CARTESIAN_POINT('Ctrl Pts',(1.32952798427551,2.46284503800688,9.32262763335619));
#58686=CARTESIAN_POINT('Ctrl Pts',(-1.33641957225244,2.45911225223807,9.48063827120967));
#58687=CARTESIAN_POINT('Ctrl Pts',(-2.3444674266217,0.908984670945501,9.59023242945595));
#58688=CARTESIAN_POINT('Ctrl Pts',(-2.37528445367183,0.0642422837537755,
9.64715637508439));
#58689=CARTESIAN_POINT('Ctrl Pts',(-2.37492150693046,0.00109068279076715,
9.65141010809499));
#58690=CARTESIAN_POINT('Ctrl Pts',(-2.37488002645211,0.00112430501927616,
8.84858989190502));
#58691=CARTESIAN_POINT('Ctrl Pts',(-2.3706566377328,-0.715502201037878,
8.89685780872028));
#58692=CARTESIAN_POINT('Ctrl Pts',(-1.64485462669885,-2.22153253962258,
8.99779593815339));
#58693=CARTESIAN_POINT('Ctrl Pts',(0.911807102923268,-2.64610261394623,
9.1514042802043));
#58694=CARTESIAN_POINT('Ctrl Pts',(2.71443697103106,-0.681970062960328,
9.30941491805779));
#58695=CARTESIAN_POINT('Ctrl Pts',(2.05419501292893,1.90092979495096,9.46742555591129));
#58696=CARTESIAN_POINT('Ctrl Pts',(-0.469865879588134,2.75907181705611,
9.62543619376478));
#58697=CARTESIAN_POINT('Ctrl Pts',(-2.15663822083001,1.4361603528293,9.75249097242936));
#58698=CARTESIAN_POINT('Ctrl Pts',(-2.36974683011402,0.325711359237552,
9.82687553847611));
#58699=CARTESIAN_POINT('Ctrl Pts',(-2.36842114142019,0.00106267303466433,
9.84858989190503));
#58700=CARTESIAN_POINT('Origin',(0.,0.,-1.848589891905));
#58701=CARTESIAN_POINT('',(-2.36830911924029,0.000938119109969627,7.65141010809499));
#58702=CARTESIAN_POINT('',(-2.37146590747834,-0.00211451867861201,7.84858989190503));
#58703=CARTESIAN_POINT('',(-2.37175,-3.45929798001232E-13,-1.848589891905));
#58704=CARTESIAN_POINT('Ctrl Pts',(-2.36830911924029,0.000938119109969611,
7.65141010809499));
#58705=CARTESIAN_POINT('Ctrl Pts',(-2.36667687882826,-0.453179513046169,
7.68178049033708));
#58706=CARTESIAN_POINT('Ctrl Pts',(-2.02273688266497,-1.69714509888228,
7.764821085197));
#58707=CARTESIAN_POINT('Ctrl Pts',(-0.0154436420140344,-2.79875183539522,
7.90053189267472));
#58708=CARTESIAN_POINT('Ctrl Pts',(2.33569789249813,-1.54200055031981,8.05854253052824));
#58709=CARTESIAN_POINT('Ctrl Pts',(2.56760637965517,1.11384371496224,8.21655316838172));
#58710=CARTESIAN_POINT('Ctrl Pts',(0.469865852767273,2.75907165956415,8.37456380623522));
#58711=CARTESIAN_POINT('Ctrl Pts',(-1.84560131583056,1.97184830688283,8.51951611947298));
#58712=CARTESIAN_POINT('Ctrl Pts',(-2.36613465776925,0.588239458909152,
8.6117982200929));
#58713=CARTESIAN_POINT('Ctrl Pts',(-2.37140051282111,-0.00211329452352778,
8.65141010809499));
#58714=CARTESIAN_POINT('Ctrl Pts',(-2.37146590747834,-0.00211451867861227,
7.84858989190503));
#58715=CARTESIAN_POINT('Ctrl Pts',(-2.37318729871088,-0.194500654570986,
7.8614996537288));
#58716=CARTESIAN_POINT('Ctrl Pts',(-2.26412346336896,-1.16987191915567,
7.92707962817041));
#58717=CARTESIAN_POINT('Ctrl Pts',(-0.919213512101427,-2.64353886970564,
8.04532981522984));
#58718=CARTESIAN_POINT('Ctrl Pts',(1.71193285976134,-2.21416736498029,8.20334045308334));
#58719=CARTESIAN_POINT('Ctrl Pts',(2.78980271289629,0.224169711582251,8.36135109093682));
#58720=CARTESIAN_POINT('Ctrl Pts',(1.33641964853712,2.45911239260802,8.51936172879032));
#58721=CARTESIAN_POINT('Ctrl Pts',(-1.32952806016717,2.4628451785897,8.67737236664382));
#58722=CARTESIAN_POINT('Ctrl Pts',(-2.34328526325323,0.913448987581096,
8.78711508768204));
#58723=CARTESIAN_POINT('Ctrl Pts',(-2.37526522240956,0.0664845291139092,
8.84418759610245));
#58724=CARTESIAN_POINT('Ctrl Pts',(-2.37488002645211,0.00112430501927616,
8.84858989190502));
#58725=CARTESIAN_POINT('Origin',(0.,0.,-1.848589891905));
#58726=CARTESIAN_POINT('',(-2.37470588355431,0.00125253531034594,6.65141010809499));
#58727=CARTESIAN_POINT('',(-2.36828313834817,0.000905845531651017,6.84858989190503));
#58728=CARTESIAN_POINT('',(-2.37175,-3.45929798001232E-13,-1.848589891905));
#58729=CARTESIAN_POINT('Ctrl Pts',(-2.37470588355431,0.00125253531034581,
6.65141010809499));
#58730=CARTESIAN_POINT('Ctrl Pts',(-2.37014919057747,-0.706818549760696,
6.69909254796341));
#58731=CARTESIAN_POINT('Ctrl Pts',(-1.65954441580295,-2.20497060362383,
6.79944520044968));
#58732=CARTESIAN_POINT('Ctrl Pts',(0.882549783362729,-2.65600380686722,
6.95246806555376));
#58733=CARTESIAN_POINT('Ctrl Pts',(2.70674546316629,-0.711884358470874,
7.11047870340726));
#58734=CARTESIAN_POINT('Ctrl Pts',(2.07504800081977,1.87814433324509,7.26848934126075));
#58735=CARTESIAN_POINT('Ctrl Pts',(-0.439388797084447,2.76408896875688,
7.42649997911426));
#58736=CARTESIAN_POINT('Ctrl Pts',(-2.1484972136029,1.45386303251217,7.55414023472565));
#58737=CARTESIAN_POINT('Ctrl Pts',(-2.36950761203602,0.334379630876223,
7.62911027771924));
#58738=CARTESIAN_POINT('Ctrl Pts',(-2.36830911924029,0.000938119109969611,
7.65141010809499));
#58739=CARTESIAN_POINT('Ctrl Pts',(-2.36828313834817,0.000905845531651017,
6.84858989190503));
#58740=CARTESIAN_POINT('Ctrl Pts',(-2.36671578067491,-0.451002880761427,
6.87881171135515));
#58741=CARTESIAN_POINT('Ctrl Pts',(-2.02528764799729,-1.69268627108249,
6.96170374342309));
#58742=CARTESIAN_POINT('Ctrl Pts',(-0.0232810366912258,-2.79869777393076,
7.09726598810887));
#58743=CARTESIAN_POINT('Ctrl Pts',(2.331370743134,-1.54853533848382,7.25527662596236));
#58744=CARTESIAN_POINT('Ctrl Pts',(2.57071559891088,1.1066492425293,7.41328726381586));
#58745=CARTESIAN_POINT('Ctrl Pts',(0.477590373663518,2.75774521510932,7.57129790166936));
#58746=CARTESIAN_POINT('Ctrl Pts',(-1.84244773179659,1.9762088147049,7.71639877769907));
#58747=CARTESIAN_POINT('Ctrl Pts',(-2.36616423790973,0.590410703244725,
7.80882944111097));
#58748=CARTESIAN_POINT('Ctrl Pts',(-2.37146590747834,-0.00211451867861227,
7.84858989190503));
#58749=CARTESIAN_POINT('Origin',(0.,0.,-1.848589891905));
#58750=CARTESIAN_POINT('',(-2.37172448707781,-0.00211299049637275,5.65141010809499));
#58751=CARTESIAN_POINT('',(-2.37465944643639,0.00128394040524511,5.84858989190503));
#58752=CARTESIAN_POINT('',(-2.37175,-3.45929798001232E-13,-1.848589891905));
#58753=CARTESIAN_POINT('Ctrl Pts',(-2.37172448707781,-0.00211299049637291,
5.65141010809499));
#58754=CARTESIAN_POINT('Ctrl Pts',(-2.37338315552618,-0.185722875755726,
5.66373439297193));
#58755=CARTESIAN_POINT('Ctrl Pts',(-2.27031792652184,-1.15218371715246,
5.7287288904667));
#58756=CARTESIAN_POINT('Ctrl Pts',(-0.948330932804408,-2.6332335225146,
5.84639360057931));
#58757=CARTESIAN_POINT('Ctrl Pts',(1.68739350215265,-2.23292487806895,6.00440423843279));
#58758=CARTESIAN_POINT('Ctrl Pts',(2.79210654854793,0.193368466308401,6.1624148762863));
#58759=CARTESIAN_POINT('Ctrl Pts',(1.3634763537543,2.4442141017022,6.32042551413978));
#58760=CARTESIAN_POINT('Ctrl Pts',(-1.30226766361206,2.47736740805983,6.47843615199329));
#58761=CARTESIAN_POINT('Ctrl Pts',(-2.33856111575396,0.931047401636643,
6.58876434997835));
#58762=CARTESIAN_POINT('Ctrl Pts',(-2.37518253175268,0.0753195854131474,
6.64642233534558));
#58763=CARTESIAN_POINT('Ctrl Pts',(-2.37470588355431,0.00125253531034581,
6.65141010809499));
#58764=CARTESIAN_POINT('Ctrl Pts',(-2.37465944643639,0.00128394040524508,
5.84858989190503));
#58765=CARTESIAN_POINT('Ctrl Pts',(-2.37002572147023,-0.704617592835783,
5.89612376898149));
#58766=CARTESIAN_POINT('Ctrl Pts',(-1.66324590363498,-2.20075959342016,
5.99632785867577));
#58767=CARTESIAN_POINT('Ctrl Pts',(0.875108661844196,-2.6584649831133,6.14920216098791));
#58768=CARTESIAN_POINT('Ctrl Pts',(2.70474148699564,-0.719461413141105,
6.30721279884139));
#58769=CARTESIAN_POINT('Ctrl Pts',(2.0802994242073,1.87232623816396,6.4652234366949));
#58770=CARTESIAN_POINT('Ctrl Pts',(-0.431646712773937,2.76530872631355,
6.62323407454837));
#58771=CARTESIAN_POINT('Ctrl Pts',(-2.14641112738202,1.45835451677764,6.75102289295177));
#58772=CARTESIAN_POINT('Ctrl Pts',(-2.36944735221498,0.336578050194668,
6.82614149873732));
#58773=CARTESIAN_POINT('Ctrl Pts',(-2.36828313834817,0.000905845531651017,
6.84858989190503));
#58774=CARTESIAN_POINT('Origin',(0.,0.,-1.848589891905));
#58775=CARTESIAN_POINT('',(-2.36818920823751,0.000776286799690231,4.65141010809499));
#58776=CARTESIAN_POINT('',(-2.37179057180682,-0.00211098337720095,4.84858989190502));
#58777=CARTESIAN_POINT('',(-2.37175,-3.45929798001232E-13,-1.848589891905));
#58778=CARTESIAN_POINT('Ctrl Pts',(-2.36818920823751,0.00077628679969001,
4.65141010809499));
#58779=CARTESIAN_POINT('Ctrl Pts',(-2.36687509819612,-0.442421667272658,
4.68104645059827));
#58780=CARTESIAN_POINT('Ctrl Pts',(-2.03525109051103,-1.67510437567302,
4.76335300571939));
#58781=CARTESIAN_POINT('Ctrl Pts',(-0.054165362850041,-2.79827026138436,
4.89832977345834));
#58782=CARTESIAN_POINT('Ctrl Pts',(2.3141393814959,-1.57416938897968,5.05634041131182));
#58783=CARTESIAN_POINT('Ctrl Pts',(2.58277161716087,1.07821199946199,5.21435104916533));
#58784=CARTESIAN_POINT('Ctrl Pts',(0.50799506591352,2.75230655182614,5.37236168701881));
#58785=CARTESIAN_POINT('Ctrl Pts',(-1.82992197413507,1.99337119126977,5.51804803999537));
#58786=CARTESIAN_POINT('Ctrl Pts',(-2.36629451543789,0.598969444481106,
5.61106418035409));
#58787=CARTESIAN_POINT('Ctrl Pts',(-2.37172448707781,-0.00211299049637291,
5.65141010809499));
#58788=CARTESIAN_POINT('Ctrl Pts',(-2.37179057180682,-0.00211098337720095,
4.84858989190503));
#58789=CARTESIAN_POINT('Ctrl Pts',(-2.37343199969618,-0.183494640583722,
4.86076561399));
#58790=CARTESIAN_POINT('Ctrl Pts',(-2.27187176921823,-1.14769623702431,
4.9256115486928));
#58791=CARTESIAN_POINT('Ctrl Pts',(-0.955701215509313,-2.63056769978633,
5.04312769601343));
#58792=CARTESIAN_POINT('Ctrl Pts',(1.68113403530831,-2.23764152441791,5.20113833386694));
#58793=CARTESIAN_POINT('Ctrl Pts',(2.79263725748281,0.185548873863724,5.35914897172042));
#58794=CARTESIAN_POINT('Ctrl Pts',(1.37031571390328,2.44038646134289,5.51715960957393));
#58795=CARTESIAN_POINT('Ctrl Pts',(-1.29532516285794,2.48100462694871,5.67517024742741));
#58796=CARTESIAN_POINT('Ctrl Pts',(-2.33734608113232,0.935514281942727,
5.78564700820446));
#58797=CARTESIAN_POINT('Ctrl Pts',(-2.37516014967577,0.0775610580504524,
5.84345355636366));
#58798=CARTESIAN_POINT('Ctrl Pts',(-2.37465944643639,0.00128394040524508,
5.84858989190503));
#58799=CARTESIAN_POINT('Origin',(0.,0.,-1.848589891905));
#58800=CARTESIAN_POINT('',(-2.37446693265003,0.00140297001510288,3.65141010809499));
#58801=CARTESIAN_POINT('',(-2.36816788418401,0.000742855737058956,3.84858989190502));
#58802=CARTESIAN_POINT('',(-2.37175,-3.45929798001232E-13,-1.848589891905));
#58803=CARTESIAN_POINT('Ctrl Pts',(-2.37446693265003,0.00140297001510294,
3.65141010809499));
#58804=CARTESIAN_POINT('Ctrl Pts',(-2.36955836583972,-0.695952680709234,
3.69835850822461));
#58805=CARTESIAN_POINT('Ctrl Pts',(-1.67773013376393,-2.18413036676016,
3.79797712097207));
#58806=CARTESIAN_POINT('Ctrl Pts',(0.845717150955885,-2.66796042811686,
3.95026594633737));
#58807=CARTESIAN_POINT('Ctrl Pts',(2.69663682477438,-0.749266426116641,
4.10827658419086));
#58808=CARTESIAN_POINT('Ctrl Pts',(2.10083515905894,1.84925443784418,4.26628722204435));
#58809=CARTESIAN_POINT('Ctrl Pts',(-0.401103130814736,2.76990372055638,
4.42429785989785));
#58810=CARTESIAN_POINT('Ctrl Pts',(-2.13810821622223,1.47605202244459,4.55267215524806));
#58811=CARTESIAN_POINT('Ctrl Pts',(-2.36921055694159,0.345237284576487,
4.62837623798044));
#58812=CARTESIAN_POINT('Ctrl Pts',(-2.36818920823751,0.00077628679969001,
4.65141010809499));
#58813=CARTESIAN_POINT('Ctrl Pts',(-2.36816788418401,0.000742855737058887,
3.84858989190502));
#58814=CARTESIAN_POINT('Ctrl Pts',(-2.36691733101876,-0.440243431773009,
3.87807767161634));
#58815=CARTESIAN_POINT('Ctrl Pts',(-2.03775706613953,-1.67064082881644,
3.96023566394549));
#58816=CARTESIAN_POINT('Ctrl Pts',(-0.0620012593698648,-2.79810776790365,
4.09506386889247));
#58817=CARTESIAN_POINT('Ctrl Pts',(2.30972223178794,-1.58064368166609,4.25307450674597));
#58818=CARTESIAN_POINT('Ctrl Pts',(2.58578099692394,1.07097519687693,4.41108514459946));
#58819=CARTESIAN_POINT('Ctrl Pts',(0.515700494891298,2.75087335879294,4.56909578245295));
#58820=CARTESIAN_POINT('Ctrl Pts',(-1.8267190231715,1.99772065067605,4.71493069822147));
#58821=CARTESIAN_POINT('Ctrl Pts',(-2.36633144702867,0.6011418453507,4.80809540137217));
#58822=CARTESIAN_POINT('Ctrl Pts',(-2.37179057180682,-0.00211098337720095,
4.84858989190503));
#58823=CARTESIAN_POINT('Origin',(0.,0.,-1.848589891905));
#58824=CARTESIAN_POINT('',(-2.37205100032703,-0.00209666035588911,2.65141010809498));
#58825=CARTESIAN_POINT('',(-2.37441612858142,0.0014319253334924,2.84858989190502));
#58826=CARTESIAN_POINT('',(-2.37175,-3.45929798001232E-13,-1.848589891905));
#58827=CARTESIAN_POINT('Ctrl Pts',(-2.37205100032703,-0.00209666035588935,
2.65141010809498));
#58828=CARTESIAN_POINT('Ctrl Pts',(-2.37361961794304,-0.17470974391043,
2.66300035323312));
#58829=CARTESIAN_POINT('Ctrl Pts',(-2.27792363918998,-1.13001425292593,
2.7272608109891));
#58830=CARTESIAN_POINT('Ctrl Pts',(-0.984673254710223,-2.61986041464368,
2.8441914813629));
#58831=CARTESIAN_POINT('Ctrl Pts',(1.65633749422688,-2.25605774937986,3.0022021192164));
#58832=CARTESIAN_POINT('Ctrl Pts',(2.79451471318987,0.154718717530414,3.16021275706989));
#58833=CARTESIAN_POINT('Ctrl Pts',(1.39716369670102,2.42511523463794,3.31822339492339));
#58834=CARTESIAN_POINT('Ctrl Pts',(-1.2678664470183,2.49514829917553,3.47623403277688));
#58835=CARTESIAN_POINT('Ctrl Pts',(-2.33249179703478,0.953122680262559,
3.58729627050075));
#58836=CARTESIAN_POINT('Ctrl Pts',(-2.37506516174403,0.0863928367627885,
3.64568829560678));
#58837=CARTESIAN_POINT('Ctrl Pts',(-2.37446693265003,0.00140297001510294,
3.65141010809499));
#58838=CARTESIAN_POINT('Ctrl Pts',(-2.37441612858142,0.00143192533349229,
2.84858989190502));
#58839=CARTESIAN_POINT('Ctrl Pts',(-2.36944494516981,-0.693756276209885,
2.89538972924268));
#58840=CARTESIAN_POINT('Ctrl Pts',(-1.68137957932541,-2.17990259172208,
2.99485977919817));
#58841=CARTESIAN_POINT('Ctrl Pts',(0.838242687746051,-2.6703184178973,3.1470000417715));
#58842=CARTESIAN_POINT('Ctrl Pts',(2.69452820593443,-0.756815026848842,
3.305010679625));
#58843=CARTESIAN_POINT('Ctrl Pts',(2.10600558091548,1.8433642406156,3.46302131747849));
#58844=CARTESIAN_POINT('Ctrl Pts',(-0.393344910955346,2.77101624331114,
3.62103195533199));
#58845=CARTESIAN_POINT('Ctrl Pts',(-2.13598086517564,1.48054205574855,3.74955481347416));
#58846=CARTESIAN_POINT('Ctrl Pts',(-2.36915103263171,0.347433421218035,
3.82540745899851));
#58847=CARTESIAN_POINT('Ctrl Pts',(-2.36816788418401,0.000742855737058887,
3.84858989190502));
#58848=CARTESIAN_POINT('Origin',(0.,0.,-1.848589891905));
#58849=CARTESIAN_POINT('',(-2.36809210481233,0.000611552607929038,1.65141010809499));
#58850=CARTESIAN_POINT('',(-2.37211733643984,-0.00209141235254701,1.84858989190502));
#58851=CARTESIAN_POINT('',(-2.37175,-3.45929798001232E-13,-1.848589891905));
#58852=CARTESIAN_POINT('Ctrl Pts',(-2.36809210481233,0.000611552607929014,
1.65141010809499));
#58853=CARTESIAN_POINT('Ctrl Pts',(-2.36708900480144,-0.431654494041978,
1.68031241085947));
#58854=CARTESIAN_POINT('Ctrl Pts',(-2.04754546137161,-1.65304532360689,
1.76188492624178));
#58855=CARTESIAN_POINT('Ctrl Pts',(-0.0928761899139844,-2.79725011229448,
1.89612765424193));
#58856=CARTESIAN_POINT('Ctrl Pts',(2.29213757529781,-1.60603837127393,2.05413829209543));
#58857=CARTESIAN_POINT('Ctrl Pts',(2.59744255060163,1.04237465766208,2.21214892994892));
#58858=CARTESIAN_POINT('Ctrl Pts',(0.546026952813309,2.74501412804214,2.37015956780242));
#58859=CARTESIAN_POINT('Ctrl Pts',(-1.81399809354475,2.0148385946783,2.51657996051777));
#58860=CARTESIAN_POINT('Ctrl Pts',(-2.36649125936507,0.609705745415088,
2.61033014061529));
#58861=CARTESIAN_POINT('Ctrl Pts',(-2.37205100032703,-0.00209666035588935,
2.65141010809498));
#58862=CARTESIAN_POINT('Ctrl Pts',(-2.37211733643984,-0.00209141235254718,
1.84858989190502));
#58863=CARTESIAN_POINT('Ctrl Pts',(-2.37366633030799,-0.172479818929997,
1.8600315742512));
#58864=CARTESIAN_POINT('Ctrl Pts',(-2.27944161784295,-1.12552878575702,
1.9241434692152));
#58865=CARTESIAN_POINT('Ctrl Pts',(-0.992005816601449,-2.617092539026,2.04092557679704));
#58866=CARTESIAN_POINT('Ctrl Pts',(1.65001329883352,-2.26068751370113,2.19893621465053));
#58867=CARTESIAN_POINT('Ctrl Pts',(2.79493721635935,0.146892622206337,2.35694685250402));
#58868=CARTESIAN_POINT('Ctrl Pts',(1.40394942456389,2.42119328420925,2.51495749035753));
#58869=CARTESIAN_POINT('Ctrl Pts',(-1.26087427680964,2.49868913935238,2.67296812821101));
#58870=CARTESIAN_POINT('Ctrl Pts',(-2.33124358910813,0.957592063764426,
2.78417892872685));
#58871=CARTESIAN_POINT('Ctrl Pts',(-2.3750396929755,0.0886334171669318,
2.84271951662485));
#58872=CARTESIAN_POINT('Ctrl Pts',(-2.37441612858142,0.00143192533349229,
2.84858989190502));
#58873=CARTESIAN_POINT('Origin',(0.,0.,-1.848589891905));
#58874=CARTESIAN_POINT('',(-2.37417832678934,0.00170073231846648,0.651410108094986));
#58875=CARTESIAN_POINT('',(-2.36807033412218,0.000590439285148986,0.848589891905023));
#58876=CARTESIAN_POINT('',(-2.37175,-3.45929798001232E-13,-1.848589891905));
#58877=CARTESIAN_POINT('Ctrl Pts',(-2.37417832678934,0.00170073231846661,
0.651410108094986));
#58878=CARTESIAN_POINT('Ctrl Pts',(-2.36898203260896,-0.684918424266715,
0.697624468485814));
#58879=CARTESIAN_POINT('Ctrl Pts',(-1.69570475500353,-2.16345817758698,
0.796509041494473));
#58880=CARTESIAN_POINT('Ctrl Pts',(0.80874805201177,-2.67926694285025,0.948063827120964));
#58881=CARTESIAN_POINT('Ctrl Pts',(2.68599862008771,-0.786578017594937,
1.10607446497446));
#58882=CARTESIAN_POINT('Ctrl Pts',(2.12622710642163,1.82004872489232,1.26408510282796));
#58883=CARTESIAN_POINT('Ctrl Pts',(-0.362744329120993,2.775168194831,1.42209574068145));
#58884=CARTESIAN_POINT('Ctrl Pts',(-2.12751372443616,1.49823817530827,1.55120407577046));
#58885=CARTESIAN_POINT('Ctrl Pts',(-2.36891700761771,0.356087049254629,
1.62764219824164));
#58886=CARTESIAN_POINT('Ctrl Pts',(-2.36809210481233,0.000611552607929014,
1.65141010809499));
#58887=CARTESIAN_POINT('Ctrl Pts',(-2.36807033412218,0.000590439285148986,
0.848589891905023));
#58888=CARTESIAN_POINT('Ctrl Pts',(-2.36713171325374,-0.429468009012812,
0.87734363187754));
#58889=CARTESIAN_POINT('Ctrl Pts',(-2.05001637623951,-1.64860125877915,
0.958767584467889));
#58890=CARTESIAN_POINT('Ctrl Pts',(-0.1007027086929,-2.79696300482839,1.09286174967607));
#58891=CARTESIAN_POINT('Ctrl Pts',(2.28762793115499,-1.61245941657473,1.25087238752956));
#58892=CARTESIAN_POINT('Ctrl Pts',(2.6003532631254,1.03510135356512,1.40888302538306));
#58893=CARTESIAN_POINT('Ctrl Pts',(0.553710899450507,2.74347213477777,1.56689366323655));
#58894=CARTESIAN_POINT('Ctrl Pts',(-1.81074509731807,2.0191774297212,1.71346261874387));
#58895=CARTESIAN_POINT('Ctrl Pts',(-2.36653574986442,0.611879799745258,
1.80736136163337));
#58896=CARTESIAN_POINT('Ctrl Pts',(-2.37211733643984,-0.00209141235254718,
1.84858989190502));
#58897=CARTESIAN_POINT('Origin',(-0.866025403784439,-1.5,0.));
#58898=CARTESIAN_POINT('',(-0.866025403784439,-1.5,0.));
#58899=CARTESIAN_POINT('',(0.866025403784439,-1.5,0.));
#58900=CARTESIAN_POINT('',(-0.43301270189222,-1.5,0.));
#58901=CARTESIAN_POINT('',(-0.866025403784439,-1.5,3.));
#58902=CARTESIAN_POINT('',(-0.866025403784439,-1.5,0.));
#58903=CARTESIAN_POINT('',(0.866025403784439,-1.5,3.));
#58904=CARTESIAN_POINT('',(-0.866025403784439,-1.5,3.));
#58905=CARTESIAN_POINT('',(0.866025403784439,-1.5,0.));
#58906=CARTESIAN_POINT('Origin',(-1.73205080756888,2.12115047744981E-16,
0.));
#58907=CARTESIAN_POINT('',(-1.73205080756888,2.12115047744981E-16,0.));
#58908=CARTESIAN_POINT('',(-1.51554445662277,-0.375,0.));
#58909=CARTESIAN_POINT('',(-1.73205080756888,2.77555756156289E-16,3.));
#58910=CARTESIAN_POINT('',(-1.73205080756888,2.12115047744981E-16,0.));
#58911=CARTESIAN_POINT('',(-1.73205080756888,2.12115047744981E-16,3.));
#58912=CARTESIAN_POINT('Origin',(-0.866025403784438,1.5,0.));
#58913=CARTESIAN_POINT('',(-0.866025403784438,1.5,0.));
#58914=CARTESIAN_POINT('',(-1.08253175473055,1.125,0.));
#58915=CARTESIAN_POINT('',(-0.866025403784438,1.5,3.));
#58916=CARTESIAN_POINT('',(-0.866025403784438,1.5,0.));
#58917=CARTESIAN_POINT('',(-0.866025403784438,1.5,3.));
#58918=CARTESIAN_POINT('Origin',(0.866025403784439,1.5,0.));
#58919=CARTESIAN_POINT('',(0.866025403784439,1.5,0.));
#58920=CARTESIAN_POINT('',(0.43301270189222,1.5,0.));
#58921=CARTESIAN_POINT('',(0.866025403784439,1.5,3.));
#58922=CARTESIAN_POINT('',(0.866025403784439,1.5,0.));
#58923=CARTESIAN_POINT('',(0.866025403784439,1.5,3.));
#58924=CARTESIAN_POINT('Origin',(1.73205080756888,0.,0.));
#58925=CARTESIAN_POINT('',(1.73205080756888,0.,0.));
#58926=CARTESIAN_POINT('',(1.51554445662277,0.375,0.));
#58927=CARTESIAN_POINT('',(1.73205080756888,0.,3.));
#58928=CARTESIAN_POINT('',(1.73205080756888,0.,0.));
#58929=CARTESIAN_POINT('',(1.73205080756888,0.,3.));
#58930=CARTESIAN_POINT('Origin',(0.866025403784439,-1.5,0.));
#58931=CARTESIAN_POINT('',(1.08253175473055,-1.125,0.));
#58932=CARTESIAN_POINT('',(0.866025403784439,-1.5,3.));
#58933=CARTESIAN_POINT('Origin',(0.,2.77555756156289E-16,3.));
#58934=CARTESIAN_POINT('Ctrl Pts',(-1.03908919352512,2.13201587949042,-0.329233991005384));
#58935=CARTESIAN_POINT('Ctrl Pts',(-1.74465150592227,1.78814312449682,-0.276563778387552));
#58936=CARTESIAN_POINT('Ctrl Pts',(-2.77586045906315,0.351246257520133,
-0.171223353151889));
#58937=CARTESIAN_POINT('Ctrl Pts',(-1.80897499257101,-2.13797378108051,
-0.0132127152983944));
#58938=CARTESIAN_POINT('Ctrl Pts',(0.801552232242426,-2.68072923420017,
0.1447979225551));
#58939=CARTESIAN_POINT('Ctrl Pts',(2.68362344803569,-0.794509576969642,
0.302808560408595));
#58940=CARTESIAN_POINT('Ctrl Pts',(2.13140048014165,1.81430348231616,0.46081919826209));
#58941=CARTESIAN_POINT('Ctrl Pts',(-0.355015924163216,2.7760602537354,0.618829836115584));
#58942=CARTESIAN_POINT('Ctrl Pts',(-2.51914843674926,1.2195020760201,0.77684047396908));
#58943=CARTESIAN_POINT('Ctrl Pts',(-2.39768778263246,-1.44378427629767,
0.934851111822574));
#58944=CARTESIAN_POINT('Ctrl Pts',(-0.1007027086929,-2.79696300482839,1.09286174967607));
#58945=CARTESIAN_POINT('Ctrl Pts',(2.28762793115499,-1.61245941657473,1.25087238752956));
#58946=CARTESIAN_POINT('Ctrl Pts',(2.6003532631254,1.03510135356512,1.40888302538306));
#58947=CARTESIAN_POINT('Ctrl Pts',(0.553710899450507,2.74347213477777,1.56689366323655));
#58948=CARTESIAN_POINT('Ctrl Pts',(-1.99532275459133,1.96263646638017,1.72490430109005));
#58949=CARTESIAN_POINT('Ctrl Pts',(-2.73395547277665,-0.598949991906553,
1.88291493894354));
#58950=CARTESIAN_POINT('Ctrl Pts',(-0.992005816601449,-2.617092539026,2.04092557679704));
#58951=CARTESIAN_POINT('Ctrl Pts',(1.65001329883352,-2.26068751370113,2.19893621465053));
#58952=CARTESIAN_POINT('Ctrl Pts',(2.79493721635935,0.146892622206337,2.35694685250402));
#58953=CARTESIAN_POINT('Ctrl Pts',(1.40394942456389,2.42119328420925,2.51495749035753));
#58954=CARTESIAN_POINT('Ctrl Pts',(-1.26087427680964,2.49868913935238,2.67296812821101));
#58955=CARTESIAN_POINT('Ctrl Pts',(-2.78167744512252,0.309066092145391,
2.83097876606452));
#58956=CARTESIAN_POINT('Ctrl Pts',(-1.77859992075117,-2.16097975765903,
2.988989403918));
#58957=CARTESIAN_POINT('Ctrl Pts',(0.838242687746051,-2.6703184178973,3.1470000417715));
#58958=CARTESIAN_POINT('Ctrl Pts',(2.69452820593443,-0.756815026848842,
3.305010679625));
#58959=CARTESIAN_POINT('Ctrl Pts',(2.10600558091548,1.8433642406156,3.46302131747849));
#58960=CARTESIAN_POINT('Ctrl Pts',(-0.393344910955346,2.77101624331114,
3.62103195533199));
#58961=CARTESIAN_POINT('Ctrl Pts',(-2.53580441312556,1.18446072736811,3.77904259318548));
#58962=CARTESIAN_POINT('Ctrl Pts',(-2.37746956507925,-1.47678356668067,
3.93705323103898));
#58963=CARTESIAN_POINT('Ctrl Pts',(-0.0620012593698648,-2.79810776790365,
4.09506386889247));
#58964=CARTESIAN_POINT('Ctrl Pts',(2.30972223178794,-1.58064368166609,4.25307450674597));
#58965=CARTESIAN_POINT('Ctrl Pts',(2.58578099692394,1.07097519687693,4.41108514459946));
#58966=CARTESIAN_POINT('Ctrl Pts',(0.515700494891298,2.75087335879294,4.56909578245295));
#58967=CARTESIAN_POINT('Ctrl Pts',(-2.0222870660373,1.93484011199812,4.72710642030645));
#58968=CARTESIAN_POINT('Ctrl Pts',(-2.72540651522529,-0.63671859029782,
4.88511705815995));
#58969=CARTESIAN_POINT('Ctrl Pts',(-0.955701215509313,-2.63056769978633,
5.04312769601343));
#58970=CARTESIAN_POINT('Ctrl Pts',(1.68113403530831,-2.23764152441791,5.20113833386694));
#58971=CARTESIAN_POINT('Ctrl Pts',(2.79263725748281,0.185548873863724,5.35914897172042));
#58972=CARTESIAN_POINT('Ctrl Pts',(1.37031571390328,2.44038646134289,5.51715960957393));
#58973=CARTESIAN_POINT('Ctrl Pts',(-1.29532516285794,2.48100462694871,5.67517024742741));
#58974=CARTESIAN_POINT('Ctrl Pts',(-2.78568737836061,0.27054956388192,5.83318088528093));
#58975=CARTESIAN_POINT('Ctrl Pts',(-1.74853061515341,-2.18538141392889,
5.99119152313439));
#58976=CARTESIAN_POINT('Ctrl Pts',(0.875108661844196,-2.6584649831133,6.14920216098791));
#58977=CARTESIAN_POINT('Ctrl Pts',(2.70474148699564,-0.719461413141105,
6.30721279884139));
#58978=CARTESIAN_POINT('Ctrl Pts',(2.0802994242073,1.87232623816396,6.4652234366949));
#58979=CARTESIAN_POINT('Ctrl Pts',(-0.431646712773937,2.76530872631355,
6.62323407454837));
#58980=CARTESIAN_POINT('Ctrl Pts',(-2.55194974324264,1.14926226094754,6.78124471240189));
#58981=CARTESIAN_POINT('Ctrl Pts',(-2.3568093901987,-1.50953659602729,6.93925535025537));
#58982=CARTESIAN_POINT('Ctrl Pts',(-0.0232810366912258,-2.79869777393076,
7.09726598810887));
#58983=CARTESIAN_POINT('Ctrl Pts',(2.331370743134,-1.54853533848382,7.25527662596236));
#58984=CARTESIAN_POINT('Ctrl Pts',(2.57071559891088,1.1066492425293,7.41328726381586));
#58985=CARTESIAN_POINT('Ctrl Pts',(0.477590373663518,2.75774521510932,7.57129790166936));
#58986=CARTESIAN_POINT('Ctrl Pts',(-2.04886371068724,1.90667478388511,7.72930853952283));
#58987=CARTESIAN_POINT('Ctrl Pts',(-2.71633607520133,-0.674366045285695,
7.88731917737635));
#58988=CARTESIAN_POINT('Ctrl Pts',(-0.919213512101427,-2.64353886970564,
8.04532981522984));
#58989=CARTESIAN_POINT('Ctrl Pts',(1.71193285976134,-2.21416736498029,8.20334045308334));
#58990=CARTESIAN_POINT('Ctrl Pts',(2.78980271289629,0.224169711582251,8.36135109093682));
#58991=CARTESIAN_POINT('Ctrl Pts',(1.33641964853712,2.45911239260802,8.51936172879032));
#58992=CARTESIAN_POINT('Ctrl Pts',(-1.32952806016717,2.4628451785897,8.67737236664382));
#58993=CARTESIAN_POINT('Ctrl Pts',(-2.78916402301518,0.231981225947694,
8.8353830044973));
#58994=CARTESIAN_POINT('Ctrl Pts',(-1.71812656655989,-2.20936469098144,
8.99339364235082));
#58995=CARTESIAN_POINT('Ctrl Pts',(0.911807102923268,-2.64610261394623,
9.1514042802043));
#58996=CARTESIAN_POINT('Ctrl Pts',(2.71443697103106,-0.681970062960328,
9.30941491805779));
#58997=CARTESIAN_POINT('Ctrl Pts',(2.05419501292893,1.90092979495096,9.46742555591129));
#58998=CARTESIAN_POINT('Ctrl Pts',(-0.469865879588134,2.75907181705611,
9.62543619376478));
#58999=CARTESIAN_POINT('Ctrl Pts',(-2.5676065262181,1.11384377854193,9.78344683161828));
#59000=CARTESIAN_POINT('Ctrl Pts',(-2.3356980258232,-1.54200063833969,9.94145746947177));
#59001=CARTESIAN_POINT('Ctrl Pts',(0.0154436428957695,-2.79875199515222,
10.0994681073253));
#59002=CARTESIAN_POINT('Ctrl Pts',(2.35257293505637,-1.51613054243843,10.2574787451788));
#59003=CARTESIAN_POINT('Ctrl Pts',(2.5551580610824,1.14211143036047,10.4154893830323));
#59004=CARTESIAN_POINT('Ctrl Pts',(0.439388822165221,2.7640891265353,10.5735000208858));
#59005=CARTESIAN_POINT('Ctrl Pts',(-2.07504811926679,1.87814444045227,10.7315106587392));
#59006=CARTESIAN_POINT('Ctrl Pts',(-2.70674561767137,-0.711884399106498,
10.8895212965927));
#59007=CARTESIAN_POINT('Ctrl Pts',(-0.882549833739827,-2.656003958476,11.0475319344462));
#59008=CARTESIAN_POINT('Ctrl Pts',(1.74240395044783,-2.190269323608,11.2055425722998));
#59009=CARTESIAN_POINT('Ctrl Pts',(2.78643408629422,0.262747634075224,11.3635532101532));
#59010=CARTESIAN_POINT('Ctrl Pts',(1.3022677379473,2.47736754947181,11.5215638480067));
#59011=CARTESIAN_POINT('Ctrl Pts',(-1.36347643158376,2.44421424122154,11.6795744858602));
#59012=CARTESIAN_POINT('Ctrl Pts',(-2.79210670792561,0.193368477345981,
11.8375851237137));
#59013=CARTESIAN_POINT('Ctrl Pts',(-1.68739359847148,-2.2329250055278,11.9955957615672));
#59014=CARTESIAN_POINT('Ctrl Pts',(0.948330986936765,-2.63323367282349,
12.1536063994207));
#59015=CARTESIAN_POINT('Ctrl Pts',(2.72361280112762,-0.644348155896335,
12.3116170372742));
#59016=CARTESIAN_POINT('Ctrl Pts',(2.02769734494933,1.92916943624887,12.4696276751277));
#59017=CARTESIAN_POINT('Ctrl Pts',(-0.507995094910846,2.75230670893191,
12.6276383129812));
#59018=CARTESIAN_POINT('Ctrl Pts',(-2.58277176458946,1.0782120610078,12.7856489508347));
#59019=CARTESIAN_POINT('Ctrl Pts',(-2.31413951359037,-1.57416947883587,
12.9436595886882));
#59020=CARTESIAN_POINT('Ctrl Pts',(0.0541653659420804,-2.79827042111378,
13.1016702265417));
#59021=CARTESIAN_POINT('Ctrl Pts',(2.37332474856975,-1.48343549715007,13.2596808643952));
#59022=CARTESIAN_POINT('Ctrl Pts',(2.53911136180312,1.17735497143754,13.4176915022487));
#59023=CARTESIAN_POINT('Ctrl Pts',(0.401103153710141,2.76990387866618,13.5757021401021));
#59024=CARTESIAN_POINT('Ctrl Pts',(-2.10083527897802,1.84925454340324,13.7337127779557));
#59025=CARTESIAN_POINT('Ctrl Pts',(-2.6966369787023,-0.749266468887916,
13.8917234158091));
#59026=CARTESIAN_POINT('Ctrl Pts',(-0.845717199230744,-2.66796058040481,
14.0497340536626));
#59027=CARTESIAN_POINT('Ctrl Pts',(1.77254147373567,-2.16595197414774,14.2077446915161));
#59028=CARTESIAN_POINT('Ctrl Pts',(2.78253202299393,0.301275253636565,14.3657553293696));
#59029=CARTESIAN_POINT('Ctrl Pts',(1.26786651939106,2.49514844158187,14.5237659672231));
#59030=CARTESIAN_POINT('Ctrl Pts',(-1.3971637764554,2.42511537310475,14.6817766050766));
#59031=CARTESIAN_POINT('Ctrl Pts',(-2.79451487270181,0.154718726293029,
14.8397872429301));
#59032=CARTESIAN_POINT('Ctrl Pts',(-1.65633758877797,-2.25605787803393,
14.9977978807836));
#59033=CARTESIAN_POINT('Ctrl Pts',(0.984673310924482,-2.61986056441679,
15.1558085186371));
#59034=CARTESIAN_POINT('Ctrl Pts',(2.73226724128555,-0.606603006955222,
15.3138191564906));
#59035=CARTESIAN_POINT('Ctrl Pts',(2.0008114535995,1.95703997099618,15.4718297943441));
#59036=CARTESIAN_POINT('Ctrl Pts',(-0.546026983988871,2.74501428607443,
15.6298404321976));
#59037=CARTESIAN_POINT('Ctrl Pts',(-2.59744269888199,1.04237471475225,15.7878510700511));
#59038=CARTESIAN_POINT('Ctrl Pts',(-2.29213770605498,-1.60603845864169,
15.9458617079046));
#59039=CARTESIAN_POINT('Ctrl Pts',(0.0928761949570627,-2.79725027962867,
16.1038723457581));
#59040=CARTESIAN_POINT('Ctrl Pts',(2.39362321294746,-1.45046193319176,16.2618829836116));
#59041=CARTESIAN_POINT('Ctrl Pts',(2.52257665905884,1.21238356994498,16.4198936214651));
#59042=CARTESIAN_POINT('Ctrl Pts',(0.362744353785385,2.77516839483905,16.5779042593186));
#59043=CARTESIAN_POINT('Ctrl Pts',(-2.12622723672383,1.82004875684226,16.735914897172));
#59044=CARTESIAN_POINT('Ctrl Pts',(-2.68599875372316,-0.786577939425693,
16.8939255350255));
#59045=CARTESIAN_POINT('Ctrl Pts',(-0.80874814078054,-2.6792673034923,17.051936172879));
#59046=CARTESIAN_POINT('Ctrl Pts',(1.80238833174315,-2.14148580062739,17.2099468107325));
#59047=CARTESIAN_POINT('Ctrl Pts',(2.77800430721521,0.340253358304015,17.367957448586));
#59048=CARTESIAN_POINT('Ctrl Pts',(1.23340008456365,2.51147754111133,17.5259680864395));
#59049=CARTESIAN_POINT('Ctrl Pts',(-1.43092211742628,2.4074435208734,17.683978724293));
#59050=CARTESIAN_POINT('Ctrl Pts',(-2.7957460534832,0.112157148881699,17.8419893621465));
#59051=CARTESIAN_POINT('Ctrl Pts',(-2.01608411688922,-1.47535404036764,
17.9473297873822));
#59052=CARTESIAN_POINT('Ctrl Pts',(-1.37702479013086,-1.93106208855776,
18.));
#59053=CARTESIAN_POINT('Ctrl Pts',(-1.12236674703449,2.30288577939267,-0.219489327336923));
#59054=CARTESIAN_POINT('Ctrl Pts',(-1.88447618126776,1.93145342515308,-0.166819114719091));
#59055=CARTESIAN_POINT('Ctrl Pts',(-2.99833112794769,0.379396804352793,
-0.061478689483428));
#59056=CARTESIAN_POINT('Ctrl Pts',(-1.95395485828392,-2.30932117557277,
0.096531948370067));
#59057=CARTESIAN_POINT('Ctrl Pts',(0.865792443118504,-2.89557563394757,
0.254542586223561));
#59058=CARTESIAN_POINT('Ctrl Pts',(2.89870180385485,-0.858185355932735,
0.412553224077057));
#59059=CARTESIAN_POINT('Ctrl Pts',(2.30222105901111,1.95971039855811,0.570563861930551));
#59060=CARTESIAN_POINT('Ctrl Pts',(-0.383468590022299,2.9985469351159,0.728574499784046));
#59061=CARTESIAN_POINT('Ctrl Pts',(-2.72104498234585,1.31723877660696,0.88658513763754));
#59062=CARTESIAN_POINT('Ctrl Pts',(-2.58984989331673,-1.55949601988483,
1.04459577549104));
#59063=CARTESIAN_POINT('Ctrl Pts',(-0.108773503061664,-3.02112493216803,
1.20260641334453));
#59064=CARTESIAN_POINT('Ctrl Pts',(2.47096932151246,-1.74168958871231,1.36061705119803));
#59065=CARTESIAN_POINT('Ctrl Pts',(2.80875795000181,1.11805930259998,1.51862768905152));
#59066=CARTESIAN_POINT('Ctrl Pts',(0.598087926317007,2.963347049202,1.67663832690502));
#59067=CARTESIAN_POINT('Ctrl Pts',(-2.15523741687382,2.11993149395523,1.83464896475851));
#59068=CARTESIAN_POINT('Ctrl Pts',(-2.95306767661361,-0.646952694957672,
1.992659602612));
#59069=CARTESIAN_POINT('Ctrl Pts',(-1.07150988419109,-2.82683879114357,
2.1506702404655));
#59070=CARTESIAN_POINT('Ctrl Pts',(1.7822532178328,-2.4418697707811,2.30868087831899));
#59071=CARTESIAN_POINT('Ctrl Pts',(3.01893678736936,0.158665296084686,2.46669151617249));
#59072=CARTESIAN_POINT('Ctrl Pts',(1.51646861353936,2.61523923766418,2.62470215402598));
#59073=CARTESIAN_POINT('Ctrl Pts',(-1.36192674247852,2.69894597947969,2.78271279187948));
#59074=CARTESIAN_POINT('Ctrl Pts',(-3.00461431495578,0.333836119768613,
2.94072342973297));
#59075=CARTESIAN_POINT('Ctrl Pts',(-1.92114538363842,-2.33417096061113,
3.09873406758647));
#59076=CARTESIAN_POINT('Ctrl Pts',(0.905423446354246,-2.88433044527596,
3.25674470543996));
#59077=CARTESIAN_POINT('Ctrl Pts',(2.91048052095275,-0.817469785158218,
3.41475534329346));
#59078=CARTESIAN_POINT('Ctrl Pts',(2.27479089169405,1.99110022434223,3.57276598114695));
#59079=CARTESIAN_POINT('Ctrl Pts',(-0.424869444242589,2.99309867368931,
3.73077661900045));
#59080=CARTESIAN_POINT('Ctrl Pts',(-2.73903584794299,1.27938904749487,3.88878725685394));
#59081=CARTESIAN_POINT('Ctrl Pts',(-2.56801129158029,-1.5951400304591,4.04679789470744));
#59082=CARTESIAN_POINT('Ctrl Pts',(-0.066970335390515,-3.02236144200463,
4.20480853256093));
#59083=CARTESIAN_POINT('Ctrl Pts',(2.49483436455587,-1.70732398938125,4.36281917041442));
#59084=CARTESIAN_POINT('Ctrl Pts',(2.79301779303032,1.15680824645619,4.52082980826793));
#59085=CARTESIAN_POINT('Ctrl Pts',(0.557031187026083,2.97134144253583,4.67884044612141));
#59086=CARTESIAN_POINT('Ctrl Pts',(-2.1843627765756,2.08990740743638,4.83685108397491));
#59087=CARTESIAN_POINT('Ctrl Pts',(-2.94383356491536,-0.68774824858349,
4.9948617218284));
#59088=CARTESIAN_POINT('Ctrl Pts',(-1.03229565957585,-2.84139391542219,
5.15287235968191));
#59089=CARTESIAN_POINT('Ctrl Pts',(1.81586811824769,-2.41697676622944,5.31088299753539));
#59090=CARTESIAN_POINT('Ctrl Pts',(3.0164524988418,0.200419643734152,5.46889363538889));
#59091=CARTESIAN_POINT('Ctrl Pts',(1.48013933722692,2.63597064736315,5.62690427324239));
#59092=CARTESIAN_POINT('Ctrl Pts',(-1.39913868650357,2.67984414608263,5.78491491109587));
#59093=CARTESIAN_POINT('Ctrl Pts',(-3.00894562332883,0.292232693610869,
5.94292554894938));
#59094=CARTESIAN_POINT('Ctrl Pts',(-1.88866618077534,-2.36052828175403,
6.10093618680286));
#59095=CARTESIAN_POINT('Ctrl Pts',(0.945244035080052,-2.87152701981199,
6.25894682465637));
#59096=CARTESIAN_POINT('Ctrl Pts',(2.92151234296826,-0.777122475063588,
6.41695746250985));
#59097=CARTESIAN_POINT('Ctrl Pts',(2.24702452123894,2.02238337421861,6.57496810036335));
#59098=CARTESIAN_POINT('Ctrl Pts',(-0.466240934756171,2.98693372911462,
6.73297873821685));
#59099=CARTESIAN_POINT('Ctrl Pts',(-2.75647514165928,1.2413696084484,6.89098937607034));
#59100=CARTESIAN_POINT('Ctrl Pts',(-2.54569531195281,-1.63051804346545,
7.04900001392383));
#59101=CARTESIAN_POINT('Ctrl Pts',(-0.0251468897776794,-3.02299873392289,
7.20701065177733));
#59102=CARTESIAN_POINT('Ctrl Pts',(2.51821789063718,-1.67264233075684,7.36502128963082));
#59103=CARTESIAN_POINT('Ctrl Pts',(2.77674498231681,1.19534137991761,7.52303192748432));
#59104=CARTESIAN_POINT('Ctrl Pts',(0.515866739298153,2.97876404212398,7.68104256533782));
#59105=CARTESIAN_POINT('Ctrl Pts',(-2.2130694000192,2.05948477587565,7.8390532031913));
#59106=CARTESIAN_POINT('Ctrl Pts',(-2.93403617665716,-0.728412949796985,
7.99706384104482));
#59107=CARTESIAN_POINT('Ctrl Pts',(-0.992883657953795,-2.85540465663506,
8.15507447889828));
#59108=CARTESIAN_POINT('Ctrl Pts',(1.84913530707925,-2.39162127592933,8.31308511675181));
#59109=CARTESIAN_POINT('Ctrl Pts',(3.01339078036112,0.242135739203144,8.47109575460528));
#59110=CARTESIAN_POINT('Ctrl Pts',(1.44352667985415,2.65619736388585,8.62910639245879));
#59111=CARTESIAN_POINT('Ctrl Pts',(-1.43608276679169,2.66022931310232,8.78711703031227));
#59112=CARTESIAN_POINT('Ctrl Pts',(-3.01270090283309,0.250573305508763,
8.94512766816578));
#59113=CARTESIAN_POINT('Ctrl Pts',(-1.8558254070196,-2.38643369277787,9.10313830601926));
#59114=CARTESIAN_POINT('Ctrl Pts',(0.984883663893263,-2.85817387154125,
9.26114894387277));
#59115=CARTESIAN_POINT('Ctrl Pts',(2.93198486923989,-0.736626389639412,
9.41915958172626));
#59116=CARTESIAN_POINT('Ctrl Pts',(2.21882797819689,2.05327935618502,9.57717021957975));
#59117=CARTESIAN_POINT('Ctrl Pts',(-0.507523167502811,2.98019696426475,
9.73518085743326));
#59118=CARTESIAN_POINT('Ctrl Pts',(-2.77338673374079,1.20311252028871,9.89319149528673));
#59119=CARTESIAN_POINT('Ctrl Pts',(-2.52289198235681,-1.66558390864122,
10.0512021331402));
#59120=CARTESIAN_POINT('Ctrl Pts',(0.0166813699413495,-3.0230573006911,
10.2092127709937));
#59121=CARTESIAN_POINT('Ctrl Pts',(2.54111932713196,-1.63764046012589,10.3672234088472));
#59122=CARTESIAN_POINT('Ctrl Pts',(2.75994058936072,1.23364567626368,10.5252340467007));
#59123=CARTESIAN_POINT('Ctrl Pts',(0.474603533642675,2.98561638480545,10.6832446845542));
#59124=CARTESIAN_POINT('Ctrl Pts',(-2.24135235172689,2.02866787493005,10.8412553224077));
#59125=CARTESIAN_POINT('Ctrl Pts',(-2.92367709421501,-0.768938203061419,
10.9992659602612));
#59126=CARTESIAN_POINT('Ctrl Pts',(-0.953281577907687,-2.86886875694702,
11.1572765981147));
#59127=CARTESIAN_POINT('Ctrl Pts',(1.88204849600037,-2.36580793177884,11.3152872359682));
#59128=CARTESIAN_POINT('Ctrl Pts',(3.00975217599019,0.283805480016149,11.4732978738217));
#59129=CARTESIAN_POINT('Ctrl Pts',(1.4066376726038,2.67591557590604,11.6313085116752));
#59130=CARTESIAN_POINT('Ctrl Pts',(-1.47275192227073,2.64010520373961,11.7893191495287));
#59131=CARTESIAN_POINT('Ctrl Pts',(-3.01587942851794,0.208865947456909,
11.9473297873822));
#59132=CARTESIAN_POINT('Ctrl Pts',(-1.82262935259517,-2.41188224306718,
12.1053404252356));
#59133=CARTESIAN_POINT('Ctrl Pts',(1.02433474580686,-2.84427355222726,12.2633510630892));
#59134=CARTESIAN_POINT('Ctrl Pts',(2.94189609403271,-0.695989283882013,
12.4213617009427));
#59135=CARTESIAN_POINT('Ctrl Pts',(2.19020666098988,2.08378225674299,12.5793723387962));
#59136=CARTESIAN_POINT('Ctrl Pts',(-0.548708239617311,2.97288966817698,
12.7373829766496));
#59137=CARTESIAN_POINT('Ctrl Pts',(-2.78976738649411,1.16462510732239,12.8953936145031));
#59138=CARTESIAN_POINT('Ctrl Pts',(-2.499605668346,-1.70033091312222,13.0534042523566));
#59139=CARTESIAN_POINT('Ctrl Pts',(0.0585064361684609,-3.02253713101717,
13.2114148902101));
#59140=CARTESIAN_POINT('Ctrl Pts',(2.56353428974845,-1.60232507829621,13.3694255280636));
#59141=CARTESIAN_POINT('Ctrl Pts',(2.74260783122701,1.27171380246415,13.5274361659171));
#59142=CARTESIAN_POINT('Ctrl Pts',(0.433249469497138,2.99189715884739,13.6854468037706));
#59143=CARTESIAN_POINT('Ctrl Pts',(-2.26920621715125,1.99746260403018,13.8434574416241));
#59144=CARTESIAN_POINT('Ctrl Pts',(-2.91275830080694,-0.809316249834913,
14.0014680794776));
#59145=CARTESIAN_POINT('Ctrl Pts',(-0.913497000764287,-2.88178363946469,
14.1594787173311));
#59146=CARTESIAN_POINT('Ctrl Pts',(1.9146013838439,-2.33954167419453,14.3174893551846));
#59147=CARTESIAN_POINT('Ctrl Pts',(3.00553738276517,0.325420886381165,14.4754999930381));
#59148=CARTESIAN_POINT('Ctrl Pts',(1.36947937666002,2.69512151333788,14.6335106308916));
#59149=CARTESIAN_POINT('Ctrl Pts',(-1.50913913129515,2.61947566143097,14.7915212687451));
#59150=CARTESIAN_POINT('Ctrl Pts',(-3.01848059508095,0.16711862140126,14.9495319065986));
#59151=CARTESIAN_POINT('Ctrl Pts',(-1.78908436647388,-2.43686909407676,
15.1075425444521));
#59152=CARTESIAN_POINT('Ctrl Pts',(1.06358971661008,-2.8298286592636,15.2655531823056));
#59153=CARTESIAN_POINT('Ctrl Pts',(2.95124414221567,-0.655219059056894,
15.423563820159));
#59154=CARTESIAN_POINT('Ctrl Pts',(2.16116600634399,2.11388646879463,15.5815744580126));
#59155=CARTESIAN_POINT('Ctrl Pts',(-0.589788185298654,2.96501279584345,
15.739585095866));
#59156=CARTESIAN_POINT('Ctrl Pts',(-2.80561411928709,1.12591558557024,15.8975957337196));
#59157=CARTESIAN_POINT('Ctrl Pts',(-2.47584053123723,-1.73475402464994,
16.055606371573));
#59158=CARTESIAN_POINT('Ctrl Pts',(0.100319735264717,-3.0214352305381,16.2136170094265));
#59159=CARTESIAN_POINT('Ctrl Pts',(2.58545956967184,-1.56670885598474,16.37162764728));
#59160=CARTESIAN_POINT('Ctrl Pts',(2.72474795870796,1.30954975957442,16.5296382851335));
#59161=CARTESIAN_POINT('Ctrl Pts',(0.391816412777878,2.9975835984028,16.687648922987));
#59162=CARTESIAN_POINT('Ctrl Pts',(-2.29663320724372,1.9659161267294,16.8456595608405));
#59163=CARTESIAN_POINT('Ctrl Pts',(-2.90126747784539,-0.84961803920536,
17.003670198694));
#59164=CARTESIAN_POINT('Ctrl Pts',(-0.87356506601582,-2.89399653715471,
17.1616808365475));
#59165=CARTESIAN_POINT('Ctrl Pts',(1.94684031110808,-2.31311466508161,17.319691474401));
#59166=CARTESIAN_POINT('Ctrl Pts',(3.0006467942943,0.367522881872776,17.4777021122545));
#59167=CARTESIAN_POINT('Ctrl Pts',(1.3322506377027,2.71275930462191,17.635712750108));
#59168=CARTESIAN_POINT('Ctrl Pts',(-1.5456030263841,2.6003875028527,17.7937233879614));
#59169=CARTESIAN_POINT('Ctrl Pts',(-3.01981044854997,0.12114595660455,17.951734025815));
#59170=CARTESIAN_POINT('Ctrl Pts',(-2.17766269355992,-1.59359593510352,
18.0570744510506));
#59171=CARTESIAN_POINT('Ctrl Pts',(-1.4873861107552,-2.08582659521598,18.1097446636685));
#59172=CARTESIAN_POINT('Ctrl Pts',(-1.20564430054386,2.47375567929492,-0.109744663668461));
#59173=CARTESIAN_POINT('Ctrl Pts',(-2.02430085661326,2.07476372580934,-0.0570744510506297));
#59174=CARTESIAN_POINT('Ctrl Pts',(-3.22080179683223,0.407547351185454,
0.0482659741850331));
#59175=CARTESIAN_POINT('Ctrl Pts',(-2.09893472399684,-2.48066857006502,
0.206276612038529));
#59176=CARTESIAN_POINT('Ctrl Pts',(0.930032653994585,-3.11042203369498,
0.364287249892023));
#59177=CARTESIAN_POINT('Ctrl Pts',(3.11378015967401,-0.921861134895831,
0.522297887745518));
#59178=CARTESIAN_POINT('Ctrl Pts',(2.47304163788057,2.10511731480007,0.680308525599012));
#59179=CARTESIAN_POINT('Ctrl Pts',(-0.411921255881383,3.22103361649641,
0.838319163452508));
#59180=CARTESIAN_POINT('Ctrl Pts',(-2.92294152794244,1.41497547719382,0.996329801306002));
#59181=CARTESIAN_POINT('Ctrl Pts',(-2.782012004001,-1.67520776347199,1.1543404391595));
#59182=CARTESIAN_POINT('Ctrl Pts',(-0.11684429743043,-3.24528685950767,
1.31235107701299));
#59183=CARTESIAN_POINT('Ctrl Pts',(2.65431071186993,-1.8709197608499,1.47036171486649));
#59184=CARTESIAN_POINT('Ctrl Pts',(3.01716263687821,1.20101725163484,1.62837235271998));
#59185=CARTESIAN_POINT('Ctrl Pts',(0.64246495318351,3.18322196362623,1.78638299057348));
#59186=CARTESIAN_POINT('Ctrl Pts',(-2.31515207915632,2.27722652153029,1.94439362842697));
#59187=CARTESIAN_POINT('Ctrl Pts',(-3.17217988045057,-0.69495539800879,
2.10240426628047));
#59188=CARTESIAN_POINT('Ctrl Pts',(-1.15101395178073,-3.03658504326113,
2.26041490413396));
#59189=CARTESIAN_POINT('Ctrl Pts',(1.91449313683208,-2.62305202786106,2.41842554198746));
#59190=CARTESIAN_POINT('Ctrl Pts',(3.24293635837937,0.170437969963035,2.57643617984095));
#59191=CARTESIAN_POINT('Ctrl Pts',(1.62898780251483,2.80928519111911,2.73444681769445));
#59192=CARTESIAN_POINT('Ctrl Pts',(-1.46297920814739,2.89920281960699,2.89245745554793));
#59193=CARTESIAN_POINT('Ctrl Pts',(-3.22755118478904,0.358606147391836,
3.05046809340144));
#59194=CARTESIAN_POINT('Ctrl Pts',(-2.06369084652567,-2.50736216356323,
3.20847873125493));
#59195=CARTESIAN_POINT('Ctrl Pts',(0.97260420496244,-3.09834247265461,3.36648936910842));
#59196=CARTESIAN_POINT('Ctrl Pts',(3.12643283597106,-0.878124543467593,
3.52450000696191));
#59197=CARTESIAN_POINT('Ctrl Pts',(2.44357620247262,2.13883620806886,3.68251064481542));
#59198=CARTESIAN_POINT('Ctrl Pts',(-0.456393977529832,3.21518110406747,
3.84052128266891));
#59199=CARTESIAN_POINT('Ctrl Pts',(-2.94226728276043,1.37431736762162,3.9985319205224));
#59200=CARTESIAN_POINT('Ctrl Pts',(-2.75855301808134,-1.71349649423752,
4.1565425583759));
#59201=CARTESIAN_POINT('Ctrl Pts',(-0.0719394114111575,-3.24661511610562,
4.31455319622939));
#59202=CARTESIAN_POINT('Ctrl Pts',(2.67994649732378,-1.8340042970964,4.47256383408289));
#59203=CARTESIAN_POINT('Ctrl Pts',(3.00025458913671,1.24264129603545,4.63057447193638));
#59204=CARTESIAN_POINT('Ctrl Pts',(0.598361879160862,3.19180952627872,4.78858510978988));
#59205=CARTESIAN_POINT('Ctrl Pts',(-2.3464384871139,2.24497470287464,4.94659574764337));
#59206=CARTESIAN_POINT('Ctrl Pts',(-3.16226061460543,-0.738777906869158,
5.10460638549687));
#59207=CARTESIAN_POINT('Ctrl Pts',(-1.10889010364238,-3.05222013105805,
5.26261702335036));
#59208=CARTESIAN_POINT('Ctrl Pts',(1.95060220118706,-2.59631200804096,5.42062766120385));
#59209=CARTESIAN_POINT('Ctrl Pts',(3.2402677402008,0.215290413604578,5.57863829905735));
#59210=CARTESIAN_POINT('Ctrl Pts',(1.58996296055057,2.83155483338342,5.73664893691084));
#59211=CARTESIAN_POINT('Ctrl Pts',(-1.50295221014919,2.87868366521655,5.89465957476434));
#59212=CARTESIAN_POINT('Ctrl Pts',(-3.23220386829704,0.313915823339817,
6.05267021261783));
#59213=CARTESIAN_POINT('Ctrl Pts',(-2.02880174639727,-2.53567514957916,
6.21068085047134));
#59214=CARTESIAN_POINT('Ctrl Pts',(1.01537940831591,-3.08458905651069,6.36869148832482));
#59215=CARTESIAN_POINT('Ctrl Pts',(3.13828319894088,-0.834783536986071,
6.52670212617832));
#59216=CARTESIAN_POINT('Ctrl Pts',(2.41374961827058,2.17244051027326,6.68471276403182));
#59217=CARTESIAN_POINT('Ctrl Pts',(-0.500835156738408,3.20855873191569,
6.84272340188529));
#59218=CARTESIAN_POINT('Ctrl Pts',(-2.96100054007592,1.33347695594927,7.00073403973882));
#59219=CARTESIAN_POINT('Ctrl Pts',(-2.73458123370692,-1.75149949090362,
7.15874467759228));
#59220=CARTESIAN_POINT('Ctrl Pts',(-0.0270127428641371,-3.24729969391502,
7.31675531544581));
#59221=CARTESIAN_POINT('Ctrl Pts',(2.70506503814037,-1.79674932302986,7.47476595329927));
#59222=CARTESIAN_POINT('Ctrl Pts',(2.98277436572273,1.28403351730591,7.6327765911528));
#59223=CARTESIAN_POINT('Ctrl Pts',(0.554143104932792,3.19978286913864,7.79078722900626));
#59224=CARTESIAN_POINT('Ctrl Pts',(-2.37727508935116,2.21229476786618,7.94879786685977));
#59225=CARTESIAN_POINT('Ctrl Pts',(-3.15173627811299,-0.782459854308269,
8.10680850471327));
#59226=CARTESIAN_POINT('Ctrl Pts',(-1.06655380380616,-3.06727044356448,
8.26481914256675));
#59227=CARTESIAN_POINT('Ctrl Pts',(1.98633775439715,-2.56907518687836,8.42282978042027));
#59228=CARTESIAN_POINT('Ctrl Pts',(3.23697884782595,0.260101766824033,8.58084041827374));
#59229=CARTESIAN_POINT('Ctrl Pts',(1.55063371117118,2.85328233516369,8.73885105612725));
#59230=CARTESIAN_POINT('Ctrl Pts',(-1.54263747341621,2.85761344761494,8.89686169398074));
#59231=CARTESIAN_POINT('Ctrl Pts',(-3.236237782651,0.269165385069836,9.05487233183424));
#59232=CARTESIAN_POINT('Ctrl Pts',(-1.99352424747931,-2.5635026945743,9.21288296968773));
#59233=CARTESIAN_POINT('Ctrl Pts',(1.05796022486326,-3.07024512913626,9.37089360754123));
#59234=CARTESIAN_POINT('Ctrl Pts',(3.14953276744873,-0.791282716318499,
9.52890424539472));
#59235=CARTESIAN_POINT('Ctrl Pts',(2.38346094346486,2.20562891741908,9.68691488324822));
#59236=CARTESIAN_POINT('Ctrl Pts',(-0.545180455417489,3.20132211147338,
9.8449255211017));
#59237=CARTESIAN_POINT('Ctrl Pts',(-2.97916694126347,1.29238126203549,10.0029361589552));
#59238=CARTESIAN_POINT('Ctrl Pts',(-2.71008593889043,-1.78916717894277,
10.1609467968087));
#59239=CARTESIAN_POINT('Ctrl Pts',(0.0179190969869355,-3.24736260622999,
10.3189574346622));
#59240=CARTESIAN_POINT('Ctrl Pts',(2.72966571920753,-1.75915037781335,10.4769680725157));
#59241=CARTESIAN_POINT('Ctrl Pts',(2.96472311763905,1.3251799221669,10.6349787103692));
#59242=CARTESIAN_POINT('Ctrl Pts',(0.509818245120129,3.20714364307561,10.7929893482227));
#59243=CARTESIAN_POINT('Ctrl Pts',(-2.407656584187,2.17919130940784,10.9509999860762));
#59244=CARTESIAN_POINT('Ctrl Pts',(-3.14060857075865,-0.82599200701634,
11.1090106239297));
#59245=CARTESIAN_POINT('Ctrl Pts',(-1.02401332207554,-3.08173355541803,
11.2670212617832));
#59246=CARTESIAN_POINT('Ctrl Pts',(2.02169304155291,-2.54134653994968,11.4250318996367));
#59247=CARTESIAN_POINT('Ctrl Pts',(3.23307026568617,0.304863325957073,11.5830425374901));
#59248=CARTESIAN_POINT('Ctrl Pts',(1.51100760726029,2.87446360234028,11.7410531753437));
#59249=CARTESIAN_POINT('Ctrl Pts',(-1.58202741295769,2.83599616625768,11.8990638131971));
#59250=CARTESIAN_POINT('Ctrl Pts',(-3.23965214911027,0.224363417567839,
12.0570744510506));
#59251=CARTESIAN_POINT('Ctrl Pts',(-1.95786510671885,-2.59083948060657,
12.2150850889041));
#59252=CARTESIAN_POINT('Ctrl Pts',(1.10033850467697,-3.05531343163102,12.3730957267576));
#59253=CARTESIAN_POINT('Ctrl Pts',(3.1601793869378,-0.747630411867695,12.5311063646111));
#59254=CARTESIAN_POINT('Ctrl Pts',(2.35271597703043,2.2383950772371,12.6891170024646));
#59255=CARTESIAN_POINT('Ctrl Pts',(-0.589421384323778,3.19347262742205,
12.8471276403181));
#59256=CARTESIAN_POINT('Ctrl Pts',(-2.99676300839876,1.25103815363699,13.0051382781716));
#59257=CARTESIAN_POINT('Ctrl Pts',(-2.68507182310164,-1.82649234740857,
13.1631489160251));
#59258=CARTESIAN_POINT('Ctrl Pts',(0.0628475063948363,-3.24680384092056,
13.3211595538786));
#59259=CARTESIAN_POINT('Ctrl Pts',(2.75374383092715,-1.72121465944234,13.4791701917321));
#59260=CARTESIAN_POINT('Ctrl Pts',(2.9461043006509,1.36607263349075,13.6371808295856));
#59261=CARTESIAN_POINT('Ctrl Pts',(0.465395785284136,3.2138904390286,13.7951914674391));
#59262=CARTESIAN_POINT('Ctrl Pts',(-2.43757715532447,2.14567066465713,13.9532021052926));
#59263=CARTESIAN_POINT('Ctrl Pts',(-3.12887962291158,-0.869366030781908,
14.1112127431461));
#59264=CARTESIAN_POINT('Ctrl Pts',(-0.981276802297831,-3.09560669852456,
14.2692233809996));
#59265=CARTESIAN_POINT('Ctrl Pts',(2.05666129395213,-2.51313137424132,14.4272340188531));
#59266=CARTESIAN_POINT('Ctrl Pts',(3.22854274253641,0.349566519125767,14.5852446567066));
#59267=CARTESIAN_POINT('Ctrl Pts',(1.47109223392897,2.89509458509389,14.74325529456));
#59268=CARTESIAN_POINT('Ctrl Pts',(-1.62111448613489,2.81383594975718,14.9012659324135));
#59269=CARTESIAN_POINT('Ctrl Pts',(-3.2424463174601,0.179518516509487,15.059276570267));
#59270=CARTESIAN_POINT('Ctrl Pts',(-1.92183114416979,-2.61768031011958,
15.2172872081205));
#59271=CARTESIAN_POINT('Ctrl Pts',(1.14250612229568,-3.03979675411041,15.375297845974));
#59272=CARTESIAN_POINT('Ctrl Pts',(3.17022104314579,-0.703835111158572,
15.5333084838275));
#59273=CARTESIAN_POINT('Ctrl Pts',(2.32152055908849,2.27073296659308,15.691319121681));
#59274=CARTESIAN_POINT('Ctrl Pts',(-0.633549386608433,3.18501130561246,
15.8493297595345));
#59275=CARTESIAN_POINT('Ctrl Pts',(-3.01378553969219,1.20945645638823,16.007340397388));
#59276=CARTESIAN_POINT('Ctrl Pts',(-2.65954335641947,-1.8634695906582,16.1653510352415));
#59277=CARTESIAN_POINT('Ctrl Pts',(0.107763275572369,-3.24562018144752,
16.323361673095));
#59278=CARTESIAN_POINT('Ctrl Pts',(2.77729592639622,-1.68295577877773,16.4813723109485));
#59279=CARTESIAN_POINT('Ctrl Pts',(2.92691925835708,1.40671594920387,16.639382948802));
#59280=CARTESIAN_POINT('Ctrl Pts',(0.420888471770377,3.21999880196654,16.7973935866555));
#59281=CARTESIAN_POINT('Ctrl Pts',(-2.46703917776361,2.11178349661654,16.955404224509));
#59282=CARTESIAN_POINT('Ctrl Pts',(-3.11653620196762,-0.912658138985028,
17.1134148623625));
#59283=CARTESIAN_POINT('Ctrl Pts',(-0.938381991251102,-3.10872577081711,
17.2714255002159));
#59284=CARTESIAN_POINT('Ctrl Pts',(2.09129229047302,-2.48474352953584,17.4294361380695));
#59285=CARTESIAN_POINT('Ctrl Pts',(3.2232892813734,0.39479240544154,17.5874467759229));
#59286=CARTESIAN_POINT('Ctrl Pts',(1.43110119084175,2.91404106813249,17.7454574137765));
#59287=CARTESIAN_POINT('Ctrl Pts',(-1.66028393534192,2.79333148483199,17.9034680516299));
#59288=CARTESIAN_POINT('Ctrl Pts',(-3.24387484361673,0.130134764327401,
18.0614786894834));
#59289=CARTESIAN_POINT('Ctrl Pts',(-2.33924127023062,-1.7118378298394,18.1668191147191));
#59290=CARTESIAN_POINT('Ctrl Pts',(-1.59774743137953,-2.24059110187421,
18.2194893273369));
#59291=CARTESIAN_POINT('Ctrl Pts',(-1.28892185405323,2.64462557919718,0.));
#59292=CARTESIAN_POINT('Ctrl Pts',(-2.16412553195875,2.2180740264656,0.0526702126178316));
#59293=CARTESIAN_POINT('Ctrl Pts',(-3.44327246571677,0.435697898018116,
0.158010637853495));
#59294=CARTESIAN_POINT('Ctrl Pts',(-2.24391458970975,-2.65201596455728,
0.31602127570699));
#59295=CARTESIAN_POINT('Ctrl Pts',(0.994272864870662,-3.32526843344238,
0.474031913560484));
#59296=CARTESIAN_POINT('Ctrl Pts',(3.32885851549317,-0.985536913858929,
0.632042551413979));
#59297=CARTESIAN_POINT('Ctrl Pts',(2.64386221675003,2.25052423104204,0.790053189267474));
#59298=CARTESIAN_POINT('Ctrl Pts',(-0.440373921740465,3.44352029787691,
0.948063827120969));
#59299=CARTESIAN_POINT('Ctrl Pts',(-3.12483807353904,1.51271217778069,1.10607446497446));
#59300=CARTESIAN_POINT('Ctrl Pts',(-2.97417411468528,-1.79091950705915,
1.26408510282796));
#59301=CARTESIAN_POINT('Ctrl Pts',(-0.124915091799196,-3.46944878684731,
1.42209574068145));
#59302=CARTESIAN_POINT('Ctrl Pts',(2.8376521022274,-2.00014993298748,1.58010637853495));
#59303=CARTESIAN_POINT('Ctrl Pts',(3.22556732375462,1.2839752006697,1.73811701638844));
#59304=CARTESIAN_POINT('Ctrl Pts',(0.68684198005001,3.40309687805045,1.89612765424193));
#59305=CARTESIAN_POINT('Ctrl Pts',(-2.47506674143882,2.43452154910535,2.05413829209543));
#59306=CARTESIAN_POINT('Ctrl Pts',(-3.39129208428754,-0.742958101059912,
2.21214892994892));
#59307=CARTESIAN_POINT('Ctrl Pts',(-1.23051801937037,-3.24633129537869,
2.37015956780242));
#59308=CARTESIAN_POINT('Ctrl Pts',(2.04673305583136,-2.80423428494102,2.52817020565591));
#59309=CARTESIAN_POINT('Ctrl Pts',(3.46693592938937,0.182210643841385,2.68618084350942));
#59310=CARTESIAN_POINT('Ctrl Pts',(1.74150699149031,3.00333114457405,2.8441914813629));
#59311=CARTESIAN_POINT('Ctrl Pts',(-1.56403167381627,3.09945965973429,3.0022021192164));
#59312=CARTESIAN_POINT('Ctrl Pts',(-3.45048805462229,0.38337617501506,3.1602127570699));
#59313=CARTESIAN_POINT('Ctrl Pts',(-2.20623630941293,-2.68055336651533,
3.31822339492339));
#59314=CARTESIAN_POINT('Ctrl Pts',(1.03978496357064,-3.31235450003327,3.47623403277689));
#59315=CARTESIAN_POINT('Ctrl Pts',(3.34238515098937,-0.938779301776967,
3.63424467063038));
#59316=CARTESIAN_POINT('Ctrl Pts',(2.61236151325119,2.28657219179548,3.79225530848387));
#59317=CARTESIAN_POINT('Ctrl Pts',(-0.487918510817076,3.43726353444563,
3.95026594633737));
#59318=CARTESIAN_POINT('Ctrl Pts',(-3.14549871757786,1.46924568774838,4.10827658419087));
#59319=CARTESIAN_POINT('Ctrl Pts',(-2.94909474458238,-1.83185295801596,
4.26628722204435));
#59320=CARTESIAN_POINT('Ctrl Pts',(-0.0769084874318037,-3.4708687902066,
4.42429785989786));
#59321=CARTESIAN_POINT('Ctrl Pts',(2.8650586300917,-1.96068460481156,4.58230849775135));
#59322=CARTESIAN_POINT('Ctrl Pts',(3.20749138524309,1.32847434561472,4.74031913560485));
#59323=CARTESIAN_POINT('Ctrl Pts',(0.63969257129564,3.41227761002162,4.89832977345833));
#59324=CARTESIAN_POINT('Ctrl Pts',(-2.50851419765219,2.40004199831291,5.05634041131184));
#59325=CARTESIAN_POINT('Ctrl Pts',(-3.3806876642955,-0.789807565154828,
5.21435104916532));
#59326=CARTESIAN_POINT('Ctrl Pts',(-1.18548454770891,-3.26304634669391,
5.37236168701883));
#59327=CARTESIAN_POINT('Ctrl Pts',(2.08533628412643,-2.77564724985249,5.53037232487231));
#59328=CARTESIAN_POINT('Ctrl Pts',(3.4640829815598,0.230161183475004,5.68838296272581));
#59329=CARTESIAN_POINT('Ctrl Pts',(1.6997865838742,3.02713901940368,5.84639360057932));
#59330=CARTESIAN_POINT('Ctrl Pts',(-1.60676573379481,3.07752318435047,6.00440423843279));
#59331=CARTESIAN_POINT('Ctrl Pts',(-3.45546211326527,0.335598953068766,
6.1624148762863));
#59332=CARTESIAN_POINT('Ctrl Pts',(-2.16893731201919,-2.7108220174043,6.32042551413978));
#59333=CARTESIAN_POINT('Ctrl Pts',(1.08551478155176,-3.2976510932094,6.47843615199329));
#59334=CARTESIAN_POINT('Ctrl Pts',(3.35505405491351,-0.89244459890855,6.63644678984678));
#59335=CARTESIAN_POINT('Ctrl Pts',(2.58047471530221,2.3224976463279,6.79445742770027));
#59336=CARTESIAN_POINT('Ctrl Pts',(-0.535429378720641,3.43018373471677,
6.95246806555377));
#59337=CARTESIAN_POINT('Ctrl Pts',(-3.16552593849257,1.42558430345014,7.11047870340726));
#59338=CARTESIAN_POINT('Ctrl Pts',(-2.92346715546102,-1.87248093834177,
7.26848934126076));
#59339=CARTESIAN_POINT('Ctrl Pts',(-0.0288785959505942,-3.47160065390715,
7.42649997911425));
#59340=CARTESIAN_POINT('Ctrl Pts',(2.89191218564355,-1.92085631530288,7.58451061696775));
#59341=CARTESIAN_POINT('Ctrl Pts',(3.18880374912866,1.37272565469421,7.74252125482125));
#59342=CARTESIAN_POINT('Ctrl Pts',(0.592419470567429,3.4208016961533,7.90053189267473));
#59343=CARTESIAN_POINT('Ctrl Pts',(-2.54148077868312,2.36510475985672,8.05854253052824));
#59344=CARTESIAN_POINT('Ctrl Pts',(-3.36943637956882,-0.836506758819556,
8.21655316838173));
#59345=CARTESIAN_POINT('Ctrl Pts',(-1.14022394965853,-3.2791362304939,8.37456380623523));
#59346=CARTESIAN_POINT('Ctrl Pts',(2.12354020171506,-2.7465290978274,8.53257444408871));
#59347=CARTESIAN_POINT('Ctrl Pts',(3.46056691529078,0.278067794444923,8.69058508194221));
#59348=CARTESIAN_POINT('Ctrl Pts',(1.65774074248821,3.05036730644152,8.84859571979571));
#59349=CARTESIAN_POINT('Ctrl Pts',(-1.64919218004073,3.05499758212755,9.00660635764919));
#59350=CARTESIAN_POINT('Ctrl Pts',(-3.45977466246891,0.287757464630905,
9.16461699550271));
#59351=CARTESIAN_POINT('Ctrl Pts',(-2.13122308793902,-2.74057169637072,
9.32262763335619));
#59352=CARTESIAN_POINT('Ctrl Pts',(1.13103678583326,-3.28231638673127,9.48063827120969));
#59353=CARTESIAN_POINT('Ctrl Pts',(3.36708066565756,-0.845939042997581,
9.63864890906319));
#59354=CARTESIAN_POINT('Ctrl Pts',(2.54809390873282,2.35797847865313,9.79665954691667));
#59355=CARTESIAN_POINT('Ctrl Pts',(-0.582837743332163,3.42244725868203,
9.95467018477017));
#59356=CARTESIAN_POINT('Ctrl Pts',(-3.18494714878616,1.38165000378226,10.1126808226237));
#59357=CARTESIAN_POINT('Ctrl Pts',(-2.89727989542405,-1.9127504492443,10.2706914604771));
#59358=CARTESIAN_POINT('Ctrl Pts',(0.0191568240325155,-3.47166791176887,
10.4287020983307));
#59359=CARTESIAN_POINT('Ctrl Pts',(2.91821211128312,-1.88066029550081,10.5867127361841));
#59360=CARTESIAN_POINT('Ctrl Pts',(3.16950564591737,1.41671416807011,10.7447233740376));
#59361=CARTESIAN_POINT('Ctrl Pts',(0.545032956597581,3.42867090134576,10.9027340118911));
#59362=CARTESIAN_POINT('Ctrl Pts',(-2.5739608166471,2.32971474388563,11.0607446497446));
#59363=CARTESIAN_POINT('Ctrl Pts',(-3.3575400473023,-0.883045810971261,
11.2187552875982));
#59364=CARTESIAN_POINT('Ctrl Pts',(-1.0947450662434,-3.29459835388904,11.3767659254516));
#59365=CARTESIAN_POINT('Ctrl Pts',(2.16133758710544,-2.71688514812053,11.5347765633051));
#59366=CARTESIAN_POINT('Ctrl Pts',(3.45638835538215,0.325921171897996,11.6927872011586));
#59367=CARTESIAN_POINT('Ctrl Pts',(1.61537754191679,3.07301162877451,11.8507978390121));
#59368=CARTESIAN_POINT('Ctrl Pts',(-1.69130290364466,3.03188712877575,12.0088084768656));
#59369=CARTESIAN_POINT('Ctrl Pts',(-3.4634248697026,0.239860887678766,12.1668191147191));
#59370=CARTESIAN_POINT('Ctrl Pts',(-2.09310086084253,-2.76979671814595,
12.3248297525726));
#59371=CARTESIAN_POINT('Ctrl Pts',(1.17634226354706,-3.26635331103479,12.4828403904261));
#59372=CARTESIAN_POINT('Ctrl Pts',(3.3784626798429,-0.799271539853375,12.6408510282796));
#59373=CARTESIAN_POINT('Ctrl Pts',(2.51522529307098,2.39300789773122,12.7988616661331));
#59374=CARTESIAN_POINT('Ctrl Pts',(-0.630134529030243,3.41405558666711,
12.9568723039866));
#59375=CARTESIAN_POINT('Ctrl Pts',(-3.2037586303034,1.33745119995158,13.1148829418401));
#59376=CARTESIAN_POINT('Ctrl Pts',(-2.87053797785727,-1.95265378169492,
13.2728935796936));
#59377=CARTESIAN_POINT('Ctrl Pts',(0.0671885766212145,-3.47107055082396,
13.4309042175471));
#59378=CARTESIAN_POINT('Ctrl Pts',(2.94395337210586,-1.84010424058848,13.5889148554006));
#59379=CARTESIAN_POINT('Ctrl Pts',(3.14960077007479,1.46043146451736,13.746925493254));
#59380=CARTESIAN_POINT('Ctrl Pts',(0.497542101071137,3.43588371920981,13.9049361311076));
#59381=CARTESIAN_POINT('Ctrl Pts',(-2.6059480934977,2.29387872528407,14.062946768961));
#59382=CARTESIAN_POINT('Ctrl Pts',(-3.34500094501622,-0.929415811728904,
14.2209574068145));
#59383=CARTESIAN_POINT('Ctrl Pts',(-1.04905660383138,-3.30942975758444,
14.378968044668));
#59384=CARTESIAN_POINT('Ctrl Pts',(2.19872120406036,-2.6867210742881,14.5369786825215));
#59385=CARTESIAN_POINT('Ctrl Pts',(3.45154810230765,0.373712151870365,14.694989320375));
#59386=CARTESIAN_POINT('Ctrl Pts',(1.57270509119793,3.09506765684991,14.8529999582285));
#59387=CARTESIAN_POINT('Ctrl Pts',(-1.73308984097463,3.0081962380834,15.011010596082));
#59388=CARTESIAN_POINT('Ctrl Pts',(-3.46641203983924,0.191918411617718,
15.1690212339355));
#59389=CARTESIAN_POINT('Ctrl Pts',(-2.0545779218657,-2.79849152616241,15.327031871789));
#59390=CARTESIAN_POINT('Ctrl Pts',(1.22142252798128,-3.24976484895722,15.4850425096425));
#59391=CARTESIAN_POINT('Ctrl Pts',(3.38919794407591,-0.752451163260243,
15.643053147496));
#59392=CARTESIAN_POINT('Ctrl Pts',(2.48187511183298,2.42757946439152,15.8010637853495));
#59393=CARTESIAN_POINT('Ctrl Pts',(-0.677310587918214,3.40500981538148,
15.959074423203));
#59394=CARTESIAN_POINT('Ctrl Pts',(-3.22195696009729,1.29299732720621,16.1170850610565));
#59395=CARTESIAN_POINT('Ctrl Pts',(-2.84324618160172,-1.99218515666645,
16.27509569891));
#59396=CARTESIAN_POINT('Ctrl Pts',(0.115206815880023,-3.46980513235694,
16.4331063367635));
#59397=CARTESIAN_POINT('Ctrl Pts',(2.9691322831206,-1.79920270157072,16.591116974617));
#59398=CARTESIAN_POINT('Ctrl Pts',(3.1290905580062,1.50388213883331,16.7491276124704));
#59399=CARTESIAN_POINT('Ctrl Pts',(0.44996053076287,3.44241400553029,16.9071382503239));
#59400=CARTESIAN_POINT('Ctrl Pts',(-2.63744514828349,2.25765086650368,17.0651488881774));
#59401=CARTESIAN_POINT('Ctrl Pts',(-3.33180492608985,-0.975698238764695,
17.2231595260309));
#59402=CARTESIAN_POINT('Ctrl Pts',(-1.00319891648638,-3.32345500447951,
17.3811701638844));
#59403=CARTESIAN_POINT('Ctrl Pts',(2.23574426983795,-2.65637239399007,17.5391808017379));
#59404=CARTESIAN_POINT('Ctrl Pts',(3.44593176845249,0.422061929010304,17.6971914395914));
#59405=CARTESIAN_POINT('Ctrl Pts',(1.5299517439808,3.11532283164306,17.8552020774449));
#59406=CARTESIAN_POINT('Ctrl Pts',(-1.77496484429974,2.98627546681129,18.0132127152984));
#59407=CARTESIAN_POINT('Ctrl Pts',(-3.46793923868349,0.139123572050251,
18.1712233531519));
#59408=CARTESIAN_POINT('Ctrl Pts',(-2.50081984690132,-1.83007972457528,
18.2765637783876));
#59409=CARTESIAN_POINT('Ctrl Pts',(-1.70810875200386,-2.39535560853244,
18.3292339910054));
#59410=CARTESIAN_POINT('',(-1.28892185405336,2.64462557919711,18.));
#59411=CARTESIAN_POINT('Ctrl Pts',(-1.29200505722538,2.64817880365269,18.));
#59412=CARTESIAN_POINT('Ctrl Pts',(-1.36163618241778,2.60626194974374,18.));
#59413=CARTESIAN_POINT('Ctrl Pts',(-1.42923518191538,2.56138581315695,18.));
#59414=CARTESIAN_POINT('Ctrl Pts',(-1.49459061409937,2.51355245406074,18.));
#59415=CARTESIAN_POINT('Ctrl Pts',(-1.57240585429751,2.45659981518786,18.));
#59416=CARTESIAN_POINT('Ctrl Pts',(-1.64704183718319,2.3954553757506,18.));
#59417=CARTESIAN_POINT('Ctrl Pts',(-1.71834950288611,2.3304978961962,18.));
#59418=CARTESIAN_POINT('Ctrl Pts',(-1.79066304650991,2.26462411551435,18.));
#59419=CARTESIAN_POINT('Ctrl Pts',(-1.85955417595172,2.19482804870293,18.));
#59420=CARTESIAN_POINT('Ctrl Pts',(-1.92482309271148,2.12147574581737,18.));
#59421=CARTESIAN_POINT('Ctrl Pts',(-1.98558358441959,2.05319022473766,18.));
#59422=CARTESIAN_POINT('Ctrl Pts',(-2.04320479258379,1.98182188662656,18.));
#59423=CARTESIAN_POINT('Ctrl Pts',(-2.09748654005121,1.90765458443028,18.));
#59424=CARTESIAN_POINT('Ctrl Pts',(-2.10646572746629,1.89538596491152,18.));
#59425=CARTESIAN_POINT('Ctrl Pts',(-2.11535395516661,1.88303990420399,18.));
#59426=CARTESIAN_POINT('Ctrl Pts',(-2.12414062558065,1.87063159113709,18.));
#59427=CARTESIAN_POINT('Ctrl Pts',(-2.17962766214166,1.79227420564738,18.));
#59428=CARTESIAN_POINT('Ctrl Pts',(-2.23116240517441,1.71130999749083,18.));
#59429=CARTESIAN_POINT('Ctrl Pts',(-2.27859485862069,1.62810446801355,18.));
#59430=CARTESIAN_POINT('Ctrl Pts',(-2.32587805625837,1.5451607615642,18.));
#59431=CARTESIAN_POINT('Ctrl Pts',(-2.3690850323679,1.45998884995688,18.));
#59432=CARTESIAN_POINT('Ctrl Pts',(-2.40801882408265,1.37293340222991,18.));
#59433=CARTESIAN_POINT('Ctrl Pts',(-2.44628322593828,1.28737470145007,18.));
#59434=CARTESIAN_POINT('Ctrl Pts',(-2.48042026711449,1.19999579594418,18.));
#59435=CARTESIAN_POINT('Ctrl Pts',(-2.51019309935484,1.11112072325793,18.));
#59436=CARTESIAN_POINT('Ctrl Pts',(-2.52373989101854,1.07068210848132,18.));
#59437=CARTESIAN_POINT('Ctrl Pts',(-2.53638245890231,1.02993377861641,18.));
#59438=CARTESIAN_POINT('Ctrl Pts',(-2.54809485627599,0.988906771366336,
18.));
#59439=CARTESIAN_POINT('Ctrl Pts',(-2.55316334672363,0.971152507426353,
18.));
#59440=CARTESIAN_POINT('Ctrl Pts',(-2.55805761544222,0.953346062512553,
18.));
#59441=CARTESIAN_POINT('Ctrl Pts',(-2.56277542193469,0.935489987393445,
18.));
#59442=CARTESIAN_POINT('Ctrl Pts',(-2.56650095821091,0.921389482060481,
18.));
#59443=CARTESIAN_POINT('Ctrl Pts',(-2.57011653103175,0.907257407319225,
18.));
#59444=CARTESIAN_POINT('Ctrl Pts',(-2.5736173989552,0.893110501520028,18.));
#59445=CARTESIAN_POINT('Ctrl Pts',(-2.59566737033708,0.804007206327108,
18.));
#59446=CARTESIAN_POINT('Ctrl Pts',(-2.61321077029624,0.714169511674567,
18.));
#59447=CARTESIAN_POINT('Ctrl Pts',(-2.62607329651336,0.623911051832834,
18.));
#59448=CARTESIAN_POINT('Ctrl Pts',(-2.63856625673392,0.536245897310476,
18.));
#59449=CARTESIAN_POINT('Ctrl Pts',(-2.64664344597227,0.448183056834854,
18.));
#59450=CARTESIAN_POINT('Ctrl Pts',(-2.65009718893369,0.360012694318155,
18.));
#59451=CARTESIAN_POINT('Ctrl Pts',(-2.65337274389513,0.276391280791186,
18.));
#59452=CARTESIAN_POINT('Ctrl Pts',(-2.65248941241092,0.192672662846889,
18.));
#59453=CARTESIAN_POINT('Ctrl Pts',(-2.64722813834475,0.109115603594406,
18.));
#59454=CARTESIAN_POINT('Ctrl Pts',(-2.64396768384946,0.0573346117613012,
18.));
#59455=CARTESIAN_POINT('Ctrl Pts',(-2.6390249363967,0.00561591434296466,
18.));
#59456=CARTESIAN_POINT('Ctrl Pts',(-2.63242870157844,-0.0459750284110199,
18.));
#59457=CARTESIAN_POINT('Ctrl Pts',(-2.630403908258,-0.0618114865059137,
18.));
#59458=CARTESIAN_POINT('Ctrl Pts',(-2.62822328410621,-0.0776358837596198,
18.));
#59459=CARTESIAN_POINT('Ctrl Pts',(-2.6258875853782,-0.0934462620603028,
18.));
#59460=CARTESIAN_POINT('Ctrl Pts',(-2.62391361832001,-0.106808073482704,
18.));
#59461=CARTESIAN_POINT('Ctrl Pts',(-2.62182902790254,-0.12015847992975,
18.));
#59462=CARTESIAN_POINT('Ctrl Pts',(-2.61963650138613,-0.133484262718106,
18.));
#59463=CARTESIAN_POINT('Ctrl Pts',(-2.60533039958249,-0.22043418271049,
18.));
#59464=CARTESIAN_POINT('Ctrl Pts',(-2.58641281438588,-0.30647770673795,
18.));
#59465=CARTESIAN_POINT('Ctrl Pts',(-2.56311020645715,-0.391323689237884,
18.));
#59466=CARTESIAN_POINT('Ctrl Pts',(-2.53941406581745,-0.47760254438493,
18.));
#59467=CARTESIAN_POINT('Ctrl Pts',(-2.51118302420645,-0.562643940056807,
18.));
#59468=CARTESIAN_POINT('Ctrl Pts',(-2.47860728478706,-0.646118919116556,
18.));
#59469=CARTESIAN_POINT('Ctrl Pts',(-2.44637774874284,-0.728706755781168,
18.));
#59470=CARTESIAN_POINT('Ctrl Pts',(-2.4098946850966,-0.809762009208342,
18.));
#59471=CARTESIAN_POINT('Ctrl Pts',(-2.36930513861691,-0.888932237840673,
18.));
#59472=CARTESIAN_POINT('Ctrl Pts',(-2.35350807431684,-0.919744535607576,
18.));
#59473=CARTESIAN_POINT('Ctrl Pts',(-2.33708865769319,-0.950270887707321,
18.));
#59474=CARTESIAN_POINT('Ctrl Pts',(-2.32005434850432,-0.980488756468179,
18.));
#59475=CARTESIAN_POINT('Ctrl Pts',(-2.31145049889473,-0.99575148273774,
18.));
#59476=CARTESIAN_POINT('Ctrl Pts',(-2.30268977113614,-1.01093549317028,
18.));
#59477=CARTESIAN_POINT('Ctrl Pts',(-2.29377307107857,-1.02603777506919,
18.));
#59478=CARTESIAN_POINT('Ctrl Pts',(-2.28696307843181,-1.03757191079393,
18.));
#59479=CARTESIAN_POINT('Ctrl Pts',(-2.28006311659331,-1.04905657461536,
18.));
#59480=CARTESIAN_POINT('Ctrl Pts',(-2.27307846241723,-1.060482846395,18.));
#59481=CARTESIAN_POINT('Ctrl Pts',(-2.22741856850457,-1.13517836375679,
18.));
#59482=CARTESIAN_POINT('Ctrl Pts',(-2.17808652500359,-1.20747656221673,
18.));
#59483=CARTESIAN_POINT('Ctrl Pts',(-2.12525028267988,-1.27705246380043,
18.));
#59484=CARTESIAN_POINT('Ctrl Pts',(-2.07473471720153,-1.3435724481444,18.));
#59485=CARTESIAN_POINT('Ctrl Pts',(-2.02101528451866,-1.40760435474595,
18.));
#59486=CARTESIAN_POINT('Ctrl Pts',(-1.96421326719147,-1.46882640916218,
18.));
#59487=CARTESIAN_POINT('Ctrl Pts',(-1.94502793769979,-1.48950464105255,
18.));
#59488=CARTESIAN_POINT('Ctrl Pts',(-1.92549077017066,-1.50986197314986,
18.));
#59489=CARTESIAN_POINT('Ctrl Pts',(-1.90560595192038,-1.5298848741256,18.));
#59490=CARTESIAN_POINT('Ctrl Pts',(-1.89094077503979,-1.54465188787328,
18.));
#59491=CARTESIAN_POINT('Ctrl Pts',(-1.87608378637058,-1.55923940543717,
18.));
#59492=CARTESIAN_POINT('Ctrl Pts',(-1.86105580868443,-1.57362393088814,
18.));
#59493=CARTESIAN_POINT('Ctrl Pts',(-1.80044929335635,-1.63163545981358,
18.));
#59494=CARTESIAN_POINT('Ctrl Pts',(-1.73700668600649,-1.68640854165577,
18.));
#59495=CARTESIAN_POINT('Ctrl Pts',(-1.67086296650322,-1.73762479738526,
18.));
#59496=CARTESIAN_POINT('Ctrl Pts',(-1.60658789828107,-1.78739412326861,
18.));
#59497=CARTESIAN_POINT('Ctrl Pts',(-1.53976159075827,-1.83380507910934,
18.));
#59498=CARTESIAN_POINT('Ctrl Pts',(-1.47049053791553,-1.87651975790584,
18.));
#59499=CARTESIAN_POINT('Ctrl Pts',(-1.43981212378135,-1.89543701918527,
18.));
#59500=CARTESIAN_POINT('Ctrl Pts',(-1.40865402146917,-1.91362865851037,
18.));
#59501=CARTESIAN_POINT('Ctrl Pts',(-1.37702479013086,-1.93106208855776,
18.));
#59502=CARTESIAN_POINT('Ctrl Pts',(-2.94047623996122,-0.00254690177668123,
17.1778238829104));
#59503=CARTESIAN_POINT('Ctrl Pts',(-2.94279871458441,-0.28218123486593,
17.1929357639506));
#59504=CARTESIAN_POINT('Ctrl Pts',(-2.9061256239192,-0.561215560283936,
17.2080476449907));
#59505=CARTESIAN_POINT('Ctrl Pts',(-2.82797729485488,-0.828099515505769,
17.2231595260309));
#59506=CARTESIAN_POINT('Ctrl Pts',(-2.5556029228887,-1.7582838273363,17.2758297386488));
#59507=CARTESIAN_POINT('Ctrl Pts',(-1.77940091968755,-2.5408694159079,17.3284999512666));
#59508=CARTESIAN_POINT('Ctrl Pts',(-0.851476053699583,-2.82098177511213,
17.3811701638844));
#59509=CARTESIAN_POINT('Ctrl Pts',(0.0764488122883847,-3.10109413431636,
17.4338403765023));
#59510=CARTESIAN_POINT('Ctrl Pts',(1.15609654106319,-2.87873326415321,17.4865105891201));
#59511=CARTESIAN_POINT('Ctrl Pts',(1.89761832188633,-2.2544804419049,17.5391808017379));
#59512=CARTESIAN_POINT('Ctrl Pts',(2.63914010270947,-1.6302276196566,17.5918510143558));
#59513=CARTESIAN_POINT('Ctrl Pts',(3.04253593558097,-0.604082845323161,
17.6445212269736));
#59514=CARTESIAN_POINT('Ctrl Pts',(2.92490384793812,0.357866358949023,17.6971914395914));
#59515=CARTESIAN_POINT('Ctrl Pts',(2.80727176029526,1.31981556322121,17.7498616522092));
#59516=CARTESIAN_POINT('Ctrl Pts',(2.16861175213802,2.21756919743215,17.8025318648271));
#59517=CARTESIAN_POINT('Ctrl Pts',(1.29846231667931,2.64493812039898,17.8552020774449));
#59518=CARTESIAN_POINT('Ctrl Pts',(0.501074037772838,3.03657081710122,17.9034680516299));
#59519=CARTESIAN_POINT('Ctrl Pts',(-0.490708381591009,3.03319613617707,
17.951734025815));
#59520=CARTESIAN_POINT('Ctrl Pts',(-1.29200505722546,2.64817880365265,18.));
#59521=CARTESIAN_POINT('',(-1.37702479013096,-1.93106208855769,0.));
#59522=CARTESIAN_POINT('Ctrl Pts',(-1.3799494420105,-1.93347660712335,1.42247325030098E-16));
#59523=CARTESIAN_POINT('Ctrl Pts',(-1.43821263219875,-1.90182368491271,
1.23053055000976E-16));
#59524=CARTESIAN_POINT('Ctrl Pts',(-1.49490526047651,-1.86766952812869,
-2.48068321828561E-16));
#59525=CARTESIAN_POINT('Ctrl Pts',(-1.549846300109,-1.83106214637216,-2.13370987545147E-16));
#59526=CARTESIAN_POINT('Ctrl Pts',(-1.61731957854391,-1.78610449579702,
-1.67289625843952E-16));
#59527=CARTESIAN_POINT('Ctrl Pts',(-1.68215240278323,-1.73744874012217,
-3.23480018873332E-16));
#59528=CARTESIAN_POINT('Ctrl Pts',(-1.74427176305372,-1.68546195262933,
-2.84494650060196E-16));
#59529=CARTESIAN_POINT('Ctrl Pts',(-1.80797447841918,-1.63215007832797,
-2.44515586494396E-16));
#59530=CARTESIAN_POINT('Ctrl Pts',(-1.868824194171,-1.57533478867279,-1.55964265601244E-16));
#59531=CARTESIAN_POINT('Ctrl Pts',(-1.92672184730615,-1.51536121788337,
-2.35922392732846E-16));
#59532=CARTESIAN_POINT('Ctrl Pts',(-1.95606181343154,-1.48496926864022,
-2.76441629946403E-16));
#59533=CARTESIAN_POINT('Ctrl Pts',(-1.98464331411229,-1.45376551033272,
6.02784865253053E-16));
#59534=CARTESIAN_POINT('Ctrl Pts',(-2.01245082769788,-1.42179063200257,
6.52256026967279E-16));
#59535=CARTESIAN_POINT('Ctrl Pts',(-2.02687733290328,-1.40520210288967,
6.77921607235376E-16));
#59536=CARTESIAN_POINT('Ctrl Pts',(-2.04109548602495,-1.38840598216825,
-1.37311273491396E-16));
#59537=CARTESIAN_POINT('Ctrl Pts',(-2.05510290128969,-1.37140769097759,
-1.38777878078145E-16));
#59538=CARTESIAN_POINT('Ctrl Pts',(-2.0656990377528,-1.35854905791134,-1.39887314904631E-16));
#59539=CARTESIAN_POINT('Ctrl Pts',(-2.07617457831541,-1.34557473093587,
4.80447834609329E-16));
#59540=CARTESIAN_POINT('Ctrl Pts',(-2.08652842904455,-1.33248699500139,
4.78783679369599E-16));
#59541=CARTESIAN_POINT('Ctrl Pts',(-2.09478335563421,-1.32205239417602,
4.77456880317038E-16));
#59542=CARTESIAN_POINT('Ctrl Pts',(-2.10295522323914,-1.31155289687732,
2.18586909375805E-17));
#59543=CARTESIAN_POINT('Ctrl Pts',(-2.11104250565761,-1.30099164443844,
2.77555756156289E-17));
#59544=CARTESIAN_POINT('Ctrl Pts',(-2.16374877773385,-1.23216206539,6.61866322006358E-17));
#59545=CARTESIAN_POINT('Ctrl Pts',(-2.21288179583151,-1.16069141693027,
-6.93676353204663E-16));
#59546=CARTESIAN_POINT('Ctrl Pts',(-2.25835600178031,-1.08697821947129,
-6.24500451351651E-16));
#59547=CARTESIAN_POINT('Ctrl Pts',(-2.30474705056889,-1.01177882965603,
-5.5392983728813E-16));
#59548=CARTESIAN_POINT('Ctrl Pts',(-2.34733088662335,-0.934244926701822,
-1.69721227198088E-16));
#59549=CARTESIAN_POINT('Ctrl Pts',(-2.38598783736931,-0.854752868970769,
-1.38777878078145E-17));
#59550=CARTESIAN_POINT('Ctrl Pts',(-2.42492693896919,-0.774680611520505,
1.43103127732354E-16));
#59551=CARTESIAN_POINT('Ctrl Pts',(-2.45988224219415,-0.692620710719185,
2.60993908428853E-16));
#59552=CARTESIAN_POINT('Ctrl Pts',(-2.49069311686026,-0.608921827612739,
3.33066907387547E-16));
#59553=CARTESIAN_POINT('Ctrl Pts',(-2.50574516374886,-0.568032384301111,
3.6827675363451E-16));
#59554=CARTESIAN_POINT('Ctrl Pts',(-2.51980745733986,-0.526751310611613,
-3.26906346154409E-16));
#59555=CARTESIAN_POINT('Ctrl Pts',(-2.5328572845043,-0.485117072282149,
-3.19189119579733E-16));
#59556=CARTESIAN_POINT('Ctrl Pts',(-2.53785227082093,-0.469181041242136,
-3.16235253550921E-16));
#59557=CARTESIAN_POINT('Ctrl Pts',(-2.54269948804001,-0.453190870391766,
-7.06596396842216E-16));
#59558=CARTESIAN_POINT('Ctrl Pts',(-2.54739126005051,-0.437171230049419,
-6.80011602582908E-16));
#59559=CARTESIAN_POINT('Ctrl Pts',(-2.57317421298316,-0.349137618863687,
-5.33918719642838E-16));
#59560=CARTESIAN_POINT('Ctrl Pts',(-2.59431180385391,-0.260075883706848,
-3.6235006954443E-17));
#59561=CARTESIAN_POINT('Ctrl Pts',(-2.61068704576328,-0.170387020957126,
-5.55111512312578E-17));
#59562=CARTESIAN_POINT('Ctrl Pts',(-2.62702393945783,-0.0809081952739614,
-7.47421538408212E-17));
#59563=CARTESIAN_POINT('Ctrl Pts',(-2.63862130354526,0.00919573051068487,
-2.73664664561228E-16));
#59564=CARTESIAN_POINT('Ctrl Pts',(-2.64532172794212,0.0995568412614959,
-2.22044604925031E-16));
#59565=CARTESIAN_POINT('Ctrl Pts',(-2.65107237655398,0.177109390970093,
-1.77741616530647E-16));
#59566=CARTESIAN_POINT('Ctrl Pts',(-2.65321550243264,0.254852199236274,
1.12929186103332E-17));
#59567=CARTESIAN_POINT('Ctrl Pts',(-2.65162265236425,0.332562839778456,
0.));
#59568=CARTESIAN_POINT('Ctrl Pts',(-2.65043736981845,0.390389415979805,
1.93522113658955E-17));
#59569=CARTESIAN_POINT('Ctrl Pts',(-2.64718281331851,0.44819839777396,-2.31905195015141E-17));
#59570=CARTESIAN_POINT('Ctrl Pts',(-2.64191368221943,0.505918652854124,
-5.55111512312578E-17));
#59571=CARTESIAN_POINT('Ctrl Pts',(-2.64062714885064,0.520011874833084,
-6.34026935821171E-17));
#59572=CARTESIAN_POINT('Ctrl Pts',(-2.63922017825452,0.534102463086072,
2.85447298507148E-17));
#59573=CARTESIAN_POINT('Ctrl Pts',(-2.63769444945471,0.54818059290278,2.77555756156289E-17));
#59574=CARTESIAN_POINT('Ctrl Pts',(-2.62812339489243,0.636494157297667,
2.28051294793074E-17));
#59575=CARTESIAN_POINT('Ctrl Pts',(-2.61390606721349,0.724122954628742,
-4.18247658184506E-16));
#59576=CARTESIAN_POINT('Ctrl Pts',(-2.59532950233633,0.810804767956044,
-3.60822483003176E-16));
#59577=CARTESIAN_POINT('Ctrl Pts',(-2.57528112215592,0.904354353673597,
-2.98847529529524E-16));
#59578=CARTESIAN_POINT('Ctrl Pts',(-2.55015582011987,0.996801631758693,
-3.84935125803439E-17));
#59579=CARTESIAN_POINT('Ctrl Pts',(-2.52025055163084,1.08782868833812,2.77555756156289E-17));
#59580=CARTESIAN_POINT('Ctrl Pts',(-2.49271682268382,1.1716371418092,8.87509964741449E-17));
#59581=CARTESIAN_POINT('Ctrl Pts',(-2.4611302440109,1.25424238620021,0.));
#59582=CARTESIAN_POINT('Ctrl Pts',(-2.42567698904207,1.33539544644047,0.));
#59583=CARTESIAN_POINT('Ctrl Pts',(-2.40983756184422,1.37165214531589,0.));
#59584=CARTESIAN_POINT('Ctrl Pts',(-2.393225777586,1.40761891354161,-2.28767883718138E-16));
#59585=CARTESIAN_POINT('Ctrl Pts',(-2.37585563123953,1.4432729734042,-2.77555756156289E-16));
#59586=CARTESIAN_POINT('Ctrl Pts',(-2.36243258110441,1.47082520143443,-3.15257341661739E-16));
#59587=CARTESIAN_POINT('Ctrl Pts',(-2.34855663009738,1.49819068371341,-2.16366534335116E-16));
#59588=CARTESIAN_POINT('Ctrl Pts',(-2.33423361450165,1.525358672182,-1.94289029309402E-16));
#59589=CARTESIAN_POINT('Ctrl Pts',(-2.32544410379061,1.54203067285435,-1.80740872107477E-16));
#59590=CARTESIAN_POINT('Ctrl Pts',(-2.31648502739695,1.55863024006332,-2.44555389199E-16));
#59591=CARTESIAN_POINT('Ctrl Pts',(-2.30736938707237,1.57513424614642,-2.22044604925031E-16));
#59592=CARTESIAN_POINT('Ctrl Pts',(-2.26079576520303,1.65945650012684,-1.07032524870574E-16));
#59593=CARTESIAN_POINT('Ctrl Pts',(-2.21007880645611,1.74140267576173,4.6804266504151E-16));
#59594=CARTESIAN_POINT('Ctrl Pts',(-2.15547853607709,1.82066722818668,2.22044604925031E-16));
#59595=CARTESIAN_POINT('Ctrl Pts',(-2.09852378318569,1.90334984065495,-3.45614270312331E-17));
#59596=CARTESIAN_POINT('Ctrl Pts',(-2.0373435353391,1.983115662051,-7.77281236950037E-17));
#59597=CARTESIAN_POINT('Ctrl Pts',(-1.97217568716847,2.05960284446263,-5.55111512312578E-17));
#59598=CARTESIAN_POINT('Ctrl Pts',(-1.95099981991528,2.08445685555532,-4.82918909231929E-17));
#59599=CARTESIAN_POINT('Ctrl Pts',(-1.92940247813391,2.10896449437444,8.29443404019046E-17));
#59600=CARTESIAN_POINT('Ctrl Pts',(-1.90739062217049,2.13311271156995,5.55111512312578E-17));
#59601=CARTESIAN_POINT('Ctrl Pts',(-1.89181625573621,2.15019864852877,3.61009505959917E-17));
#59602=CARTESIAN_POINT('Ctrl Pts',(-1.8760313823833,2.16710758411654,-7.69645308807625E-17));
#59603=CARTESIAN_POINT('Ctrl Pts',(-1.86005799875434,2.18381470943084,-5.55111512312578E-17));
#59604=CARTESIAN_POINT('Ctrl Pts',(-1.79161590462605,2.25540070961311,3.64114034038663E-17));
#59605=CARTESIAN_POINT('Ctrl Pts',(-1.71965512009666,2.32335348522212,6.21368422360659E-16));
#59606=CARTESIAN_POINT('Ctrl Pts',(-1.64441684451929,2.38734608371888,4.44089209850063E-16));
#59607=CARTESIAN_POINT('Ctrl Pts',(-1.57011202763153,2.45054474526429,2.69009447288759E-16));
#59608=CARTESIAN_POINT('Ctrl Pts',(-1.49261003531049,2.5098817110976,1.70169119721682E-16));
#59609=CARTESIAN_POINT('Ctrl Pts',(-1.41210026973023,2.56501611482162,2.22044604925031E-16));
#59610=CARTESIAN_POINT('Ctrl Pts',(-1.37178873803333,2.59262211078115,2.48018848558651E-16));
#59611=CARTESIAN_POINT('Ctrl Pts',(-1.33072251584557,2.61917402239002,1.62339022710125E-17));
#59612=CARTESIAN_POINT('Ctrl Pts',(-1.28892185405323,2.64462557919718,0.));
#59613=CARTESIAN_POINT('Ctrl Pts',(-1.37994944201052,-1.93347660712334,
-9.85539774789324E-16));
#59614=CARTESIAN_POINT('Ctrl Pts',(-0.794121452243435,-2.34631813400529,
0.0482659741850328));
#59615=CARTESIAN_POINT('Ctrl Pts',(0.854011297622218,-2.62815453910416,
0.149202160987898));
#59616=CARTESIAN_POINT('Ctrl Pts',(2.68362344803569,-0.794509576969642,
0.302808560408595));
#59617=CARTESIAN_POINT('Ctrl Pts',(2.13140048014165,1.81430348231616,0.46081919826209));
#59618=CARTESIAN_POINT('Ctrl Pts',(-0.355015924163216,2.7760602537354,0.618829836115584));
#59619=CARTESIAN_POINT('Ctrl Pts',(-2.12533378997424,1.50275432854008,0.748086733996563));
#59620=CARTESIAN_POINT('Ctrl Pts',(-2.36885104996457,0.358299771164603,
0.824673419259709));
#59621=CARTESIAN_POINT('Ctrl Pts',(-2.36807033412218,0.000590439285148986,
0.848589891905023));
#59622=CARTESIAN_POINT('Origin',(0.,0.,-1.848589891905));
#59623=CARTESIAN_POINT('',(1.37702479013102,-1.93106208855765,0.));
#59624=CARTESIAN_POINT('Origin',(0.,0.,0.));
#59625=CARTESIAN_POINT('Ctrl Pts',(1.37702479013102,-1.93106208855765,-4.44089209850063E-15));
#59626=CARTESIAN_POINT('Ctrl Pts',(2.01608411688934,-1.47535404036748,0.0526702126178271));
#59627=CARTESIAN_POINT('Ctrl Pts',(2.79574737452458,0.112154857826279,0.15801063785349));
#59628=CARTESIAN_POINT('Ctrl Pts',(1.43092122672701,2.40744480175264,0.316021275706985));
#59629=CARTESIAN_POINT('Ctrl Pts',(-1.23339961524159,2.5114765043851,0.47403191356048));
#59630=CARTESIAN_POINT('Ctrl Pts',(-2.3262441272451,0.975284966418893,0.585828191023147));
#59631=CARTESIAN_POINT('Ctrl Pts',(-2.37490421603833,0.0976170616511061,
0.644954255867982));
#59632=CARTESIAN_POINT('Ctrl Pts',(-2.37417832678934,0.00170073231846661,
0.651410108094986));
#59633=CARTESIAN_POINT('Ctrl Pts',(1.70810875200392,-2.3953556085324,-0.329233991005388));
#59634=CARTESIAN_POINT('Ctrl Pts',(2.50081984690136,-1.83007972457522,-0.276563778387557));
#59635=CARTESIAN_POINT('Ctrl Pts',(3.46794087734851,0.139120730146379,-0.171223353151894));
#59636=CARTESIAN_POINT('Ctrl Pts',(1.77496373944601,2.9862770556577,-0.0132127152983989));
#59637=CARTESIAN_POINT('Ctrl Pts',(-1.52995116181745,3.11532154565238,0.144797922555096));
#59638=CARTESIAN_POINT('Ctrl Pts',(-3.4459318095318,0.422062600215018,0.302808560408591));
#59639=CARTESIAN_POINT('Ctrl Pts',(-2.23574402944417,-2.65637266992881,
0.460819198262086));
#59640=CARTESIAN_POINT('Ctrl Pts',(1.00319880637436,-3.3234545571268,0.618829836115579));
#59641=CARTESIAN_POINT('Ctrl Pts',(3.3318047603238,-0.975698335728692,0.776840473969075));
#59642=CARTESIAN_POINT('Ctrl Pts',(2.6374449866523,2.25765082687173,0.93485111182257));
#59643=CARTESIAN_POINT('Ctrl Pts',(-0.449960500168118,3.44241375743347,
1.09286174967606));
#59644=CARTESIAN_POINT('Ctrl Pts',(-3.12909038149708,1.50388208255809,1.25087238752956));
#59645=CARTESIAN_POINT('Ctrl Pts',(-2.96913211278082,-1.79920261568766,
1.40888302538306));
#59646=CARTESIAN_POINT('Ctrl Pts',(-0.115206809624608,-3.46980492478986,
1.56689366323655));
#59647=CARTESIAN_POINT('Ctrl Pts',(2.84324601940593,-1.99218504829265,1.72490430109004));
#59648=CARTESIAN_POINT('Ctrl Pts',(3.22195677616531,1.29299725638943,1.88291493894354));
#59649=CARTESIAN_POINT('Ctrl Pts',(0.677310549247169,3.40500961935277,2.04092557679703));
#59650=CARTESIAN_POINT('Ctrl Pts',(-2.48187497014949,2.42757932674622,2.19893621465053));
#59651=CARTESIAN_POINT('Ctrl Pts',(-3.3891977506279,-0.752451120820911,
2.35694685250402));
#59652=CARTESIAN_POINT('Ctrl Pts',(-1.22142245825137,-3.24976466317345,
2.51495749035752));
#59653=CARTESIAN_POINT('Ctrl Pts',(2.05457780458113,-2.7984913665756,2.67296812821101));
#59654=CARTESIAN_POINT('Ctrl Pts',(3.46641184197517,0.191918400748076,2.83097876606451));
#59655=CARTESIAN_POINT('Ctrl Pts',(1.73308974204474,3.00819606632432,2.988989403918));
#59656=CARTESIAN_POINT('Ctrl Pts',(-1.57270500142412,3.09506748020428,3.1470000417715));
#59657=CARTESIAN_POINT('Ctrl Pts',(-3.45154790528896,0.373712130524309,
3.30501067962499));
#59658=CARTESIAN_POINT('Ctrl Pts',(-2.19872107855347,-2.68672092091844,
3.46302131747849));
#59659=CARTESIAN_POINT('Ctrl Pts',(1.0490565439494,-3.3094295686813,3.62103195533198));
#59660=CARTESIAN_POINT('Ctrl Pts',(3.34500075407871,-0.929415758674134,
3.77904259318548));
#59661=CARTESIAN_POINT('Ctrl Pts',(2.6059479447461,2.29387859434484,3.93705323103896));
#59662=CARTESIAN_POINT('Ctrl Pts',(-0.497542072670693,3.43588352308502,
4.09506386889247));
#59663=CARTESIAN_POINT('Ctrl Pts',(-3.14960059029087,1.46043138115332,4.25307450674595));
#59664=CARTESIAN_POINT('Ctrl Pts',(-2.9439532040605,-1.8401041355524,4.41108514459945));
#59665=CARTESIAN_POINT('Ctrl Pts',(-0.0671885727859433,-3.47107035269011,
4.56909578245295));
#59666=CARTESIAN_POINT('Ctrl Pts',(2.87053781400266,-1.95265367023439,4.72710642030644));
#59667=CARTESIAN_POINT('Ctrl Pts',(3.203758447428,1.33745112360787,4.88511705815994));
#59668=CARTESIAN_POINT('Ctrl Pts',(0.630134493061158,3.41405539178769,5.04312769601343));
#59669=CARTESIAN_POINT('Ctrl Pts',(-2.51522514949815,2.39300776113466,5.20113833386693));
#59670=CARTESIAN_POINT('Ctrl Pts',(-3.37846248699513,-0.799271494229795,
5.35914897172041));
#59671=CARTESIAN_POINT('Ctrl Pts',(-1.17634219639961,-3.26635312458643,
5.51715960957392));
#59672=CARTESIAN_POINT('Ctrl Pts',(2.0931007413652,-2.76979656004174,5.67517024742741));
#59673=CARTESIAN_POINT('Ctrl Pts',(3.46342467200507,0.239860873987174,5.83318088528091));
#59674=CARTESIAN_POINT('Ctrl Pts',(1.69130280710249,3.03188695571109,5.9911915231344));
#59675=CARTESIAN_POINT('Ctrl Pts',(-1.61537744970865,3.07301145336234,6.1492021609879));
#59676=CARTESIAN_POINT('Ctrl Pts',(-3.45638815808628,0.325921153293867,
6.30721279884139));
#59677=CARTESIAN_POINT('Ctrl Pts',(-2.16133746373299,-2.71688499303665,
6.46522343669488));
#59678=CARTESIAN_POINT('Ctrl Pts',(1.09474500375374,-3.29459816582837,6.62323407454838));
#59679=CARTESIAN_POINT('Ctrl Pts',(3.35753985564886,-0.883045760565633,
6.78124471240187));
#59680=CARTESIAN_POINT('Ctrl Pts',(2.57396066972148,2.32971461090203,6.93925535025537));
#59681=CARTESIAN_POINT('Ctrl Pts',(-0.545032925486335,3.42867070563204,
7.09726598810886));
#59682=CARTESIAN_POINT('Ctrl Pts',(-3.16950546499722,1.41671408720188,7.25527662596235));
#59683=CARTESIAN_POINT('Ctrl Pts',(-2.91821194470713,-1.88066018814992,
7.41328726381586));
#59684=CARTESIAN_POINT('Ctrl Pts',(-0.0191568229389774,-3.47166771360082,
7.57129790166934));
#59685=CARTESIAN_POINT('Ctrl Pts',(2.89727973004295,-1.91275034006159,7.72930853952286));
#59686=CARTESIAN_POINT('Ctrl Pts',(3.18494696698455,1.38164992491564,7.88731917737633));
#59687=CARTESIAN_POINT('Ctrl Pts',(0.58283771006284,3.42244706332358,8.04532981522985));
#59688=CARTESIAN_POINT('Ctrl Pts',(-2.54809376328382,2.3579783440561,8.20334045308332));
#59689=CARTESIAN_POINT('Ctrl Pts',(-3.3670804734595,-0.845938994710182,
8.36135109093683));
#59690=CARTESIAN_POINT('Ctrl Pts',(-1.13103672127189,-3.28231619937171,
8.51936172879031));
#59691=CARTESIAN_POINT('Ctrl Pts',(2.13122296628565,-2.74057153993471,8.67737236664381));
#59692=CARTESIAN_POINT('Ctrl Pts',(3.45977446497974,0.287757448205339,8.83538300449731));
#59693=CARTESIAN_POINT('Ctrl Pts',(1.64919208590229,3.0549974077437,8.9933936423508));
#59694=CARTESIAN_POINT('Ctrl Pts',(-1.65774064786191,3.05036713232192,9.1514042802043));
#59695=CARTESIAN_POINT('Ctrl Pts',(-3.46056671775639,0.278067778572342,
9.30941491805778));
#59696=CARTESIAN_POINT('Ctrl Pts',(-2.12354008050013,-2.74652894105141,
9.46742555591129));
#59697=CARTESIAN_POINT('Ctrl Pts',(1.14022388457288,-3.27913604331583,9.62543619376477));
#59698=CARTESIAN_POINT('Ctrl Pts',(3.36943618723632,-0.836506711070431,
9.78344683161829));
#59699=CARTESIAN_POINT('Ctrl Pts',(2.54148063361152,2.365104624853,9.94145746947176));
#59700=CARTESIAN_POINT('Ctrl Pts',(-0.592419436751292,3.42080150088876,
10.0994681073253));
#59701=CARTESIAN_POINT('Ctrl Pts',(-3.18880356710694,1.37272557633691,10.2574787451788));
#59702=CARTESIAN_POINT('Ctrl Pts',(-2.8919120205688,-1.92085620565756,10.4154893830323));
#59703=CARTESIAN_POINT('Ctrl Pts',(0.0288785943022343,-3.47160045574294,
10.5735000208857));
#59704=CARTESIAN_POINT('Ctrl Pts',(2.92346698858513,-1.87248083145767,10.7315106587392));
#59705=CARTESIAN_POINT('Ctrl Pts',(3.16552575779954,1.42558422207569,10.8895212965927));
#59706=CARTESIAN_POINT('Ctrl Pts',(0.535429348157471,3.4301835389167,11.0475319344462));
#59707=CARTESIAN_POINT('Ctrl Pts',(-2.58047456800486,2.32249751375618,11.2055425722997));
#59708=CARTESIAN_POINT('Ctrl Pts',(-3.35505386340194,-0.892444547966527,
11.3635532101532));
#59709=CARTESIAN_POINT('Ctrl Pts',(-1.08551471958888,-3.2976509049745,11.5215638480067));
#59710=CARTESIAN_POINT('Ctrl Pts',(2.16893718821302,-2.71082186266645,11.6795744858602));
#59711=CARTESIAN_POINT('Ctrl Pts',(3.45546191602226,0.335598933912326,11.8375851237137));
#59712=CARTESIAN_POINT('Ctrl Pts',(1.60676564207814,3.07752300868082,11.9955957615672));
#59713=CARTESIAN_POINT('Ctrl Pts',(-1.69978648684786,3.02713884660998,12.1536063994207));
#59714=CARTESIAN_POINT('Ctrl Pts',(-3.46408278382471,0.230161170336986,
12.3116170372742));
#59715=CARTESIAN_POINT('Ctrl Pts',(-2.08533616509223,-2.77564709141439,
12.4696276751277));
#59716=CARTESIAN_POINT('Ctrl Pts',(1.18548448003973,-3.26304616043428,12.6276383129812));
#59717=CARTESIAN_POINT('Ctrl Pts',(3.38068747132074,-0.789807520071332,
12.7856489508347));
#59718=CARTESIAN_POINT('Ctrl Pts',(2.50851405446239,2.40004186131487,12.9436595886882));
#59719=CARTESIAN_POINT('Ctrl Pts',(-0.639692534781115,3.41227741524375,
13.1016702265417));
#59720=CARTESIAN_POINT('Ctrl Pts',(-3.20749120215462,1.32847426978314,13.2596808643952));
#59721=CARTESIAN_POINT('Ctrl Pts',(-2.86505846654987,-1.96068449289242,
13.4176915022487));
#59722=CARTESIAN_POINT('Ctrl Pts',(0.0769084830419716,-3.47086859208481,
13.5757021401021));
#59723=CARTESIAN_POINT('Ctrl Pts',(2.94909457624333,-1.83185285344978,13.7337127779556));
#59724=CARTESIAN_POINT('Ctrl Pts',(3.14549853802855,1.46924560387948,13.8917234158091));
#59725=CARTESIAN_POINT('Ctrl Pts',(0.487918482964918,3.43726333824546,14.0497340536626));
#59726=CARTESIAN_POINT('Ctrl Pts',(-2.61236136413192,2.28657206126704,14.2077446915161));
#59727=CARTESIAN_POINT('Ctrl Pts',(-3.34238496020413,-0.938779248176496,
14.3657553293696));
#59728=CARTESIAN_POINT('Ctrl Pts',(-1.03978490421238,-3.31235431098403,
14.5237659672231));
#59729=CARTESIAN_POINT('Ctrl Pts',(2.20623618346753,-2.68055321345958,14.6817766050766));
#59730=CARTESIAN_POINT('Ctrl Pts',(3.45048785768122,0.383376153047962,14.8397872429301));
#59731=CARTESIAN_POINT('Ctrl Pts',(1.56403158450715,3.09945948296467,14.9977978807836));
#59732=CARTESIAN_POINT('Ctrl Pts',(-1.74150689202679,3.00333097286243,15.1558085186371));
#59733=CARTESIAN_POINT('Ctrl Pts',(-3.46693573158834,0.182210633943016,
15.3138191564906));
#59734=CARTESIAN_POINT('Ctrl Pts',(-2.04673293883378,-2.8042341257807,15.4718297943441));
#59735=CARTESIAN_POINT('Ctrl Pts',(1.2305179488465,-3.24633110843195,15.6298404321976));
#59736=CARTESIAN_POINT('Ctrl Pts',(3.39129189118379,-0.742958061601936,
15.7878510700511));
#59737=CARTESIAN_POINT('Ctrl Pts',(2.47506659937511,2.43452141542566,15.9458617079046));
#59738=CARTESIAN_POINT('Ctrl Pts',(-0.686841939590187,3.40309667436876,
16.1038723457581));
#59739=CARTESIAN_POINT('Ctrl Pts',(-3.22556714156735,1.28397514410703,16.2618829836115));
#59740=CARTESIAN_POINT('Ctrl Pts',(-2.83765193744026,-2.00014984832596,
16.4198936214651));
#59741=CARTESIAN_POINT('Ctrl Pts',(0.124915080987664,-3.46944853710508,
16.5779042593186));
#59742=CARTESIAN_POINT('Ctrl Pts',(2.97417394872773,-1.7909194946734,16.735914897172));
#59743=CARTESIAN_POINT('Ctrl Pts',(3.12483789403196,1.51271224602764,16.8939255350255));
#59744=CARTESIAN_POINT('Ctrl Pts',(0.440373887044776,3.44351983848023,17.051936172879));
#59745=CARTESIAN_POINT('Ctrl Pts',(-2.64386202524497,2.25052454290272,17.2099468107325));
#59746=CARTESIAN_POINT('Ctrl Pts',(-3.32885844512377,-0.985537582627644,
17.367957448586));
#59747=CARTESIAN_POINT('Ctrl Pts',(-0.994272503154261,-3.32526706894708,
17.5259680864395));
#59748=CARTESIAN_POINT('Ctrl Pts',(2.24391376251738,-2.65201771409636,17.683978724293));
#59749=CARTESIAN_POINT('Ctrl Pts',(3.44327361237846,0.435700971584197,17.8419893621465));
#59750=CARTESIAN_POINT('Ctrl Pts',(2.16412553195871,2.21807402646564,17.9473297873822));
#59751=CARTESIAN_POINT('Ctrl Pts',(1.28892185405319,2.64462557919719,18.));
#59752=CARTESIAN_POINT('Ctrl Pts',(1.59774743137962,-2.24059110187415,-0.219489327336927));
#59753=CARTESIAN_POINT('Ctrl Pts',(2.33924127023069,-1.71183782983931,-0.166819114719096));
#59754=CARTESIAN_POINT('Ctrl Pts',(3.2438763764072,0.130132106039679,-0.0614786894834324));
#59755=CARTESIAN_POINT('Ctrl Pts',(1.66028290187301,2.79333297102268,0.0965319483700627));
#59756=CARTESIAN_POINT('Ctrl Pts',(-1.43110064629217,2.91403986522995,0.254542586223557));
#59757=CARTESIAN_POINT('Ctrl Pts',(-3.22328931979857,0.394793033279504,
0.412553224077053));
#59758=CARTESIAN_POINT('Ctrl Pts',(-2.0912920656111,-2.48474378764615,0.570563861930546));
#59759=CARTESIAN_POINT('Ctrl Pts',(0.938381888253501,-3.10872535236795,
0.728574499784042));
#59760=CARTESIAN_POINT('Ctrl Pts',(3.11653604691177,-0.912658229684108,
0.886585137637534));
#59761=CARTESIAN_POINT('Ctrl Pts',(2.46703902657541,2.11178345954526,1.04459577549103));
#59762=CARTESIAN_POINT('Ctrl Pts',(-0.42088844315241,3.21999856989931,1.20260641334452));
#59763=CARTESIAN_POINT('Ctrl Pts',(-2.92691909325228,1.40671589656455,1.36061705119802));
#59764=CARTESIAN_POINT('Ctrl Pts',(-2.77729576706211,-1.68295569844364,
1.51862768905151));
#59765=CARTESIAN_POINT('Ctrl Pts',(-0.107763269721067,-3.2456199872914,
1.67663832690501));
#59766=CARTESIAN_POINT('Ctrl Pts',(2.65954320470322,-1.86346948928641,1.8346489647585));
#59767=CARTESIAN_POINT('Ctrl Pts',(3.01378536764409,1.20945639014698,1.992659602612));
#59768=CARTESIAN_POINT('Ctrl Pts',(0.633549350435882,3.18501112224923,2.15067024046549));
#59769=CARTESIAN_POINT('Ctrl Pts',(-2.32152042655924,2.27073283784104,2.30868087831899));
#59770=CARTESIAN_POINT('Ctrl Pts',(-3.17022086219649,-0.703835071461303,
2.46669151617248));
#59771=CARTESIAN_POINT('Ctrl Pts',(-1.14250605707099,-3.03979658033019,
2.62470215402598));
#59772=CARTESIAN_POINT('Ctrl Pts',(1.92183103446304,-2.61768016084369,2.78271279187947));
#59773=CARTESIAN_POINT('Ctrl Pts',(3.24244613238007,0.179518506342186,2.94072342973297));
#59774=CARTESIAN_POINT('Ctrl Pts',(1.62111439359683,2.81383578909553,3.09873406758646));
#59775=CARTESIAN_POINT('Ctrl Pts',(-1.47109214995551,2.89509441986136,3.25674470543996));
#59776=CARTESIAN_POINT('Ctrl Pts',(-3.22854255824715,0.349566499158832,
3.41475534329345));
#59777=CARTESIAN_POINT('Ctrl Pts',(-2.05666117655423,-2.51313123078094,
3.57276598114695));
#59778=CARTESIAN_POINT('Ctrl Pts',(0.981276746284894,-3.09560652182649,
3.73077661900044));
#59779=CARTESIAN_POINT('Ctrl Pts',(3.1288794443106,-0.869365981154969,3.88878725685394));
#59780=CARTESIAN_POINT('Ctrl Pts',(2.43757701618371,2.14567054217795,4.04679789470743));
#59781=CARTESIAN_POINT('Ctrl Pts',(-0.465395758718706,3.21389025557547,
4.20480853256093));
#59782=CARTESIAN_POINT('Ctrl Pts',(-2.94610413248288,1.36607255551284,4.36281917041442));
#59783=CARTESIAN_POINT('Ctrl Pts',(-2.75374367373922,-1.72121456119272,
4.52082980826791));
#59784=CARTESIAN_POINT('Ctrl Pts',(-0.0628475028073083,-3.24680365558819,
4.67884044612141));
#59785=CARTESIAN_POINT('Ctrl Pts',(2.68507166983374,-1.82649224314949,4.8368510839749));
#59786=CARTESIAN_POINT('Ctrl Pts',(2.99676283733896,1.25103808222591,4.9948617218284));
#59787=CARTESIAN_POINT('Ctrl Pts',(0.589421350678613,3.19347244513383,5.1528723596819));
#59788=CARTESIAN_POINT('Ctrl Pts',(-2.35271584273392,2.23839494946604,5.31088299753539));
#59789=CARTESIAN_POINT('Ctrl Pts',(-3.16017920654996,-0.747630369191917,
5.46889363538888));
#59790=CARTESIAN_POINT('Ctrl Pts',(-1.10033844186788,-3.05531325722915,
5.62690427324238));
#59791=CARTESIAN_POINT('Ctrl Pts',(1.95786499496102,-2.59083933271748,5.78491491109587));
#59792=CARTESIAN_POINT('Ctrl Pts',(3.23965196418602,0.224363404760918,5.94292554894936));
#59793=CARTESIAN_POINT('Ctrl Pts',(1.5820273226531,2.83599600437479,6.10093618680287));
#59794=CARTESIAN_POINT('Ctrl Pts',(-1.51100752100979,2.8744634382615,6.25894682465635));
#59795=CARTESIAN_POINT('Ctrl Pts',(-3.23307008113764,0.304863308554905,
6.41695746250985));
#59796=CARTESIAN_POINT('Ctrl Pts',(-2.02169292615153,-2.54134639488584,
6.57496810036335));
#59797=CARTESIAN_POINT('Ctrl Pts',(1.0240132636234,-3.08173337950799,6.73297873821683));
#59798=CARTESIAN_POINT('Ctrl Pts',(3.140608391488,-0.825991959867379,6.89098937607034));
#59799=CARTESIAN_POINT('Ctrl Pts',(2.40765644675425,2.17919118501639,7.04900001392383));
#59800=CARTESIAN_POINT('Ctrl Pts',(-0.509818216019039,3.20714346000698,
7.20701065177733));
#59801=CARTESIAN_POINT('Ctrl Pts',(-2.96472294840821,1.32517984652353,7.36502128963082));
#59802=CARTESIAN_POINT('Ctrl Pts',(-2.72966556339403,-1.75915027739847,
7.52303192748432));
#59803=CARTESIAN_POINT('Ctrl Pts',(-0.0179190959639986,-3.24736242086562,
7.6810425653378));
#59804=CARTESIAN_POINT('Ctrl Pts',(2.71008578419468,-1.78916707681433,7.83905320319131));
#59805=CARTESIAN_POINT('Ctrl Pts',(2.97916677120809,1.29238118826451,7.99706384104479));
#59806=CARTESIAN_POINT('Ctrl Pts',(0.545180424297654,3.2013219287371,8.1550744788983));
#59807=CARTESIAN_POINT('Ctrl Pts',(-2.38346080741339,2.20562879151835,8.31308511675178));
#59808=CARTESIAN_POINT('Ctrl Pts',(-3.14953258766861,-0.791282671151008,
8.47109575460529));
#59809=CARTESIAN_POINT('Ctrl Pts',(-1.05796016447317,-3.07024495388206,
8.62910639245878));
#59810=CARTESIAN_POINT('Ctrl Pts',(1.99352413368603,-2.56350254824561,8.78711703031228));
#59811=CARTESIAN_POINT('Ctrl Pts',(3.23623759792164,0.26916536970558,8.94512766816576));
#59812=CARTESIAN_POINT('Ctrl Pts',(1.54263738536003,2.85761328449809,9.10313830601927));
#59813=CARTESIAN_POINT('Ctrl Pts',(-1.55063362265875,2.85328217229397,9.26114894387275));
#59814=CARTESIAN_POINT('Ctrl Pts',(-3.23697866305431,0.260101751976928,
9.41915958172626));
#59815=CARTESIAN_POINT('Ctrl Pts',(-1.98633764101391,-2.56907504023173,
9.57717021957974));
#59816=CARTESIAN_POINT('Ctrl Pts',(1.06655374292576,-3.06727026848002,9.73518085743324));
#59817=CARTESIAN_POINT('Ctrl Pts',(3.15173609820715,-0.782459809644175,
9.89319149528675));
#59818=CARTESIAN_POINT('Ctrl Pts',(2.37727495365263,2.21229464158513,10.0512021331402));
#59819=CARTESIAN_POINT('Ctrl Pts',(-0.554143073301574,3.19978268649018,
10.2092127709937));
#59820=CARTESIAN_POINT('Ctrl Pts',(-2.9827741954615,1.28403344401124,10.3672234088472));
#59821=CARTESIAN_POINT('Ctrl Pts',(-2.70506488373111,-1.79674922046879,
10.5252340467007));
#59822=CARTESIAN_POINT('Ctrl Pts',(0.027012741322331,-3.24729950855425,
10.6832446845542));
#59823=CARTESIAN_POINT('Ctrl Pts',(2.73458107761294,-1.75149939092527,10.8412553224077));
#59824=CARTESIAN_POINT('Ctrl Pts',(2.96100037105749,1.33347687983249,10.9992659602612));
#59825=CARTESIAN_POINT('Ctrl Pts',(0.500835128149877,3.20855854876633,11.1572765981147));
#59826=CARTESIAN_POINT('Ctrl Pts',(-2.41374948049017,2.17244038626699,11.3152872359682));
#59827=CARTESIAN_POINT('Ctrl Pts',(-3.13828301980291,-0.834783489335473,
11.4732978738217));
#59828=CARTESIAN_POINT('Ctrl Pts',(-1.01537935035641,-3.08458888043772,
11.6313085116752));
#59829=CARTESIAN_POINT('Ctrl Pts',(2.02880163059028,-2.53567500483893,11.7893191495287));
#59830=CARTESIAN_POINT('Ctrl Pts',(3.23220368379796,0.313915805421134,11.9473297873822));
#59831=CARTESIAN_POINT('Ctrl Pts',(1.50295212435831,2.87868350089698,12.1053404252357));
#59832=CARTESIAN_POINT('Ctrl Pts',(-1.58996286979316,2.83155467175394,12.2633510630892));
#59833=CARTESIAN_POINT('Ctrl Pts',(-3.24026755524143,0.215290401315357,
12.4213617009427));
#59834=CARTESIAN_POINT('Ctrl Pts',(-1.95060208984364,-2.59631185983962,
12.5793723387961));
#59835=CARTESIAN_POINT('Ctrl Pts',(1.10889004034537,-3.05221995683268,12.7373829766496));
#59836=CARTESIAN_POINT('Ctrl Pts',(3.16226043409883,-0.738777864698467,
12.8953936145032));
#59837=CARTESIAN_POINT('Ctrl Pts',(2.34643835317558,2.24497457472812,13.0534042523566));
#59838=CARTESIAN_POINT('Ctrl Pts',(-0.598361845005598,3.19180934408549,
13.2114148902101));
#59839=CARTESIAN_POINT('Ctrl Pts',(-3.00025441787765,1.24264122510332,13.3694255280636));
#59840=CARTESIAN_POINT('Ctrl Pts',(-2.6799463443484,-1.83400419240843,13.5274361659171));
#59841=CARTESIAN_POINT('Ctrl Pts',(0.0719394073050037,-3.24661493078452,
13.6854468037706));
#59842=CARTESIAN_POINT('Ctrl Pts',(2.75855286061874,-1.71349639642736,13.8434574416241));
#59843=CARTESIAN_POINT('Ctrl Pts',(2.94226711481182,1.37431728917156,14.0014680794776));
#59844=CARTESIAN_POINT('Ctrl Pts',(0.45639395147716,3.21518092054385,14.1594787173311));
#59845=CARTESIAN_POINT('Ctrl Pts',(-2.44357606298802,2.13883608597385,14.3174893551846));
#59846=CARTESIAN_POINT('Ctrl Pts',(-3.12643265751249,-0.878124493330309,
14.4754999930381));
#59847=CARTESIAN_POINT('Ctrl Pts',(-0.972604149439291,-3.09834229581991,
14.6335106308916));
#59848=CARTESIAN_POINT('Ctrl Pts',(2.06369072871768,-2.50736202039641,14.7915212687451));
#59849=CARTESIAN_POINT('Ctrl Pts',(3.22755100057236,0.358606126844088,14.9495319065986));
#59850=CARTESIAN_POINT('Ctrl Pts',(1.46297912460851,2.89920265425852,15.1075425444521));
#59851=CARTESIAN_POINT('Ctrl Pts',(-1.62898770947773,2.8092850305018,15.2655531823055));
#59852=CARTESIAN_POINT('Ctrl Pts',(-3.2429361733583,0.170437960704151,15.4235638201591));
#59853=CARTESIAN_POINT('Ctrl Pts',(-1.9144930273937,-2.62305187898416,15.5815744580125));
#59854=CARTESIAN_POINT('Ctrl Pts',(1.15101388581347,-3.03658486839304,15.739585095866));
#59855=CARTESIAN_POINT('Ctrl Pts',(3.17217969982332,-0.694955361100154,
15.8975957337195));
#59856=CARTESIAN_POINT('Ctrl Pts',(2.31515194627134,2.27722639648772,16.055606371573));
#59857=CARTESIAN_POINT('Ctrl Pts',(-0.642464915337856,3.18322177310445,
16.2136170094265));
#59858=CARTESIAN_POINT('Ctrl Pts',(-3.01716246646213,1.20101719872665,16.37162764728));
#59859=CARTESIAN_POINT('Ctrl Pts',(-2.6543105577297,-1.87091968165842,16.5296382851335));
#59860=CARTESIAN_POINT('Ctrl Pts',(0.116844287317486,-3.24528662590135,
16.687648922987));
#59861=CARTESIAN_POINT('Ctrl Pts',(2.78201184876604,-1.67520775188644,16.8456595608405));
#59862=CARTESIAN_POINT('Ctrl Pts',(2.92294136003334,1.41497554103137,17.003670198694));
#59863=CARTESIAN_POINT('Ctrl Pts',(0.411921223427336,3.22103318678147,17.1616808365475));
#59864=CARTESIAN_POINT('Ctrl Pts',(-2.47304145874873,2.10511760651132,17.319691474401));
#59865=CARTESIAN_POINT('Ctrl Pts',(-3.11378009385118,-0.921861760455288,
17.4777021122545));
#59866=CARTESIAN_POINT('Ctrl Pts',(-0.930032315648715,-3.11042075736007,
17.635712750108));
#59867=CARTESIAN_POINT('Ctrl Pts',(2.09893395024961,-2.48067020656593,17.7937233879615));
#59868=CARTESIAN_POINT('Ctrl Pts',(3.22080286940782,0.407550226167737,17.951734025815));
#59869=CARTESIAN_POINT('Ctrl Pts',(2.02430085661319,2.07476372580941,18.0570744510506));
#59870=CARTESIAN_POINT('Ctrl Pts',(1.20564430054378,2.47375567929496,18.1097446636685));
#59871=CARTESIAN_POINT('Ctrl Pts',(1.48738611075532,-2.0858265952159,-0.109744663668466));
#59872=CARTESIAN_POINT('Ctrl Pts',(2.17766269356001,-1.59359593510339,-0.0570744510506341));
#59873=CARTESIAN_POINT('Ctrl Pts',(3.01981187546589,0.121143481932978,0.0482659741850286));
#59874=CARTESIAN_POINT('Ctrl Pts',(1.54560206430001,2.60038888638766,0.206276612038524));
#59875=CARTESIAN_POINT('Ctrl Pts',(-1.33225013076688,2.71275818480752,0.364287249892018));
#59876=CARTESIAN_POINT('Ctrl Pts',(-3.00064683006534,0.36752346634399,0.522297887745513));
#59877=CARTESIAN_POINT('Ctrl Pts',(-1.94684010177802,-2.31311490536349,
0.680308525599008));
#59878=CARTESIAN_POINT('Ctrl Pts',(0.873564970132635,-2.8939961476091,0.838319163452502));
#59879=CARTESIAN_POINT('Ctrl Pts',(2.90126733349974,-0.849618123639522,
0.996329801305998));
#59880=CARTESIAN_POINT('Ctrl Pts',(2.29663306649852,1.96591609221879,1.15434043915949));
#59881=CARTESIAN_POINT('Ctrl Pts',(-0.3918163861367,2.99758338236515,1.31235107701299));
#59882=CARTESIAN_POINT('Ctrl Pts',(-2.72474780500748,1.30954971057102,1.47036171486648));
#59883=CARTESIAN_POINT('Ctrl Pts',(-2.58545942134339,-1.56670878119963,
1.62837235271998));
#59884=CARTESIAN_POINT('Ctrl Pts',(-0.100319729817524,-3.02143504979294,
1.78638299057347));
#59885=CARTESIAN_POINT('Ctrl Pts',(2.47584039000051,-1.73475393028017,1.94439362842697));
#59886=CARTESIAN_POINT('Ctrl Pts',(2.80561395912286,1.12591552390453,2.10240426628046));
#59887=CARTESIAN_POINT('Ctrl Pts',(0.589788151624594,2.96501262514568,2.26041490413395));
#59888=CARTESIAN_POINT('Ctrl Pts',(-2.16116588296898,2.11388634893584,2.41842554198745));
#59889=CARTESIAN_POINT('Ctrl Pts',(-2.95124397376509,-0.655219022101695,
2.57643617984094));
#59890=CARTESIAN_POINT('Ctrl Pts',(-1.06358965589061,-2.82982849748694,
2.73444681769444));
#59891=CARTESIAN_POINT('Ctrl Pts',(1.78908426434496,-2.43686895511177,2.89245745554793));
#59892=CARTESIAN_POINT('Ctrl Pts',(3.01848042278497,0.167118611936303,3.05046809340143));
#59893=CARTESIAN_POINT('Ctrl Pts',(1.50913904514892,2.61947551186673,3.20847873125492));
#59894=CARTESIAN_POINT('Ctrl Pts',(-1.36947929848691,2.69512135951845,3.36648936910842));
#59895=CARTESIAN_POINT('Ctrl Pts',(-3.00553721120534,0.325420867793348,
3.52450000696191));
#59896=CARTESIAN_POINT('Ctrl Pts',(-1.91460127455499,-2.33954154064343,
3.68251064481541));
#59897=CARTESIAN_POINT('Ctrl Pts',(0.913496948620389,-2.88178347497167,
3.8405212826689));
#59898=CARTESIAN_POINT('Ctrl Pts',(2.91275813454249,-0.809316203635805,
3.9985319205224));
#59899=CARTESIAN_POINT('Ctrl Pts',(2.26920608762133,1.99746249001107,4.15654255837589));
#59900=CARTESIAN_POINT('Ctrl Pts',(-0.433249444766719,2.99189698806592,
4.31455319622939));
#59901=CARTESIAN_POINT('Ctrl Pts',(-2.7426076746749,1.27171372987236,4.47256383408288));
#59902=CARTESIAN_POINT('Ctrl Pts',(-2.56353414341794,-1.60232498683304,
4.63057447193638));
#59903=CARTESIAN_POINT('Ctrl Pts',(-0.0585064328286764,-3.02253695848627,
4.78858510978987));
#59904=CARTESIAN_POINT('Ctrl Pts',(2.49960552566482,-1.70033081606459,4.94659574764337));
#59905=CARTESIAN_POINT('Ctrl Pts',(2.78976722724991,1.16462504084395,5.10460638549686));
#59906=CARTESIAN_POINT('Ctrl Pts',(0.548708208296067,2.97288949847998,5.26261702335036));
#59907=CARTESIAN_POINT('Ctrl Pts',(-2.19020653596968,2.08378213779743,5.42062766120385));
#59908=CARTESIAN_POINT('Ctrl Pts',(-2.9418959261048,-0.69598924415404,5.57863829905735));
#59909=CARTESIAN_POINT('Ctrl Pts',(-1.02433468733615,-2.84427338987187,
5.73664893691084));
#59910=CARTESIAN_POINT('Ctrl Pts',(1.82262924855683,-2.41188210539321,5.89465957476434));
#59911=CARTESIAN_POINT('Ctrl Pts',(3.01587925636697,0.20886593553466,6.05267021261782));
#59912=CARTESIAN_POINT('Ctrl Pts',(1.4727518382037,2.6401050530385,6.21068085047133));
#59913=CARTESIAN_POINT('Ctrl Pts',(-1.40663759231093,2.67591542316066,6.36869148832481));
#59914=CARTESIAN_POINT('Ctrl Pts',(-3.009752004189,0.283805463815948,6.52670212617831));
#59915=CARTESIAN_POINT('Ctrl Pts',(-1.88204838857008,-2.36580779673504,
6.68471276403181));
#59916=CARTESIAN_POINT('Ctrl Pts',(0.953281523493066,-2.8688685931876,6.8427234018853));
#59917=CARTESIAN_POINT('Ctrl Pts',(2.92367692732715,-0.76893815916913,7.0007340397388));
#59918=CARTESIAN_POINT('Ctrl Pts',(2.24135222378701,2.02866775913074,7.15874467759229));
#59919=CARTESIAN_POINT('Ctrl Pts',(-0.474603506551743,2.98561621438193,
7.31675531544579));
#59920=CARTESIAN_POINT('Ctrl Pts',(-2.7599404318192,1.23364560584519,7.47476595329927));
#59921=CARTESIAN_POINT('Ctrl Pts',(-2.54111918208094,-1.63764036664702,
7.63277659115279));
#59922=CARTESIAN_POINT('Ctrl Pts',(-0.0166813689890152,-3.02305712813042,
7.79078722900626));
#59923=CARTESIAN_POINT('Ctrl Pts',(2.5228918383464,-1.66558381356707,7.94879786685977));
#59924=CARTESIAN_POINT('Ctrl Pts',(2.77338657543163,1.20311245161337,8.10680850471326));
#59925=CARTESIAN_POINT('Ctrl Pts',(0.507523138532463,2.98019679415063,8.26481914256676));
#59926=CARTESIAN_POINT('Ctrl Pts',(-2.21882785154296,2.05327923898061,8.42282978042025));
#59927=CARTESIAN_POINT('Ctrl Pts',(-2.93198470187773,-0.736626347591836,
8.58084041827374));
#59928=CARTESIAN_POINT('Ctrl Pts',(-0.984883607674447,-2.85817370839241,
8.73885105612724));
#59929=CARTESIAN_POINT('Ctrl Pts',(1.85582530108642,-2.38643355655653,8.89686169398072));
#59930=CARTESIAN_POINT('Ctrl Pts',(3.01270073086355,0.250573291205824,9.05487233183424));
#59931=CARTESIAN_POINT('Ctrl Pts',(1.43608268481777,2.66022916125249,9.2128829696877));
#59932=CARTESIAN_POINT('Ctrl Pts',(-1.44352659745559,2.65619721226602,9.37089360754124));
#59933=CARTESIAN_POINT('Ctrl Pts',(-3.01339060835223,0.242135725381516,
9.5289042453947));
#59934=CARTESIAN_POINT('Ctrl Pts',(-1.84913520152769,-2.39162113941206,
9.68691488324822));
#59935=CARTESIAN_POINT('Ctrl Pts',(0.992883601278639,-2.8554044936442,9.8449255211017));
#59936=CARTESIAN_POINT('Ctrl Pts',(2.93403600917798,-0.728412908217918,
10.0029361589552));
#59937=CARTESIAN_POINT('Ctrl Pts',(2.21306927369375,2.05948465831726,10.1609467968087));
#59938=CARTESIAN_POINT('Ctrl Pts',(-0.515866709851859,2.9787638720916,10.3189574346622));
#59939=CARTESIAN_POINT('Ctrl Pts',(-2.77674482381607,1.19534131168557,10.4769680725157));
#59940=CARTESIAN_POINT('Ctrl Pts',(-2.51821774689341,-1.67264223528003,
10.6349787103692));
#59941=CARTESIAN_POINT('Ctrl Pts',(0.025146888342429,-3.02299856136555,
10.7929893482227));
#59942=CARTESIAN_POINT('Ctrl Pts',(2.54569516664075,-1.63051795039287,10.9509999860762));
#59943=CARTESIAN_POINT('Ctrl Pts',(2.75647498431545,1.24136953758929,11.1090106239297));
#59944=CARTESIAN_POINT('Ctrl Pts',(0.466240908142281,2.98693355861595,11.2670212617832));
#59945=CARTESIAN_POINT('Ctrl Pts',(-2.24702439297549,2.02238325877779,11.4250318996367));
#59946=CARTESIAN_POINT('Ctrl Pts',(-2.92151217620389,-0.777122430704416,
11.5830425374901));
#59947=CARTESIAN_POINT('Ctrl Pts',(-0.945243981123939,-2.87152685590094,
11.7410531753436));
#59948=CARTESIAN_POINT('Ctrl Pts',(1.88866607296754,-2.36052814701141,11.8990638131971));
#59949=CARTESIAN_POINT('Ctrl Pts',(3.00894545157365,0.292232676929939,12.0570744510506));
#59950=CARTESIAN_POINT('Ctrl Pts',(1.39913860663847,2.67984399311315,12.2150850889041));
#59951=CARTESIAN_POINT('Ctrl Pts',(-1.48013925273846,2.63597049689789,12.3730957267576));
#59952=CARTESIAN_POINT('Ctrl Pts',(-3.01645232665815,0.20041963229373,12.5311063646111));
#59953=CARTESIAN_POINT('Ctrl Pts',(-1.81586801459506,-2.41697662826485,
12.6891170024646));
#59954=CARTESIAN_POINT('Ctrl Pts',(1.03229560065101,-2.84139375323108,12.8471276403181));
#59955=CARTESIAN_POINT('Ctrl Pts',(2.94383339687692,-0.687748209325603,
13.0051382781716));
#59956=CARTESIAN_POINT('Ctrl Pts',(2.18436265188878,2.08990728814137,13.1631489160251));
#59957=CARTESIAN_POINT('Ctrl Pts',(-0.557031155230083,2.97134127292723,
13.3211595538786));
#59958=CARTESIAN_POINT('Ctrl Pts',(-2.79301763360067,1.15680818042351,13.4791701917321));
#59959=CARTESIAN_POINT('Ctrl Pts',(-2.49483422214693,-1.70732389192444,
13.6371808295856));
#59960=CARTESIAN_POINT('Ctrl Pts',(0.0669703315680426,-3.02236126948423,
13.7951914674391));
#59961=CARTESIAN_POINT('Ctrl Pts',(2.56801114499415,-1.59513993940493,13.9532021052926));
#59962=CARTESIAN_POINT('Ctrl Pts',(2.73903569159509,1.27938897446365,14.1112127431461));
#59963=CARTESIAN_POINT('Ctrl Pts',(0.424869419989396,2.99309850284224,14.2692233809996));
#59964=CARTESIAN_POINT('Ctrl Pts',(-2.27479076184412,1.99110011068065,14.427234018853));
#59965=CARTESIAN_POINT('Ctrl Pts',(-2.91048035482084,-0.817469738484123,
14.5852446567066));
#59966=CARTESIAN_POINT('Ctrl Pts',(-0.905423394666194,-2.88433028065578,
14.74325529456));
#59967=CARTESIAN_POINT('Ctrl Pts',(1.92114527396783,-2.33417082733325,14.9012659324135));
#59968=CARTESIAN_POINT('Ctrl Pts',(3.00461414346351,0.333836100640218,15.059276570267));
#59969=CARTESIAN_POINT('Ctrl Pts',(1.36192666470986,2.69894582555237,15.2172872081205));
#59970=CARTESIAN_POINT('Ctrl Pts',(-1.51646852692866,2.61523908814117,15.375297845974));
#59971=CARTESIAN_POINT('Ctrl Pts',(-3.01893661512828,0.158665287465281,
15.5333084838275));
#59972=CARTESIAN_POINT('Ctrl Pts',(-1.78225311595362,-2.44186963218761,
15.691319121681));
#59973=CARTESIAN_POINT('Ctrl Pts',(1.07150982278044,-2.82683862835414,15.8493297595345));
#59974=CARTESIAN_POINT('Ctrl Pts',(2.95306750846284,-0.646952660598369,
16.007340397388));
#59975=CARTESIAN_POINT('Ctrl Pts',(2.15523729316758,2.11993137754977,16.1653510352415));
#59976=CARTESIAN_POINT('Ctrl Pts',(-0.598087891085528,2.96334687184014,
16.323361673095));
#59977=CARTESIAN_POINT('Ctrl Pts',(-2.8087577913569,1.11805925334627,16.4813723109485));
#59978=CARTESIAN_POINT('Ctrl Pts',(-2.47096917801914,-1.74168951499088,
16.639382948802));
#59979=CARTESIAN_POINT('Ctrl Pts',(0.108773493647311,-3.02112471469761,
16.7973935866555));
#59980=CARTESIAN_POINT('Ctrl Pts',(2.58984974880435,-1.55949600909948,16.955404224509));
#59981=CARTESIAN_POINT('Ctrl Pts',(2.72104482603472,1.3172388360351,17.1134148623625));
#59982=CARTESIAN_POINT('Ctrl Pts',(0.383468559809897,2.9985465350827,17.271425500216));
#59983=CARTESIAN_POINT('Ctrl Pts',(-2.30222089225249,1.95971067011992,17.4294361380694));
#59984=CARTESIAN_POINT('Ctrl Pts',(-2.89870174257858,-0.858185938282932,
17.5874467759229));
#59985=CARTESIAN_POINT('Ctrl Pts',(-0.86579212814317,-2.89557444577305,
17.7454574137764));
#59986=CARTESIAN_POINT('Ctrl Pts',(1.95395413798184,-2.30932269903549,17.9034680516299));
#59987=CARTESIAN_POINT('Ctrl Pts',(2.99833212643718,0.37939948075128,18.0614786894834));
#59988=CARTESIAN_POINT('Ctrl Pts',(1.88447618126766,1.93145342515318,18.1668191147191));
#59989=CARTESIAN_POINT('Ctrl Pts',(1.12236674703438,2.30288577939273,18.2194893273369));
#59990=CARTESIAN_POINT('Ctrl Pts',(1.37702479013102,-1.93106208855765,-4.44089209850063E-15));
#59991=CARTESIAN_POINT('Ctrl Pts',(2.01608411688934,-1.47535404036748,0.0526702126178271));
#59992=CARTESIAN_POINT('Ctrl Pts',(2.79574737452458,0.112154857826279,0.15801063785349));
#59993=CARTESIAN_POINT('Ctrl Pts',(1.43092122672701,2.40744480175264,0.316021275706985));
#59994=CARTESIAN_POINT('Ctrl Pts',(-1.23339961524159,2.5114765043851,0.47403191356048));
#59995=CARTESIAN_POINT('Ctrl Pts',(-2.77800434033211,0.340253899408475,
0.632042551413975));
#59996=CARTESIAN_POINT('Ctrl Pts',(-1.80238813794495,-2.14148602308083,
0.790053189267469));
#59997=CARTESIAN_POINT('Ctrl Pts',(0.80874805201177,-2.67926694285025,0.948063827120964));
#59998=CARTESIAN_POINT('Ctrl Pts',(2.68599862008771,-0.786578017594937,
1.10607446497446));
#59999=CARTESIAN_POINT('Ctrl Pts',(2.12622710642163,1.82004872489232,1.26408510282796));
#60000=CARTESIAN_POINT('Ctrl Pts',(-0.362744329120993,2.775168194831,1.42209574068145));
#60001=CARTESIAN_POINT('Ctrl Pts',(-2.52257651676268,1.21238352457748,1.58010637853494));
#60002=CARTESIAN_POINT('Ctrl Pts',(-2.39362307562467,-1.45046186395561,
1.73811701638844));
#60003=CARTESIAN_POINT('Ctrl Pts',(-0.0928761899139844,-2.79725011229448,
1.89612765424193));
#60004=CARTESIAN_POINT('Ctrl Pts',(2.29213757529781,-1.60603837127393,2.05413829209543));
#60005=CARTESIAN_POINT('Ctrl Pts',(2.59744255060163,1.04237465766208,2.21214892994892));
#60006=CARTESIAN_POINT('Ctrl Pts',(0.546026952813309,2.74501412804214,2.37015956780242));
#60007=CARTESIAN_POINT('Ctrl Pts',(-2.00081133937873,1.95703986003066,2.52817020565591));
#60008=CARTESIAN_POINT('Ctrl Pts',(-2.73226708533368,-0.606602972742087,
2.68618084350941));
#60009=CARTESIAN_POINT('Ctrl Pts',(-0.984673254710223,-2.61986041464368,
2.8441914813629));
#60010=CARTESIAN_POINT('Ctrl Pts',(1.65633749422688,-2.25605774937986,3.0022021192164));
#60011=CARTESIAN_POINT('Ctrl Pts',(2.79451471318987,0.154718717530414,3.16021275706989));
#60012=CARTESIAN_POINT('Ctrl Pts',(1.39716369670102,2.42511523463794,3.31822339492339));
#60013=CARTESIAN_POINT('Ctrl Pts',(-1.2678664470183,2.49514829917553,3.47623403277688));
#60014=CARTESIAN_POINT('Ctrl Pts',(-2.78253186416353,0.301275236427873,
3.63424467063038));
#60015=CARTESIAN_POINT('Ctrl Pts',(-1.77254137255575,-2.16595185050593,
3.79225530848387));
#60016=CARTESIAN_POINT('Ctrl Pts',(0.845717150955885,-2.66796042811686,
3.95026594633737));
#60017=CARTESIAN_POINT('Ctrl Pts',(2.69663682477438,-0.749266426116641,
4.10827658419086));
#60018=CARTESIAN_POINT('Ctrl Pts',(2.10083515905894,1.84925443784418,4.26628722204435));
#60019=CARTESIAN_POINT('Ctrl Pts',(-0.401103130814736,2.76990372055638,
4.42429785989785));
#60020=CARTESIAN_POINT('Ctrl Pts',(-2.53911121686691,1.17735490423188,4.58230849775134));
#60021=CARTESIAN_POINT('Ctrl Pts',(-2.37332461309666,-1.48343541247336,
4.74031913560484));
#60022=CARTESIAN_POINT('Ctrl Pts',(-0.054165362850041,-2.79827026138436,
4.89832977345834));
#60023=CARTESIAN_POINT('Ctrl Pts',(2.3141393814959,-1.57416938897968,5.05634041131182));
#60024=CARTESIAN_POINT('Ctrl Pts',(2.58277161716087,1.07821199946199,5.21435104916533));
#60025=CARTESIAN_POINT('Ctrl Pts',(0.50799506591352,2.75230655182614,5.37236168701881));
#60026=CARTESIAN_POINT('Ctrl Pts',(-2.02769722920544,1.92916932612881,5.53037232487232));
#60027=CARTESIAN_POINT('Ctrl Pts',(-2.72361264565964,-0.644348119116159,
5.6883829627258));
#60028=CARTESIAN_POINT('Ctrl Pts',(-0.948330932804408,-2.6332335225146,
5.84639360057931));
#60029=CARTESIAN_POINT('Ctrl Pts',(1.68739350215265,-2.23292487806895,6.00440423843279));
#60030=CARTESIAN_POINT('Ctrl Pts',(2.79210654854793,0.193368466308401,6.1624148762863));
#60031=CARTESIAN_POINT('Ctrl Pts',(1.3634763537543,2.4442141017022,6.32042551413978));
#60032=CARTESIAN_POINT('Ctrl Pts',(-1.30226766361206,2.47736740805983,6.47843615199329));
#60033=CARTESIAN_POINT('Ctrl Pts',(-2.78643392724037,0.262747619076987,
6.63644678984677));
#60034=CARTESIAN_POINT('Ctrl Pts',(-1.74240385098862,-2.19026919858423,
6.79445742770028));
#60035=CARTESIAN_POINT('Ctrl Pts',(0.882549783362729,-2.65600380686722,
6.95246806555376));
#60036=CARTESIAN_POINT('Ctrl Pts',(2.70674546316629,-0.711884358470874,
7.11047870340726));
#60037=CARTESIAN_POINT('Ctrl Pts',(2.07504800081977,1.87814433324509,7.26848934126075));
#60038=CARTESIAN_POINT('Ctrl Pts',(-0.439388797084447,2.76408896875688,
7.42649997911426));
#60039=CARTESIAN_POINT('Ctrl Pts',(-2.5551579152302,1.14211136516684,7.58451061696773));
#60040=CARTESIAN_POINT('Ctrl Pts',(-2.35257280076785,-1.51613045589557,
7.74252125482125));
#60041=CARTESIAN_POINT('Ctrl Pts',(-0.0154436420140344,-2.79875183539522,
7.90053189267472));
#60042=CARTESIAN_POINT('Ctrl Pts',(2.33569789249813,-1.54200055031981,8.05854253052824));
#60043=CARTESIAN_POINT('Ctrl Pts',(2.56760637965517,1.11384371496224,8.21655316838172));
#60044=CARTESIAN_POINT('Ctrl Pts',(0.469865852767273,2.75907165956415,8.37456380623522));
#60045=CARTESIAN_POINT('Ctrl Pts',(-2.05419489567252,1.90092968644286,8.53257444408872));
#60046=CARTESIAN_POINT('Ctrl Pts',(-2.71443681608685,-0.681970024032665,
8.69058508194221));
#60047=CARTESIAN_POINT('Ctrl Pts',(-0.911807050875725,-2.64610246290276,
8.8485957197957));
#60048=CARTESIAN_POINT('Ctrl Pts',(1.7181264684868,-2.20936456486744,9.0066063576492));
#60049=CARTESIAN_POINT('Ctrl Pts',(2.78916386380546,0.231981212706065,9.16461699550269));
#60050=CARTESIAN_POINT('Ctrl Pts',(1.32952798427551,2.46284503800688,9.32262763335619));
#60051=CARTESIAN_POINT('Ctrl Pts',(-1.33641957225244,2.45911225223807,9.48063827120967));
#60052=CARTESIAN_POINT('Ctrl Pts',(-2.78980255365015,0.224169698786106,
9.63864890906318));
#60053=CARTESIAN_POINT('Ctrl Pts',(-1.71193276204147,-2.21416723859239,
9.79665954691667));
#60054=CARTESIAN_POINT('Ctrl Pts',(0.919213459631522,-2.64353871880838,
9.95467018477016));
#60055=CARTESIAN_POINT('Ctrl Pts',(2.71633592014881,-0.674366006791661,
10.1126808226237));
#60056=CARTESIAN_POINT('Ctrl Pts',(2.04886359373486,1.90667467504938,10.2706914604772));
#60057=CARTESIAN_POINT('Ctrl Pts',(-0.477590346402141,2.75774505769302,
10.4287020983307));
#60058=CARTESIAN_POINT('Ctrl Pts',(-2.57071545217063,1.10664917935991,10.5867127361841));
#60059=CARTESIAN_POINT('Ctrl Pts',(-2.33137061005572,-1.54853525009127,
10.7447233740376));
#60060=CARTESIAN_POINT('Ctrl Pts',(0.0232810353625256,-2.79869761417686,
10.9027340118911));
#60061=CARTESIAN_POINT('Ctrl Pts',(2.35680925566857,-1.50953650986048,11.0607446497446));
#60062=CARTESIAN_POINT('Ctrl Pts',(2.5519495975734,1.1492621953461,11.2187552875981));
#60063=CARTESIAN_POINT('Ctrl Pts',(0.431646688134689,2.76530856846557,11.3767659254516));
#60064=CARTESIAN_POINT('Ctrl Pts',(-2.0802993054608,1.8723261312886,11.5347765633051));
#60065=CARTESIAN_POINT('Ctrl Pts',(-2.70474133260486,-0.719461372073362,
11.6927872011586));
#60066=CARTESIAN_POINT('Ctrl Pts',(-0.875108611891469,-2.65846483136416,
11.8507978390121));
#60067=CARTESIAN_POINT('Ctrl Pts',(1.7485305153448,-2.18538128918389,12.0088084768656));
#60068=CARTESIAN_POINT('Ctrl Pts',(2.78568721934935,0.270549548438745,12.1668191147191));
#60069=CARTESIAN_POINT('Ctrl Pts',(1.29532508891864,2.48100448532931,12.3248297525726));
#60070=CARTESIAN_POINT('Ctrl Pts',(-1.37031563568376,2.44038632204184,12.4828403904261));
#60071=CARTESIAN_POINT('Ctrl Pts',(-2.79263709807487,0.1855488632721,12.6408510282796));
#60072=CARTESIAN_POINT('Ctrl Pts',(-1.68113393934647,-2.23764139669008,
12.7988616661331));
#60073=CARTESIAN_POINT('Ctrl Pts',(0.955701160956647,-2.63056754962948,
12.9568723039866));
#60074=CARTESIAN_POINT('Ctrl Pts',(2.725406359655,-0.636718553952737,13.1148829418401));
#60075=CARTESIAN_POINT('Ctrl Pts',(2.02228695060197,1.93484000155462,13.2728935796935));
#60076=CARTESIAN_POINT('Ctrl Pts',(-0.515700465454569,2.75087320176898,
13.4309042175471));
#60077=CARTESIAN_POINT('Ctrl Pts',(-2.5857808493237,1.07097513574369,13.5889148554005));
#60078=CARTESIAN_POINT('Ctrl Pts',(-2.30972209994545,-1.58064359144045,
13.746925493254));
#60079=CARTESIAN_POINT('Ctrl Pts',(0.0620012558310767,-2.79810760818394,
13.9049361311075));
#60080=CARTESIAN_POINT('Ctrl Pts',(2.37746942936956,-1.4767834823825,14.062946768961));
#60081=CARTESIAN_POINT('Ctrl Pts',(2.53580426837836,1.18446065975573,14.2209574068145));
#60082=CARTESIAN_POINT('Ctrl Pts',(0.393344888501637,2.77101608514062,14.378968044668));
#60083=CARTESIAN_POINT('Ctrl Pts',(-2.10600546070022,1.84336413538746,14.5369786825215));
#60084=CARTESIAN_POINT('Ctrl Pts',(-2.69452805212919,-0.756814983637939,
14.694989320375));
#60085=CARTESIAN_POINT('Ctrl Pts',(-0.838242639893101,-2.67031826549166,
14.8529999582285));
#60086=CARTESIAN_POINT('Ctrl Pts',(1.77859981921798,-2.16097963427009,15.011010596082));
#60087=CARTESIAN_POINT('Ctrl Pts',(2.78167728635466,0.309066074436347,15.1690212339355));
#60088=CARTESIAN_POINT('Ctrl Pts',(1.26087420481122,2.49868899684622,15.327031871789));
#60089=CARTESIAN_POINT('Ctrl Pts',(-1.40394934437959,2.42119314578055,15.4850425096425));
#60090=CARTESIAN_POINT('Ctrl Pts',(-2.79493705689825,0.146892614226416,
15.643053147496));
#60091=CARTESIAN_POINT('Ctrl Pts',(-1.65001320451353,-2.26068738539107,
15.8010637853495));
#60092=CARTESIAN_POINT('Ctrl Pts',(0.992005759747417,-2.61709238831523,
15.959074423203));
#60093=CARTESIAN_POINT('Ctrl Pts',(2.73395531710238,-0.598949960096589,
16.1170850610565));
#60094=CARTESIAN_POINT('Ctrl Pts',(1.99532264006382,1.96263635861182,16.2750956989099));
#60095=CARTESIAN_POINT('Ctrl Pts',(-0.553710866833194,2.74347197057582,
16.4331063367635));
#60096=CARTESIAN_POINT('Ctrl Pts',(-2.60035311625168,1.03510130796588,16.5911169746169));
#60097=CARTESIAN_POINT('Ctrl Pts',(-2.28762779830857,-1.61245934832335,
16.7491276124704));
#60098=CARTESIAN_POINT('Ctrl Pts',(0.100702699977133,-2.79696280349387,
16.9071382503239));
#60099=CARTESIAN_POINT('Ctrl Pts',(2.39768764884266,-1.44378426631252,17.0651488881774));
#60100=CARTESIAN_POINT('Ctrl Pts',(2.51914829203609,1.21950213103884,17.2231595260309));
#60101=CARTESIAN_POINT('Ctrl Pts',(0.35501589619246,2.77605988338393,17.3811701638844));
#60102=CARTESIAN_POINT('Ctrl Pts',(-2.13140032575625,1.81430373372853,17.5391808017379));
#60103=CARTESIAN_POINT('Ctrl Pts',(-2.68362339130599,-0.79451011611058,
17.6971914395914));
#60104=CARTESIAN_POINT('Ctrl Pts',(-0.801551940637627,-2.68072813418604,
17.8552020774449));
#60105=CARTESIAN_POINT('Ctrl Pts',(1.80897432571407,-2.13797519150506,18.0132127152984));
#60106=CARTESIAN_POINT('Ctrl Pts',(2.77586138346654,0.351248735334821,18.1712233531519));
#60107=CARTESIAN_POINT('Ctrl Pts',(1.74465150592214,1.78814312449695,18.2765637783876));
#60108=CARTESIAN_POINT('Ctrl Pts',(1.03908919352497,2.13201587949049,18.3292339910054));
#60109=CARTESIAN_POINT('',(1.28892185405319,2.64462557919719,18.));
#60110=CARTESIAN_POINT('Ctrl Pts',(1.37994918219943,-1.93347698736447,18.));
#60111=CARTESIAN_POINT('Ctrl Pts',(1.43821237480841,-1.90182406103466,18.));
#60112=CARTESIAN_POINT('Ctrl Pts',(1.49490500816213,-1.86766989359623,18.));
#60113=CARTESIAN_POINT('Ctrl Pts',(1.54984605587159,-1.83106249366945,18.));
#60114=CARTESIAN_POINT('Ctrl Pts',(1.61731929964478,-1.78610485048391,18.));
#60115=CARTESIAN_POINT('Ctrl Pts',(1.68215209723072,-1.73744909575843,18.));
#60116=CARTESIAN_POINT('Ctrl Pts',(1.74427143803024,-1.68546230453832,18.));
#60117=CARTESIAN_POINT('Ctrl Pts',(1.80797414842667,-1.63215041386288,18.));
#60118=CARTESIAN_POINT('Ctrl Pts',(1.86882386541983,-1.57533510126562,18.));
#60119=CARTESIAN_POINT('Ctrl Pts',(1.92672152516503,-1.51536150307498,18.));
#60120=CARTESIAN_POINT('Ctrl Pts',(1.95606151098823,-1.48496952301181,18.));
#60121=CARTESIAN_POINT('Ctrl Pts',(1.98464303190203,-1.45376573183374,18.));
#60122=CARTESIAN_POINT('Ctrl Pts',(2.01245056612922,-1.42179081892014,18.));
#60123=CARTESIAN_POINT('Ctrl Pts',(2.02687703313248,-1.40520232810643,18.));
#60124=CARTESIAN_POINT('Ctrl Pts',(2.04109514957463,-1.38840624663065,18.));
#60125=CARTESIAN_POINT('Ctrl Pts',(2.05510252968955,-1.37140799562356,18.));
#60126=CARTESIAN_POINT('Ctrl Pts',(2.06569873728338,-1.35854927436908,18.));
#60127=CARTESIAN_POINT('Ctrl Pts',(2.07617434762788,-1.34557485760829,18.));
#60128=CARTESIAN_POINT('Ctrl Pts',(2.08652826676332,-1.33248703035156,18.));
#60129=CARTESIAN_POINT('Ctrl Pts',(2.094783223847,-1.32205238711072,18.));
#60130=CARTESIAN_POINT('Ctrl Pts',(2.10295512158607,-1.31155284675917,18.));
#60131=CARTESIAN_POINT('Ctrl Pts',(2.11104243361189,-1.30099155085768,18.));
#60132=CARTESIAN_POINT('Ctrl Pts',(2.16374871732536,-1.23216192534195,18.));
#60133=CARTESIAN_POINT('Ctrl Pts',(2.21288175146922,-1.16069122843785,18.));
#60134=CARTESIAN_POINT('Ctrl Pts',(2.25835597691573,-1.08697798281416,18.));
#60135=CARTESIAN_POINT('Ctrl Pts',(2.30474705699815,-1.01177852537899,18.));
#60136=CARTESIAN_POINT('Ctrl Pts',(2.34733092606907,-0.934244553946303,
18.));
#60137=CARTESIAN_POINT('Ctrl Pts',(2.38598791054104,-0.854752429497406,
18.));
#60138=CARTESIAN_POINT('Ctrl Pts',(2.42492705239859,-0.77468009191716,18.));
#60139=CARTESIAN_POINT('Ctrl Pts',(2.459882395318,-0.692620112126303,18.));
#60140=CARTESIAN_POINT('Ctrl Pts',(2.4906933080418,-0.608921153989719,18.));
#60141=CARTESIAN_POINT('Ctrl Pts',(2.50574535552365,-0.568031722918762,
18.));
#60142=CARTESIAN_POINT('Ctrl Pts',(2.51980765168383,-0.526750663351143,
18.));
#60143=CARTESIAN_POINT('Ctrl Pts',(2.53285748335047,-0.485116441218252,
18.));
#60144=CARTESIAN_POINT('Ctrl Pts',(2.53785250263207,-0.46918031670412,18.));
#60145=CARTESIAN_POINT('Ctrl Pts',(2.54269975128169,-0.453190051907574,
18.));
#60146=CARTESIAN_POINT('Ctrl Pts',(2.54739155306582,-0.437170317508783,
18.));
#60147=CARTESIAN_POINT('Ctrl Pts',(2.57317453750917,-0.349136640513436,
18.));
#60148=CARTESIAN_POINT('Ctrl Pts',(2.59431215770916,-0.260074846372698,
18.));
#60149=CARTESIAN_POINT('Ctrl Pts',(2.61068742566702,-0.170385934282095,
18.));
#60150=CARTESIAN_POINT('Ctrl Pts',(2.62702434602131,-0.08090705569159,18.));
#60151=CARTESIAN_POINT('Ctrl Pts',(2.63862173311556,0.00919691345965296,
18.));
#60152=CARTESIAN_POINT('Ctrl Pts',(2.64532217576655,0.0995580551948545,
18.));
#60153=CARTESIAN_POINT('Ctrl Pts',(2.65107284244143,0.177110663813041,18.));
#60154=CARTESIAN_POINT('Ctrl Pts',(2.65321597987867,0.254853522028482,18.));
#60155=CARTESIAN_POINT('Ctrl Pts',(2.65162313398611,0.332564201440169,18.));
#60156=CARTESIAN_POINT('Ctrl Pts',(2.65043785503477,0.390390782800784,18.));
#60157=CARTESIAN_POINT('Ctrl Pts',(2.64718329974002,0.448199763632709,18.));
#60158=CARTESIAN_POINT('Ctrl Pts',(2.64191416774207,0.505920012373682,18.));
#60159=CARTESIAN_POINT('Ctrl Pts',(2.64062763401441,0.520013234331792,18.));
#60160=CARTESIAN_POINT('Ctrl Pts',(2.63922066290764,0.534103822243259,18.));
#60161=CARTESIAN_POINT('Ctrl Pts',(2.63769493345068,0.548181951403584,18.));
#60162=CARTESIAN_POINT('Ctrl Pts',(2.62812387695765,0.636495491458,18.));
#60163=CARTESIAN_POINT('Ctrl Pts',(2.6139065437193,0.724124252500042,18.));
#60164=CARTESIAN_POINT('Ctrl Pts',(2.59532997065339,0.810806020554952,18.));
#60165=CARTESIAN_POINT('Ctrl Pts',(2.5752815789767,0.904355569819364,18.));
#60166=CARTESIAN_POINT('Ctrl Pts',(2.55015626103555,0.996802800692518,18.));
#60167=CARTESIAN_POINT('Ctrl Pts',(2.52025097354548,1.08782980267173,18.));
#60168=CARTESIAN_POINT('Ctrl Pts',(2.49271715414392,1.17163842795221,18.));
#60169=CARTESIAN_POINT('Ctrl Pts',(2.46113046092889,1.25424383150991,18.));
#60170=CARTESIAN_POINT('Ctrl Pts',(2.42567706973452,1.3353970388071,18.));
#60171=CARTESIAN_POINT('Ctrl Pts',(2.40983754709368,1.37165388254068,18.));
#60172=CARTESIAN_POINT('Ctrl Pts',(2.39322565968621,1.40762079193962,18.));
#60173=CARTESIAN_POINT('Ctrl Pts',(2.3758554027599,1.44327498917763,18.));
#60174=CARTESIAN_POINT('Ctrl Pts',(2.36243191962062,1.47082803675195,18.));
#60175=CARTESIAN_POINT('Ctrl Pts',(2.34855550772026,1.49819432663718,18.));
#60176=CARTESIAN_POINT('Ctrl Pts',(2.3342320039039,1.52536310987849,18.));
#60177=CARTESIAN_POINT('Ctrl Pts',(2.32544284172995,1.54203436888314,18.));
#60178=CARTESIAN_POINT('Ctrl Pts',(2.31648412915412,1.55863319919544,18.));
#60179=CARTESIAN_POINT('Ctrl Pts',(2.30736886637286,1.57513647613047,18.));
#60180=CARTESIAN_POINT('Ctrl Pts',(2.26079517697126,1.65945861938906,18.));
#60181=CARTESIAN_POINT('Ctrl Pts',(2.2100781528945,1.74140468208013,18.));
#60182=CARTESIAN_POINT('Ctrl Pts',(2.15547782018911,1.82066912257117,18.));
#60183=CARTESIAN_POINT('Ctrl Pts',(2.09852307134651,1.90335151801874,18.));
#60184=CARTESIAN_POINT('Ctrl Pts',(2.03734284105072,1.98311713055562,18.));
#60185=CARTESIAN_POINT('Ctrl Pts',(1.97217502405287,2.05960411713276,18.));
#60186=CARTESIAN_POINT('Ctrl Pts',(1.9509987109036,2.08445859982404,18.));
#60187=CARTESIAN_POINT('Ctrl Pts',(1.92940090651591,2.10896669670022,18.));
#60188=CARTESIAN_POINT('Ctrl Pts',(1.90738857169095,2.13311535773337,18.));
#60189=CARTESIAN_POINT('Ctrl Pts',(1.89181486376242,2.15020051461408,18.));
#60190=CARTESIAN_POINT('Ctrl Pts',(1.87603066798751,2.16710868538781,18.));
#60191=CARTESIAN_POINT('Ctrl Pts',(1.86005797891342,2.18381506371099,18.));
#60192=CARTESIAN_POINT('Ctrl Pts',(1.79161585954772,2.25540100231282,18.));
#60193=CARTESIAN_POINT('Ctrl Pts',(1.71965505267813,2.32335372378486,18.));
#60194=CARTESIAN_POINT('Ctrl Pts',(1.6444167588703,2.38734627880606,18.));
#60195=CARTESIAN_POINT('Ctrl Pts',(1.57011188953763,2.45054492670815,18.));
#60196=CARTESIAN_POINT('Ctrl Pts',(1.49260984581683,2.50988188571361,18.));
#60197=CARTESIAN_POINT('Ctrl Pts',(1.41210003131952,2.5650162920718,18.));
#60198=CARTESIAN_POINT('Ctrl Pts',(1.3717885747323,2.59262222114079,18.));
#60199=CARTESIAN_POINT('Ctrl Pts',(1.33072243200449,2.61917407343912,18.));
#60200=CARTESIAN_POINT('Ctrl Pts',(1.28892185405319,2.64462557919719,18.));
#60201=CARTESIAN_POINT('Ctrl Pts',(1.29200466145509,2.64817921559509,-6.24500451351651E-17));
#60202=CARTESIAN_POINT('Ctrl Pts',(1.36163579271623,2.60626235479205,-6.87923715339042E-17));
#60203=CARTESIAN_POINT('Ctrl Pts',(1.42923480273934,2.56138620404723,-2.42496828474002E-16));
#60204=CARTESIAN_POINT('Ctrl Pts',(1.49459025051858,2.51355282242146,-2.30718222304915E-16));
#60205=CARTESIAN_POINT('Ctrl Pts',(1.57240550431648,2.4566001603604,-2.24944840579866E-16));
#60206=CARTESIAN_POINT('Ctrl Pts',(1.6470415083937,2.3954556864035,-4.65838301304871E-16));
#60207=CARTESIAN_POINT('Ctrl Pts',(1.71834920131344,2.33049816358297,-4.78783679369599E-16));
#60208=CARTESIAN_POINT('Ctrl Pts',(1.79066277758345,2.26462433442851,-4.91911668029694E-16));
#60209=CARTESIAN_POINT('Ctrl Pts',(1.85955394539379,2.19482820959758,-1.96384928419704E-16));
#60210=CARTESIAN_POINT('Ctrl Pts',(1.92482290460833,2.12147584187517,-1.31838984174237E-16));
#60211=CARTESIAN_POINT('Ctrl Pts',(1.98558343594445,2.0531902603183,-7.17515258304525E-17));
#60212=CARTESIAN_POINT('Ctrl Pts',(2.0432046872693,1.98182185580739,-1.54434603693546E-16));
#60213=CARTESIAN_POINT('Ctrl Pts',(2.09748648009497,1.9076544835139,-1.2490009027033E-16));
#60214=CARTESIAN_POINT('Ctrl Pts',(2.10646567520803,1.89538585213349,-1.20014544955935E-16));
#60215=CARTESIAN_POINT('Ctrl Pts',(2.11535391066683,1.88303977945376,3.07879830521503E-17));
#60216=CARTESIAN_POINT('Ctrl Pts',(2.12414058888115,1.87063145433286,2.77555756156289E-17));
#60217=CARTESIAN_POINT('Ctrl Pts',(2.17962767318294,1.79227399486589,8.60619481851236E-18));
#60218=CARTESIAN_POINT('Ctrl Pts',(2.23116246589918,1.7113097095221,-9.20636394827646E-17));
#60219=CARTESIAN_POINT('Ctrl Pts',(2.27859496939366,1.62810410227917,-1.66533453693773E-16));
#60220=CARTESIAN_POINT('Ctrl Pts',(2.32587821025047,1.54516033001208,-2.40768923097373E-16));
#60221=CARTESIAN_POINT('Ctrl Pts',(2.36908523109373,1.45998835263573,-3.28642479298764E-16));
#60222=CARTESIAN_POINT('Ctrl Pts',(2.40801906757308,1.37293284166191,-3.05311331771918E-16));
#60223=CARTESIAN_POINT('Ctrl Pts',(2.44628350384463,1.28737410014124,-2.82381323110772E-16));
#60224=CARTESIAN_POINT('Ctrl Pts',(2.48042058153336,1.19999515723855,-3.78426003229508E-16));
#60225=CARTESIAN_POINT('Ctrl Pts',(2.5101934511382,1.11112005268495,-4.44089209850063E-16));
#60226=CARTESIAN_POINT('Ctrl Pts',(2.52374026722379,1.07068140125652,-4.73966322653916E-16));
#60227=CARTESIAN_POINT('Ctrl Pts',(2.53638285871564,1.02993303554646,-5.32472828915682E-16));
#60228=CARTESIAN_POINT('Ctrl Pts',(2.54809527872308,0.988905993523423,-5.68989300120393E-16));
#60229=CARTESIAN_POINT('Ctrl Pts',(2.55316374923826,0.971151818665729,-5.84791555973746E-16));
#60230=CARTESIAN_POINT('Ctrl Pts',(2.55805799988541,0.953345463647252,-1.91210667779528E-16));
#60231=CARTESIAN_POINT('Ctrl Pts',(2.56277579019384,0.935489479213339,-1.94289029309402E-16));
#60232=CARTESIAN_POINT('Ctrl Pts',(2.56650136447238,0.921388853289753,-1.96719969174464E-16));
#60233=CARTESIAN_POINT('Ctrl Pts',(2.57011697351366,0.907256657441779,-7.89089153153375E-16));
#60234=CARTESIAN_POINT('Ctrl Pts',(2.57361787574017,0.893109630455151,-7.91033905045424E-16));
#60235=CARTESIAN_POINT('Ctrl Pts',(2.59566788235011,0.804006302688932,-8.03282688159008E-16));
#60236=CARTESIAN_POINT('Ctrl Pts',(2.61321131606813,0.714168582471938,-3.64080492391637E-16));
#60237=CARTESIAN_POINT('Ctrl Pts',(2.62607387329613,0.623910106232047,-3.88578058618805E-16));
#60238=CARTESIAN_POINT('Ctrl Pts',(2.63856685923259,0.536244966685939,-4.1237175258874E-16));
#60239=CARTESIAN_POINT('Ctrl Pts',(2.64664407470688,0.448182150112304,-7.31559005160491E-16));
#60240=CARTESIAN_POINT('Ctrl Pts',(2.65009784347288,0.360011822186139,-7.21644966006352E-16));
#60241=CARTESIAN_POINT('Ctrl Pts',(2.65337342956238,0.276390271575919,-7.12242400014153E-16));
#60242=CARTESIAN_POINT('Ctrl Pts',(2.65249011193531,0.192671525761824,-5.49469972717259E-16));
#60243=CARTESIAN_POINT('Ctrl Pts',(2.64722883229478,0.109114351042944,-5.55111512312578E-16));
#60244=CARTESIAN_POINT('Ctrl Pts',(2.64396837891794,0.0573333602792648,
-5.59772983305919E-16));
#60245=CARTESIAN_POINT('Ctrl Pts',(2.63902562983071,0.00561466852570915,
-5.84771322736047E-16));
#60246=CARTESIAN_POINT('Ctrl Pts',(2.63242939092862,-0.0459762644840405,
-6.38378239159465E-16));
#60247=CARTESIAN_POINT('Ctrl Pts',(2.63040459618663,-0.0618127209015484,
-6.54833525894753E-16));
#60248=CARTESIAN_POINT('Ctrl Pts',(2.62822397035665,-0.0776371160914911,
8.07626614741256E-17));
#60249=CARTESIAN_POINT('Ctrl Pts',(2.62588826970276,-0.0934474919564786,
8.32667268468867E-17));
#60250=CARTESIAN_POINT('Ctrl Pts',(2.62391430098318,-0.10680930154901,8.53829854990407E-17));
#60251=CARTESIAN_POINT('Ctrl Pts',(2.62182970872418,-0.120159705897083,
-4.668564614999E-16));
#60252=CARTESIAN_POINT('Ctrl Pts',(2.61963718019352,-0.133485486331073,
-4.71844785465692E-16));
#60253=CARTESIAN_POINT('Ctrl Pts',(2.60533107299951,-0.220435343843426,
-5.04393277480817E-16));
#60254=CARTESIAN_POINT('Ctrl Pts',(2.58641348004362,-0.30647879548521,-5.84701050508147E-16));
#60255=CARTESIAN_POINT('Ctrl Pts',(2.56311086331968,-0.391324698838268,
-5.55111512312578E-16));
#60256=CARTESIAN_POINT('Ctrl Pts',(2.5394147018448,-0.477603516799134,-5.25022253095215E-16));
#60257=CARTESIAN_POINT('Ctrl Pts',(2.51118363377731,-0.562644867046194,
-6.60463472264379E-16));
#60258=CARTESIAN_POINT('Ctrl Pts',(2.4786078639959,-0.646119795222761,-7.21644966006352E-16));
#60259=CARTESIAN_POINT('Ctrl Pts',(2.44637828472532,-0.728707615336435,
-7.82176269354827E-16));
#60260=CARTESIAN_POINT('Ctrl Pts',(2.40989517054765,-0.809762845613054,
-5.71017860423719E-16));
#60261=CARTESIAN_POINT('Ctrl Pts',(2.36930556806385,-0.888933046760586,
-5.27355936696949E-16));
#60262=CARTESIAN_POINT('Ctrl Pts',(2.35350849036712,-0.919745317447226,
-5.10363141515569E-16));
#60263=CARTESIAN_POINT('Ctrl Pts',(2.33708906017935,-0.950271642113999,
-7.68273519756434E-16));
#60264=CARTESIAN_POINT('Ctrl Pts',(2.32005473735486,-0.980489483259258,
-7.7715611723761E-16));
#60265=CARTESIAN_POINT('Ctrl Pts',(2.31145085630386,-0.995752239138126,
-7.81642636187581E-16));
#60266=CARTESIAN_POINT('Ctrl Pts',(2.30269009619025,-1.01093627868412,-4.6423720985487E-16));
#60267=CARTESIAN_POINT('Ctrl Pts',(2.2937733628843,-1.02603858919702,-4.71844785465692E-16));
#60268=CARTESIAN_POINT('Ctrl Pts',(2.28696334816895,-1.03757274114479,-4.77654951597187E-16));
#60269=CARTESIAN_POINT('Ctrl Pts',(2.28006336389062,-1.04905742084503,-5.28398787028243E-16));
#60270=CARTESIAN_POINT('Ctrl Pts',(2.27307868687177,-1.06048370824817,-5.27355936696949E-16));
#60271=CARTESIAN_POINT('Ctrl Pts',(2.22741873521752,-1.13517917791805,-5.20538657160472E-16));
#60272=CARTESIAN_POINT('Ctrl Pts',(2.17808663173844,-1.20747732680705,-1.22707103107793E-16));
#60273=CARTESIAN_POINT('Ctrl Pts',(2.12525032891489,-1.27705317933263,-2.22044604925031E-16));
#60274=CARTESIAN_POINT('Ctrl Pts',(2.07473473787799,-1.343573074261,-3.17018937879127E-16));
#60275=CARTESIAN_POINT('Ctrl Pts',(2.02101528324939,-1.40760489508775,-2.95247053471268E-16));
#60276=CARTESIAN_POINT('Ctrl Pts',(1.96421324888463,-1.46882687010891,-2.77555756156289E-16));
#60277=CARTESIAN_POINT('Ctrl Pts',(1.94502782179757,-1.4895051741702,-2.71580352308384E-16));
#60278=CARTESIAN_POINT('Ctrl Pts',(1.92549055386547,-1.5098625760957,9.78135150092519E-17));
#60279=CARTESIAN_POINT('Ctrl Pts',(1.90560563251692,-1.52988554447117,1.11022302462516E-16));
#60280=CARTESIAN_POINT('Ctrl Pts',(1.89094057784228,-1.54465240830875,1.20763733509313E-16));
#60281=CARTESIAN_POINT('Ctrl Pts',(1.87608371516564,-1.55923977942274,-4.05819302166216E-16));
#60282=CARTESIAN_POINT('Ctrl Pts',(1.86105586686576,-1.57362416245269,-4.44089209850063E-16));
#60283=CARTESIAN_POINT('Ctrl Pts',(1.80044928191378,-1.63163568311025,-5.98429895546516E-16));
#60284=CARTESIAN_POINT('Ctrl Pts',(1.73700660477931,-1.68640875868871,-1.11912723490306E-15));
#60285=CARTESIAN_POINT('Ctrl Pts',(1.67086281709221,-1.73762501202154,-1.99840144432528E-15));
#60286=CARTESIAN_POINT('Ctrl Pts',(1.60658766700043,-1.78739434766466,-2.85283515244317E-15));
#60287=CARTESIAN_POINT('Ctrl Pts',(1.53976127787681,-1.83380531528516,-3.83545286917222E-15));
#60288=CARTESIAN_POINT('Ctrl Pts',(1.47049014543338,-1.87652000934262,-4.38538094726937E-15));
#60289=CARTESIAN_POINT('Ctrl Pts',(1.43981185670265,-1.89543717831499,-4.62892904249903E-15));
#60290=CARTESIAN_POINT('Ctrl Pts',(1.40865388521069,-1.91362873361342,-4.4670584227815E-15));
#60291=CARTESIAN_POINT('Ctrl Pts',(1.37702479013102,-1.93106208855765,-4.44089209850063E-15));
#60292=CARTESIAN_POINT('Ctrl Pts',(1.28892185405319,2.64462557919719,18.));
#60293=CARTESIAN_POINT('Ctrl Pts',(2.16412553195871,2.21807402646564,17.9473297873822));
#60294=CARTESIAN_POINT('Ctrl Pts',(2.80369957216858,1.32688749902492,17.8946595747643));
#60295=CARTESIAN_POINT('Ctrl Pts',(2.92359328396334,0.366674454357809,17.8419893621465));
#60296=CARTESIAN_POINT('Ctrl Pts',(3.0434869957581,-0.593538590309304,17.7893191495287));
#60297=CARTESIAN_POINT('Ctrl Pts',(2.64370037913775,-1.62277815220282,17.7366489369109));
#60298=CARTESIAN_POINT('Ctrl Pts',(1.90410935988231,-2.24960615895804,17.683978724293));
#60299=CARTESIAN_POINT('Ctrl Pts',(1.16451834062685,-2.87643416571327,17.6313085116752));
#60300=CARTESIAN_POINT('Ctrl Pts',(0.0851229187362741,-3.10085061733018,
17.5786382990573));
#60301=CARTESIAN_POINT('Ctrl Pts',(-0.843672449203934,-2.82310392875205,
17.5259680864395));
#60302=CARTESIAN_POINT('Ctrl Pts',(-1.77246781714411,-2.54535724017392,
17.4732978738217));
#60303=CARTESIAN_POINT('Ctrl Pts',(-2.55066313113394,-1.76544741140077,
17.4206276612039));
#60304=CARTESIAN_POINT('Ctrl Pts',(-2.82559471814905,-0.836148809425809,
17.367957448586));
#60305=CARTESIAN_POINT('Ctrl Pts',(-2.90525222915565,-0.566897777127469,
17.3526970047539));
#60306=CARTESIAN_POINT('Ctrl Pts',(-2.94266235676508,-0.285106034186959,
17.3374365609218));
#60307=CARTESIAN_POINT('Ctrl Pts',(-2.94033980469539,-0.00268911818531531,
17.3221761170896));
#60308=CARTESIAN_POINT('Origin',(0.,0.,18.));
#60309=CARTESIAN_POINT('Origin',(0.,0.,18.));
#60310=CARTESIAN_POINT('Origin',(0.,0.,0.));
#60311=CARTESIAN_POINT('Origin',(0.,0.,0.));
#63870=UNCERTAINTY_MEASURE_WITH_UNIT(LENGTH_MEASURE(0.01),#63899,
'DISTANCE_ACCURACY_VALUE',
'Maximum model space distance between geometric entities at asserted c
onnectivities');
#63878=UNCERTAINTY_MEASURE_WITH_UNIT(LENGTH_MEASURE(0.01),#63899,
'DISTANCE_ACCURACY_VALUE',
'Maximum model space distance between geometric entities at asserted c
onnectivities');
#63890=(
GEOMETRIC_REPRESENTATION_CONTEXT(3)
GLOBAL_UNCERTAINTY_ASSIGNED_CONTEXT((#63870))
GLOBAL_UNIT_ASSIGNED_CONTEXT((#63899,#63901,#63902))
REPRESENTATION_CONTEXT('','3D')
);
#63898=(
GEOMETRIC_REPRESENTATION_CONTEXT(3)
GLOBAL_UNCERTAINTY_ASSIGNED_CONTEXT((#63878))
GLOBAL_UNIT_ASSIGNED_CONTEXT((#63899,#63901,#63902))
REPRESENTATION_CONTEXT('','3D')
);
#63899=(
LENGTH_UNIT()
NAMED_UNIT(*)
SI_UNIT(.MILLI.,.METRE.)
);
#63901=(
NAMED_UNIT(*)
PLANE_ANGLE_UNIT()
SI_UNIT($,.RADIAN.)
);
#63902=(
NAMED_UNIT(*)
SI_UNIT($,.STERADIAN.)
SOLID_ANGLE_UNIT()
);
#63914=SHAPE_DEFINITION_REPRESENTATION(#63933,#64005);
#63933=PRODUCT_DEFINITION_SHAPE('',$,#64025);
#64005=SHAPE_REPRESENTATION('',(#16531),#63890);
#64013=PRODUCT_DEFINITION_CONTEXT('part definition',#64072,'design');
#64025=PRODUCT_DEFINITION('Set screw M6x18','Set screw M6x18',#64044,#64013);
#64044=PRODUCT_DEFINITION_FORMATION('',$,#64085);
#64072=APPLICATION_CONTEXT(
'Core Data for Automotive Mechanical Design Process');
#64073=PRODUCT_CONTEXT('part definition',#64072,'mechanical');
#64085=PRODUCT('Set screw M6x18','Set screw M6x18',$,(#64073));
#64100=PRESENTATION_STYLE_ASSIGNMENT((#64113));
#64113=SURFACE_STYLE_USAGE(.BOTH.,#64126);
#64126=SURFACE_SIDE_STYLE('',(#64139));
#64139=SURFACE_STYLE_FILL_AREA(#64152);
#64152=FILL_AREA_STYLE('Charcoal',(#64165));
#64165=FILL_AREA_STYLE_COLOUR('Charcoal',#64178);
#64178=COLOUR_RGB('Charcoal',0.164705882352941,0.184313725490196,0.211764705882353);
ENDSEC;
END-ISO-10303-21;
